ISO-10303-21;
HEADER;
FILE_DESCRIPTION (('STEP AP214'),
    '1' );
FILE_NAME ('screw.step',
    '2026-10-26T19:46:16',
    ( '' ),
    ( '' ),
    'SwSTEP 2.0',
    'SolidWorks 2025',
    '' );
FILE_SCHEMA (( 'AUTOMOTIVE_DESIGN' ));
ENDSEC;

DATA;
#13=ORIENTED_EDGE ( 'NONE', *, *, #39325, .T. ) ;
#20=CARTESIAN_POINT ( 'NONE',  ( -8.342170076843785083E-16, 9.187499998634407916, 4.541265875000002339 ) ) ;
#25=CARTESIAN_POINT ( 'NONE',  ( -2.828427124746190735, 8.375000000000000000, -2.828427124746191623 ) ) ;
#26=CARTESIAN_POINT ( 'NONE',  ( -4.000000000000001776, 21.24999999726881583, -4.898587196589415787E-16 ) ) ;
#27=CARTESIAN_POINT ( 'NONE',  ( -4.541265875000003227, 9.874999998634404363, 1.881053915767121110 ) ) ;
#38=CARTESIAN_POINT ( 'NONE',  ( 1.881053915767122664, 22.12499999863441502, 4.541265875000001451 ) ) ;
#73=CARTESIAN_POINT ( 'NONE',  ( 2.449293598294707893E-16, 11.99999999726881406, -4.000000000000001776 ) ) ;
#110=CARTESIAN_POINT ( 'NONE',  ( 4.541265875000001451, 14.37499999863440969, 1.881053915767124440 ) ) ;
#120=CARTESIAN_POINT ( 'NONE',  ( 2.449293598294707893E-16, 10.99999999726881406, -4.000000000000001776 ) ) ;
#121=CARTESIAN_POINT ( 'NONE',  ( 4.541265875000002339, 0.3749999986344066949, -1.881053915767121776 ) ) ;
#125=DIRECTION ( 'NONE',  ( 0.000000000000000000, 0.000000000000000000, -1.000000000000000000 ) ) ;
#130=CARTESIAN_POINT ( 'NONE',  ( -3.211159895383562723, 11.93749999863440614, 3.211159895383561391 ) ) ;
#131=CARTESIAN_POINT ( 'NONE',  ( -4.000000000000001776, 10.18749999726881406, -1.656854249492381470 ) ) ;
#158=CARTESIAN_POINT ( 'NONE',  ( 4.000000000000001776, 1.749999997268813168, 0.000000000000000000 ) ) ;
#174=CARTESIAN_POINT ( 'NONE',  ( 3.211159895383560947, 12.31249999863440792, 3.211159895383562723 ) ) ;
#185=CARTESIAN_POINT ( 'NONE',  ( 2.828427124746190291, 6.875000000000000000, 2.828427124746192067 ) ) ;
#192=( BOUNDED_CURVE ( )  B_SPLINE_CURVE ( 2, ( #22202, #22962, #68610, #56933, #28993, #11272, #73520, #10154, #349 ),
 .UNSPECIFIED., .F., .F. ) 
 B_SPLINE_CURVE_WITH_KNOTS ( ( 3, 2, 2, 2, 3 ),
 ( 0.7159090909090909394, 0.7215909090909090606, 0.7272727272727272929, 0.7329545454545454142, 0.7386363636363636465 ),
 .UNSPECIFIED. ) 
 CURVE ( )  GEOMETRIC_REPRESENTATION_ITEM ( )  RATIONAL_B_SPLINE_CURVE ( ( 1.000000000000000000, 0.9238795325112867385, 1.000000000000000000, 0.9238795325112867385, 1.000000000000000000, 0.9238795325112867385, 1.000000000000000000, 0.9238795325112867385, 1.000000000000000000 ) ) 
 REPRESENTATION_ITEM ( '' )  );
#202=CARTESIAN_POINT ( 'NONE',  ( 4.541265875000002339, 2.499999998634407028, -1.881053915767121776 ) ) ;
#215=CARTESIAN_POINT ( 'NONE',  ( -1.881053915767124440, 20.12499999863441147, 4.541265875000001451 ) ) ;
#221=DIRECTION ( 'NONE',  ( 0.000000000000000000, -1.000000000000000000, -0.000000000000000000 ) ) ;
#255=EDGE_CURVE ( 'NONE', #7966, #8230, #16802, .T. ) ;
#258=CARTESIAN_POINT ( 'NONE',  ( 4.541265875000002339, 21.37499999863441147, -1.881053915767121554 ) ) ;
#282=VERTEX_POINT ( 'NONE', #23223 ) ;
#294=CARTESIAN_POINT ( 'NONE',  ( -7.347880794884122694E-16, 20.49999999726881583, 4.000000000000001776 ) ) ;
#318=CARTESIAN_POINT ( 'NONE',  ( -1.737867177246331662, 21.99999999999999645, 4.195582608135537406 ) ) ;
#333=CARTESIAN_POINT ( 'NONE',  ( 1.656854249492381914, 20.81250000000000000, 4.000000000000000888 ) ) ;
#344=ADVANCED_FACE ( 'NONE', ( #11537 ), #51902, .T. ) ;
#349=CARTESIAN_POINT ( 'NONE',  ( 2.449293598294707893E-16, 16.99999999726881583, -4.000000000000001776 ) ) ;
#351=CARTESIAN_POINT ( 'NONE',  ( -4.541265875000003227, 10.87499999863440792, 1.881053915767121110 ) ) ;
#357=ORIENTED_EDGE ( 'NONE', *, *, #65945, .F. ) ;
#379=CARTESIAN_POINT ( 'NONE',  ( 2.449293598294707893E-16, 18.99999999726881228, -4.000000000000001776 ) ) ;
#391=ORIENTED_EDGE ( 'NONE', *, *, #6730, .T. ) ;
#392=CARTESIAN_POINT ( 'NONE',  ( -3.211159895383562723, 13.06249999863440792, 3.211159895383561391 ) ) ;
#399=CARTESIAN_POINT ( 'NONE',  ( 1.656854249492381914, 11.81249999999999822, 4.000000000000000888 ) ) ;
#400=CARTESIAN_POINT ( 'NONE',  ( 4.000000000000001776, 21.81249999726881583, -1.656854249492381248 ) ) ;
#401=CARTESIAN_POINT ( 'NONE',  ( 3.211159895383560947, 13.18749999863440792, 3.211159895383562723 ) ) ;
#415=CARTESIAN_POINT ( 'NONE',  ( -4.000000000000001776, 9.187499997268814056, -1.656854249492381470 ) ) ;
#479=CARTESIAN_POINT ( 'NONE',  ( -1.881053915767121776, 14.74999999863440969, -4.541265875000002339 ) ) ;
#491=CARTESIAN_POINT ( 'NONE',  ( 2.449293598294707893E-16, 11.99999999726881406, -4.000000000000001776 ) ) ;
#492=CARTESIAN_POINT ( 'NONE',  ( -3.211159895383561391, 1.687499998634406584, -3.211159895383561835 ) ) ;
#497=CARTESIAN_POINT ( 'NONE',  ( 1.881053915767122664, 12.12499999863440969, 4.541265875000001451 ) ) ;
#540=CARTESIAN_POINT ( 'NONE',  ( -1.881053915767121554, 13.74999999863440969, -4.541265875000002339 ) ) ;
#543=CARTESIAN_POINT ( 'NONE',  ( -4.000000000000001776, 4.249999997268813168, -4.898587196589415787E-16 ) ) ;
#567=CARTESIAN_POINT ( 'NONE',  ( 1.881053915767122664, 1.249999998634407028, 4.541265875000001451 ) ) ;
#579=CARTESIAN_POINT ( 'NONE',  ( -7.347880794884122694E-16, 15.75000000000000000, 4.000000000000001776 ) ) ;
#580=CARTESIAN_POINT ( 'NONE',  ( 2.780723358947928197E-16, 18.68749999863440436, -4.541265875000002339 ) ) ;
#593=CARTESIAN_POINT ( 'NONE',  ( 0.000000000000000000, 0.000000000000000000, 0.000000000000000000 ) ) ;
#630=CARTESIAN_POINT ( 'NONE',  ( 4.541265875000001451, 1.374999998634407250, 1.881053915767124440 ) ) ;
#637=FACE_OUTER_BOUND ( 'NONE', #19104, .T. ) ;
#643=EDGE_CURVE ( 'NONE', #25993, #13507, #1348, .T. ) ;
#658=CARTESIAN_POINT ( 'NONE',  ( 4.898587196589415787E-16, 0.000000000000000000, 4.000000000000001776 ) ) ;
#719=CARTESIAN_POINT ( 'NONE',  ( 1.656854249492381914, 9.812500000000000000, 4.000000000000000888 ) ) ;
#720=CARTESIAN_POINT ( 'NONE',  ( -1.881053915767121554, 10.62499999863440792, -4.541265875000002339 ) ) ;
#722=AXIS2_PLACEMENT_3D ( 'NONE', #11419, #28762, #52161 ) ;
#754=FACE_OUTER_BOUND ( 'NONE', #36560, .T. ) ;
#757=EDGE_CURVE ( 'NONE', #39246, #4559, #64250, .T. ) ;
#766=CARTESIAN_POINT ( 'NONE',  ( -4.000000000000002665, 12.56250000000000000, 1.656854249492380804 ) ) ;
#768=CARTESIAN_POINT ( 'NONE',  ( 3.211159895383560947, 12.18749999863440614, 3.211159895383562723 ) ) ;
#850=CARTESIAN_POINT ( 'NONE',  ( 4.541265875000002339, 17.49999999863440436, -1.881053915767121776 ) ) ;
#854=CARTESIAN_POINT ( 'NONE',  ( -3.211159895383561391, 1.812499998634406584, -3.211159895383561835 ) ) ;
#859=CARTESIAN_POINT ( 'NONE',  ( 4.000000000000000888, 14.68749999726881406, 1.656854249492384135 ) ) ;
#867=CARTESIAN_POINT ( 'NONE',  ( 4.541265875000002339, 13.31249999863440792, 0.000000000000000000 ) ) ;
#895=CARTESIAN_POINT ( 'NONE',  ( -1.881053915767121554, 3.624999998634406584, -4.541265875000002339 ) ) ;
#910=CARTESIAN_POINT ( 'NONE',  ( -1.881053915767121554, 11.74999999863440792, -4.541265875000002339 ) ) ;
#938=EDGE_LOOP ( 'NONE', ( #71940, #18013, #14935, #7021 ) ) ;
#940=CARTESIAN_POINT ( 'NONE',  ( 4.541265875000001451, 2.374999998634407028, 1.881053915767124440 ) ) ;
#952=CARTESIAN_POINT ( 'NONE',  ( -3.211159895383562723, 18.06249999863440792, 3.211159895383561391 ) ) ;
#954=ADVANCED_FACE ( 'NONE', ( #64215 ), #22724, .T. ) ;
#989=EDGE_CURVE ( 'NONE', #43256, #54025, #57831, .T. ) ;
#998=CARTESIAN_POINT ( 'NONE',  ( 3.211159895383561835, 0.5624999986344069169, -3.211159895383561835 ) ) ;
#1002=CARTESIAN_POINT ( 'NONE',  ( 2.449293598294707893E-16, 19.99999999726881228, -4.000000000000001776 ) ) ;
#1014=CARTESIAN_POINT ( 'NONE',  ( 2.449293598294707893E-16, 5.999999997268813168, -4.000000000000001776 ) ) ;
#1015=DIRECTION ( 'NONE',  ( 0.000000000000000000, 0.000000000000000000, -1.000000000000000000 ) ) ;
#1045=ORIENTED_EDGE ( 'NONE', *, *, #35833, .T. ) ;
#1049=( BOUNDED_CURVE ( )  B_SPLINE_CURVE ( 2, ( #3000, #66743, #54319, #2630, #26360, #25981, #48632, #1887, #72016 ),
 .UNSPECIFIED., .F., .F. ) 
 B_SPLINE_CURVE_WITH_KNOTS ( ( 3, 2, 2, 2, 3 ),
 ( 0.2159090909090909116, 0.2215909090909090884, 0.2272727272727272652, 0.2329545454545454419, 0.2386363636363636465 ),
 .UNSPECIFIED. ) 
 CURVE ( )  GEOMETRIC_REPRESENTATION_ITEM ( )  RATIONAL_B_SPLINE_CURVE ( ( 1.000000000000000000, 0.9238795325112867385, 1.000000000000000000, 0.9238795325112867385, 1.000000000000000000, 0.9238795325112867385, 1.000000000000000000, 0.9238795325112867385, 1.000000000000000000 ) ) 
 REPRESENTATION_ITEM ( '' )  );
#1051=VECTOR ( 'NONE', #57308, 1000.000000000000000 ) ;
#1056=ADVANCED_FACE ( 'NONE', ( #6137 ), #29515, .T. ) ;
#1084=AXIS2_PLACEMENT_3D ( 'NONE', #45896, #29301, #57991 ) ;
#1089=CARTESIAN_POINT ( 'NONE',  ( -3.211159895383562723, 8.937499998634407916, 3.211159895383561391 ) ) ;
#1102=CARTESIAN_POINT ( 'NONE',  ( 4.000000000000001776, 8.812499997268814056, -1.656854249492381248 ) ) ;
#1131=CARTESIAN_POINT ( 'NONE',  ( -1.656854249492383691, 10.68750000000000000, 4.000000000000000888 ) ) ;
#1133=CARTESIAN_POINT ( 'NONE',  ( 1.881053915767121998, 13.49999999863440792, -4.541265875000002339 ) ) ;
#1144=CARTESIAN_POINT ( 'NONE',  ( 2.449293598294707893E-16, 2.250000000000000444, -4.000000000000001776 ) ) ;
#1158=CARTESIAN_POINT ( 'NONE',  ( 2.449293598294707893E-16, 0.2500000000000001665, -4.000000000000001776 ) ) ;
#1166=DIRECTION ( 'NONE',  ( 0.000000000000000000, 0.000000000000000000, -1.000000000000000000 ) ) ;
#1169=CARTESIAN_POINT ( 'NONE',  ( 4.898587196589415787E-16, 0.000000000000000000, 4.000000000000001776 ) ) ;
#1189=EDGE_CURVE ( 'NONE', #59197, #7770, #19801, .T. ) ;
#1215=CARTESIAN_POINT ( 'NONE',  ( 4.541265875000002339, 17.43749999863440792, 0.000000000000000000 ) ) ;
#1219=CARTESIAN_POINT ( 'NONE',  ( 4.541265875000002339, 0.4374999986344068059, 0.000000000000000000 ) ) ;
#1223=PRODUCT ( 'screw', 'screw', '', ( #51605 ) ) ;
#1224=CARTESIAN_POINT ( 'NONE',  ( -4.000000000000002665, 0.5625000000000002220, 1.656854249492380804 ) ) ;
#1225=CARTESIAN_POINT ( 'NONE',  ( 2.449293598294707893E-16, 12.99999999726881406, -4.000000000000001776 ) ) ;
#1234=CARTESIAN_POINT ( 'NONE',  ( -3.211159895383562723, 14.93749999863440792, 3.211159895383561391 ) ) ;
#1262=CARTESIAN_POINT ( 'NONE',  ( 4.541265875000001451, 3.249999998634406584, 1.881053915767124440 ) ) ;
#1281=CARTESIAN_POINT ( 'NONE',  ( 4.541265875000001451, 18.37499999863441147, 1.881053915767124440 ) ) ;
#1282=CARTESIAN_POINT ( 'NONE',  ( -7.347880794884122694E-16, 10.75000000000000000, 4.000000000000001776 ) ) ;
#1305=CARTESIAN_POINT ( 'NONE',  ( 4.541265875000002339, 5.437499998634407028, 0.000000000000000000 ) ) ;
#1308=EDGE_CURVE ( 'NONE', #2093, #60340, #7533, .T. ) ;
#1316=CARTESIAN_POINT ( 'NONE',  ( -2.828427124746190735, 2.124999997268813168, -2.828427124746191623 ) ) ;
#1323=CARTESIAN_POINT ( 'NONE',  ( -4.541265875000002339, 0.7499999986344069169, -1.881053915767121998 ) ) ;
#1348=LINE ( 'NONE', #19401, #58660 ) ;
#1365=CARTESIAN_POINT ( 'NONE',  ( 3.211159895383561835, 2.562499998634407028, -3.211159895383561835 ) ) ;
#1381=DIRECTION ( 'NONE',  ( -0.000000000000000000, -1.000000000000000000, -0.000000000000000000 ) ) ;
#1449=VECTOR ( 'NONE', #45886, 1000.000000000000000 ) ;
#1460=CARTESIAN_POINT ( 'NONE',  ( 4.541265875000002339, 9.374999998634404363, -1.881053915767121554 ) ) ;
#1502=EDGE_CURVE ( 'NONE', #61146, #45464, #50803, .T. ) ;
#1507=CARTESIAN_POINT ( 'NONE',  ( -2.828427124746192067, 10.62500000000000000, 2.828427124746190735 ) ) ;
#1509=CARTESIAN_POINT ( 'NONE',  ( -1.881053915767121776, 12.62499999863441147, -4.541265875000002339 ) ) ;
#1512=VERTEX_POINT ( 'NONE', #27881 ) ;
#1517=CARTESIAN_POINT ( 'NONE',  ( 2.449293598294707893E-16, 13.99999999726881406, -4.000000000000001776 ) ) ;
#1581=CARTESIAN_POINT ( 'NONE',  ( 3.211159895383560947, 18.31249999863440792, 3.211159895383562723 ) ) ;
#1590=CARTESIAN_POINT ( 'NONE',  ( 4.000000000000001776, 1.806524977843537691E-16, 0.000000000000000000 ) ) ;
#1591=CARTESIAN_POINT ( 'NONE',  ( -1.656854249492383691, 13.43749999726881406, 4.000000000000000888 ) ) ;
#1592=CARTESIAN_POINT ( 'NONE',  ( 1.881053915767122664, 1.124999998634406584, 4.541265875000001451 ) ) ;
#1600=CARTESIAN_POINT ( 'NONE',  ( 2.780723358947928197E-16, 12.56249999863440792, -4.541265875000002339 ) ) ;
#1628=CARTESIAN_POINT ( 'NONE',  ( -8.342170076843785083E-16, 1.062499998634406584, 4.541265875000002339 ) ) ;
#1644=CARTESIAN_POINT ( 'NONE',  ( -1.881053915767124440, 15.12499999863441147, 4.541265875000001451 ) ) ;
#1670=CARTESIAN_POINT ( 'NONE',  ( -3.211159895383562723, 4.062499998634407028, 3.211159895383561391 ) ) ;
#1678=EDGE_CURVE ( 'NONE', #38403, #28928, #36151, .T. ) ;
#1681=CARTESIAN_POINT ( 'NONE',  ( -1.656854249492383691, 3.437499997268814500, 4.000000000000000888 ) ) ;
#1688=CARTESIAN_POINT ( 'NONE',  ( 4.541265875000002339, 4.312499998634407028, 0.000000000000000000 ) ) ;
#1710=CARTESIAN_POINT ( 'NONE',  ( -1.656854249492381248, 17.06249999726881938, -4.000000000000001776 ) ) ;
#1730=CARTESIAN_POINT ( 'NONE',  ( -8.342170076843785083E-16, 4.187499998634407028, 4.541265875000002339 ) ) ;
#1743=DIRECTION ( 'NONE',  ( 1.224646799147353207E-16, 0.000000000000000000, 1.000000000000000000 ) ) ;
#1754=CARTESIAN_POINT ( 'NONE',  ( -4.000000000000001776, 9.437500000000000000, -1.656854249492381470 ) ) ;
#1766=CARTESIAN_POINT ( 'NONE',  ( 4.898587196589415787E-16, 0.000000000000000000, 4.000000000000001776 ) ) ;
#1773=CARTESIAN_POINT ( 'NONE',  ( 3.211159895383561835, 10.56249999863440792, -3.211159895383561835 ) ) ;
#1787=CARTESIAN_POINT ( 'NONE',  ( 2.449293598294707893E-16, 14.99999999726881406, -4.000000000000001776 ) ) ;
#1812=CARTESIAN_POINT ( 'NONE',  ( -1.881053915767124440, 15.99999999863440614, 4.541265875000001451 ) ) ;
#1827=CARTESIAN_POINT ( 'NONE',  ( -4.000000000000002665, 13.31249999726881406, 1.656854249492380582 ) ) ;
#1831=CARTESIAN_POINT ( 'NONE',  ( 2.828427124746191623, 13.12500000000000000, -2.828427124746191623 ) ) ;
#1851=LINE ( 'NONE', #59561, #1997 ) ;
#1855=CARTESIAN_POINT ( 'NONE',  ( 1.656854249492381914, 10.81250000000000178, 4.000000000000000888 ) ) ;
#1857=CARTESIAN_POINT ( 'NONE',  ( -3.211159895383561391, 16.68749999863440436, -3.211159895383561835 ) ) ;
#1864=CARTESIAN_POINT ( 'NONE',  ( 2.828427124746190291, 13.62499999726881406, 2.828427124746192067 ) ) ;
#1887=CARTESIAN_POINT ( 'NONE',  ( 1.656854249492381248, 5.937499997268813168, -4.000000000000001776 ) ) ;
#1920=CARTESIAN_POINT ( 'NONE',  ( 2.828427124746191623, 7.125000000000000000, -2.828427124746191623 ) ) ;
#1931=LINE ( 'NONE', #47934, #52159 ) ;
#1935=CARTESIAN_POINT ( 'NONE',  ( -3.211159895383562723, 18.06249999863440792, 3.211159895383561391 ) ) ;
#1939=CARTESIAN_POINT ( 'NONE',  ( -1.881053915767121554, 1.749999998634407250, -4.541265875000002339 ) ) ;
#1945=CARTESIAN_POINT ( 'NONE',  ( 4.000000000000001776, 0.06250000000000018041, -1.656854249492381248 ) ) ;
#1946=CARTESIAN_POINT ( 'NONE',  ( -4.000000000000002665, 15.31249999726881406, 1.656854249492380804 ) ) ;
#1947=CARTESIAN_POINT ( 'NONE',  ( -1.881053915767121776, 4.624999998634407028, -4.541265875000002339 ) ) ;
#1953=( NAMED_UNIT ( * ) SI_UNIT ( $, .STERADIAN. ) SOLID_ANGLE_UNIT ( ) );
#1954=CARTESIAN_POINT ( 'NONE',  ( 4.541265875000001451, 14.24999999863440969, 1.881053915767124440 ) ) ;
#1975=DIRECTION ( 'NONE',  ( 0.000000000000000000, 0.000000000000000000, -1.000000000000000000 ) ) ;
#1981=CARTESIAN_POINT ( 'NONE',  ( -3.211159895383561391, 3.687499998634407028, -3.211159895383561835 ) ) ;
#1984=CARTESIAN_POINT ( 'NONE',  ( -7.347880794884122694E-16, 12.75000000000000178, 4.000000000000001776 ) ) ;
#1997=VECTOR ( 'NONE', #40725, 1000.000000000000000 ) ;
#2000=CARTESIAN_POINT ( 'NONE',  ( 2.780723358947928197E-16, 15.68749999863440436, -4.541265875000002339 ) ) ;
#2001=CARTESIAN_POINT ( 'NONE',  ( 1.656854249492381248, 11.18750000000000000, -4.000000000000001776 ) ) ;
#2004=ORIENTED_EDGE ( 'NONE', *, *, #57482, .F. ) ;
#2024=( BOUNDED_CURVE ( )  B_SPLINE_CURVE ( 2, ( #69722, #6722, #13463, #23693, #12733, #53485, #24786, #47801, #70824 ),
 .UNSPECIFIED., .F., .F. ) 
 B_SPLINE_CURVE_WITH_KNOTS ( ( 3, 2, 2, 2, 3 ),
 ( 0.8522727272727272929, 0.8579545454545454142, 0.8636363636363636465, 0.8693181818181817677, 0.8750000000000000000 ),
 .UNSPECIFIED. ) 
 CURVE ( )  GEOMETRIC_REPRESENTATION_ITEM ( )  RATIONAL_B_SPLINE_CURVE ( ( 1.000000000000000000, 0.9238795325112867385, 1.000000000000000000, 0.9238795325112867385, 1.000000000000000000, 0.9238795325112867385, 1.000000000000000000, 0.9238795325112867385, 1.000000000000000000 ) ) 
 REPRESENTATION_ITEM ( '' )  );
#2025=CARTESIAN_POINT ( 'NONE',  ( 4.541265875000001451, 5.374999998634407028, 1.881053915767124440 ) ) ;
#2036=CARTESIAN_POINT ( 'NONE',  ( -2.828427124746192067, 2.374999997268813612, 2.828427124746190735 ) ) ;
#2042=CARTESIAN_POINT ( 'NONE',  ( 1.881053915767121776, 1.499999998634406806, -4.541265875000002339 ) ) ;
#2046=ORIENTED_EDGE ( 'NONE', *, *, #44541, .F. ) ;
#2061=CARTESIAN_POINT ( 'NONE',  ( 2.449293598294707893E-16, 16.99999999726881583, -4.000000000000001776 ) ) ;
#2083=CARTESIAN_POINT ( 'NONE',  ( 3.211159895383561835, 3.562499998634407028, -3.211159895383561835 ) ) ;
#2093=VERTEX_POINT ( 'NONE', #8210 ) ;
#2115=CARTESIAN_POINT ( 'NONE',  ( 4.000000000000001776, 20.81249999726881583, -1.656854249492381248 ) ) ;
#2125=VECTOR ( 'NONE', #40089, 1000.000000000000000 ) ;
#2128=CARTESIAN_POINT ( 'NONE',  ( 1.881053915767121776, 10.62499999863440792, -4.541265875000002339 ) ) ;
#2173=CARTESIAN_POINT ( 'NONE',  ( 4.541265875000002339, 15.37499999863440614, -1.881053915767121554 ) ) ;
#2219=CARTESIAN_POINT ( 'NONE',  ( 2.449293598294707893E-16, 14.25000000000000000, -4.000000000000001776 ) ) ;
#2220=CARTESIAN_POINT ( 'NONE',  ( -8.342170076843785083E-16, 16.06249999863440436, 4.541265875000002339 ) ) ;
#2267=CARTESIAN_POINT ( 'NONE',  ( -4.000000000000001776, 14.43750000000000000, -1.656854249492381470 ) ) ;
#2297=CARTESIAN_POINT ( 'NONE',  ( 3.211159895383560947, 15.31249999863440792, 3.211159895383562723 ) ) ;
#2301=CARTESIAN_POINT ( 'NONE',  ( -4.541265875000003227, 4.999999998634406140, 1.881053915767121110 ) ) ;
#2309=CARTESIAN_POINT ( 'NONE',  ( -2.828427124746190735, 1.375000000000000222, -2.828427124746191623 ) ) ;
#2310=CARTESIAN_POINT ( 'NONE',  ( 2.828427124746190291, 13.62499999726881406, 2.828427124746192067 ) ) ;
#2311=CARTESIAN_POINT ( 'NONE',  ( 2.780723358947928197E-16, 5.562499998634407028, -4.541265875000002339 ) ) ;
#2319=CARTESIAN_POINT ( 'NONE',  ( -1.881053915767121554, 15.62499999863440614, -4.541265875000002339 ) ) ;
#2349=CARTESIAN_POINT ( 'NONE',  ( 4.541265875000002339, 1.374999998634407250, -1.881053915767121554 ) ) ;
#2367=CARTESIAN_POINT ( 'NONE',  ( 3.211159895383560947, 17.31249999863440792, 3.211159895383562723 ) ) ;
#2379=EDGE_LOOP ( 'NONE', ( #73484, #36967, #4096, #32335, #14649, #52420, #58215, #29514, #59829, #62244, #52359, #26218, #58884, #72306, #58361, #42863, #55656, #64132, #60913, #2501, #11329, #69260, #67821, #16128, #16489, #3594, #30902, #22940, #13439, #22835, #9282, #49216, #34373, #31052, #9443, #54495, #357, #58991, #4403, #51856, #5674, #38068, #29978, #64131, #20541, #68866 ) ) ;
#2381=CARTESIAN_POINT ( 'NONE',  ( -1.656854249492381248, 17.31250000000000000, -4.000000000000001776 ) ) ;
#2389=CARTESIAN_POINT ( 'NONE',  ( -1.881053915767124440, 5.124999998634407028, 4.541265875000001451 ) ) ;
#2402=CARTESIAN_POINT ( 'NONE',  ( 1.656854249492394349, 8.812500000000000000, 3.999999999999988898 ) ) ;
#2403=CARTESIAN_POINT ( 'NONE',  ( 2.828427124746191623, 3.874999997268813168, -2.828427124746191623 ) ) ;
#2411=CARTESIAN_POINT ( 'NONE',  ( 3.211159895383561835, 2.437499998634407028, -3.211159895383561835 ) ) ;
#2415=VERTEX_POINT ( 'NONE', #31701 ) ;
#2434=CARTESIAN_POINT ( 'NONE',  ( 0.000000000000000000, 0.000000000000000000, 0.000000000000000000 ) ) ;
#2448=DIRECTION ( 'NONE',  ( -0.000000000000000000, -1.000000000000000000, -0.000000000000000000 ) ) ;
#2455=CARTESIAN_POINT ( 'NONE',  ( -1.881053915767124440, 3.124999998634407472, 4.541265875000001451 ) ) ;
#2460=ORIENTED_EDGE ( 'NONE', *, *, #49917, .T. ) ;
#2500=CARTESIAN_POINT ( 'NONE',  ( 1.881053915767121776, 12.62499999863441147, -4.541265875000002339 ) ) ;
#2501=ORIENTED_EDGE ( 'NONE', *, *, #44244, .F. ) ;
#2512=CARTESIAN_POINT ( 'NONE',  ( 4.000000000000001776, 20.00000000000000000, 0.000000000000000000 ) ) ;
#2515=CARTESIAN_POINT ( 'NONE',  ( -4.443259691721288540, 21.99999999999999645, 0.3623607534594540658 ) ) ;
#2545=CYLINDRICAL_SURFACE ( 'NONE', #24107, 4.000000000000001776 ) ;
#2546=CARTESIAN_POINT ( 'NONE',  ( 1.881053915767121776, 12.49999999863440969, -4.541265875000002339 ) ) ;
#2567=CARTESIAN_POINT ( 'NONE',  ( -7.347880794884122694E-16, 12.75000000000000178, 4.000000000000001776 ) ) ;
#2597=CARTESIAN_POINT ( 'NONE',  ( 4.000000000000000888, 16.93750000000000000, 1.656854249492384135 ) ) ;
#2598=CARTESIAN_POINT ( 'NONE',  ( 1.881053915767121998, 15.49999999863440614, -4.541265875000002339 ) ) ;
#2603=CARTESIAN_POINT ( 'NONE',  ( -7.240284387734133737E-08, 22.00000000000001066, -4.000000000000000888 ) ) ;
#2618=CARTESIAN_POINT ( 'NONE',  ( 2.449293598294707893E-16, 2.999999997268813168, -4.000000000000001776 ) ) ;
#2630=CARTESIAN_POINT ( 'NONE',  ( 4.000000000000000888, 5.687499997268812280, 1.656854249492384135 ) ) ;
#2643=CARTESIAN_POINT ( 'NONE',  ( -2.828427124746190735, 14.37500000000000000, -2.828427124746191623 ) ) ;
#2657=ORIENTED_EDGE ( 'NONE', *, *, #50459, .F. ) ;
#2678=CARTESIAN_POINT ( 'NONE',  ( 2.780723358947928197E-16, 20.68749999863440436, -4.541265875000002339 ) ) ;
#2681=CARTESIAN_POINT ( 'NONE',  ( -3.211159895383561391, 4.812499998634407028, -3.211159895383561835 ) ) ;
#2687=AXIS2_PLACEMENT_3D ( 'NONE', #33432, #56432, #27745 ) ;
#2688=CARTESIAN_POINT ( 'NONE',  ( -2.828427124746190735, 2.375000000000000000, -2.828427124746191623 ) ) ;
#2689=CARTESIAN_POINT ( 'NONE',  ( -2.828427124746190735, 18.12499999726881583, -2.828427124746191623 ) ) ;
#2690=CARTESIAN_POINT ( 'NONE',  ( 4.541265875000002339, 3.312499998634407028, 0.000000000000000000 ) ) ;
#2695=CARTESIAN_POINT ( 'NONE',  ( 4.541265875000001451, 17.24999999863440792, 1.881053915767124440 ) ) ;
#2723=CARTESIAN_POINT ( 'NONE',  ( -8.342170076843785083E-16, 8.062499998634406140, 4.541265875000002339 ) ) ;
#2725=CARTESIAN_POINT ( 'NONE',  ( 2.449293598294707893E-16, 13.99999999726881406, -4.000000000000001776 ) ) ;
#2742=CARTESIAN_POINT ( 'NONE',  ( -1.881053915767124440, 16.12499999863440792, 4.541265875000001451 ) ) ;
#2767=CARTESIAN_POINT ( 'NONE',  ( -4.541265875000002339, 6.874999998634407916, -1.881053915767121998 ) ) ;
#2779=CARTESIAN_POINT ( 'NONE',  ( -2.828427124746190735, 8.124999997268814056, -2.828427124746191623 ) ) ;
#2784=CARTESIAN_POINT ( 'NONE',  ( 1.881053915767122664, 4.124999998634407028, 4.541265875000001451 ) ) ;
#2826=CARTESIAN_POINT ( 'NONE',  ( 2.780723358947928197E-16, 2.687499998634407028, -4.541265875000002339 ) ) ;
#2850=CARTESIAN_POINT ( 'NONE',  ( -4.000000000000002665, 9.562500000000000000, 1.656854249492380582 ) ) ;
#2871=CARTESIAN_POINT ( 'NONE',  ( -4.541265875000002339, 11.87499999863440969, -1.881053915767121998 ) ) ;
#2906=DIRECTION ( 'NONE',  ( -0.000000000000000000, -1.000000000000000000, -0.000000000000000000 ) ) ;
#2917=CARTESIAN_POINT ( 'NONE',  ( 3.211159895383561835, 13.43749999863440614, -3.211159895383561835 ) ) ;
#2931=EDGE_CURVE ( 'NONE', #29918, #68294, #42145, .T. ) ;
#2938=CARTESIAN_POINT ( 'NONE',  ( 1.656854249492381248, 13.18750000000000000, -4.000000000000001776 ) ) ;
#2966=CARTESIAN_POINT ( 'NONE',  ( 2.449293598294707893E-16, 15.25000000000000000, -4.000000000000001776 ) ) ;
#2967=CARTESIAN_POINT ( 'NONE',  ( -1.881053915767121776, 15.62499999863440614, -4.541265875000002339 ) ) ;
#2992=AXIS2_PLACEMENT_3D ( 'NONE', #64532, #12830, #36233 ) ;
#3000=CARTESIAN_POINT ( 'NONE',  ( -7.347880794884122694E-16, 5.499999997268813168, 4.000000000000001776 ) ) ;
#3011=VERTEX_POINT ( 'NONE', #58819 ) ;
#3036=CARTESIAN_POINT ( 'NONE',  ( -7.347880794884122694E-16, 21.75000000000000355, 4.000000000000001776 ) ) ;
#3053=CARTESIAN_POINT ( 'NONE',  ( -4.541265875000002339, 5.874999998634407028, -1.881053915767121998 ) ) ;
#3061=CARTESIAN_POINT ( 'NONE',  ( -1.656854249492381248, 4.312500000000000888, -4.000000000000001776 ) ) ;
#3062=CARTESIAN_POINT ( 'NONE',  ( -1.656854249492383691, 17.43749999726881583, 4.000000000000000888 ) ) ;
#3063=CARTESIAN_POINT ( 'NONE',  ( -1.881053915767124440, 4.999999998634407028, 4.541265875000001451 ) ) ;
#3068=CARTESIAN_POINT ( 'NONE',  ( 4.541265875000002339, 17.31249999863440792, 0.000000000000000000 ) ) ;
#3099=CARTESIAN_POINT ( 'NONE',  ( -1.881053915767121554, 4.624999998634407028, -4.541265875000002339 ) ) ;
#3101=CARTESIAN_POINT ( 'NONE',  ( -7.347880794884122694E-16, 14.49999999726881406, 4.000000000000001776 ) ) ;
#3108=CARTESIAN_POINT ( 'NONE',  ( 4.000000000000001776, 19.74999999726881228, 0.000000000000000000 ) ) ;
#3118=CARTESIAN_POINT ( 'NONE',  ( -3.211159895383562723, 20.06249999863440436, 3.211159895383561391 ) ) ;
#3143=CARTESIAN_POINT ( 'NONE',  ( -3.211159895383562723, 7.062499998634407028, 3.211159895383561391 ) ) ;
#3152=CARTESIAN_POINT ( 'NONE',  ( -4.000000000000001776, 6.249999997268812280, -4.898587196589415787E-16 ) ) ;
#3156=EDGE_CURVE ( 'NONE', #56591, #58773, #25367, .T. ) ;
#3157=CARTESIAN_POINT ( 'NONE',  ( -1.881053915767124440, 6.999999998634407916, 4.541265875000001451 ) ) ;
#3185=ADVANCED_FACE ( 'NONE', ( #8232 ), #72349, .T. ) ;
#3203=CARTESIAN_POINT ( 'NONE',  ( 2.780723358947928197E-16, 9.687499998634406140, -4.541265875000002339 ) ) ;
#3210=DIRECTION ( 'NONE',  ( -0.000000000000000000, -1.000000000000000000, -0.000000000000000000 ) ) ;
#3232=CARTESIAN_POINT ( 'NONE',  ( 2.449293598294707893E-16, 20.99999999726881583, -4.000000000000001776 ) ) ;
#3236=CARTESIAN_POINT ( 'NONE',  ( -1.403917192747188514, 21.99999999999999645, 4.310151135844173531 ) ) ;
#3247=CARTESIAN_POINT ( 'NONE',  ( -1.881053915767121554, 16.74999999863440792, -4.541265875000002339 ) ) ;
#3258=CARTESIAN_POINT ( 'NONE',  ( 1.656854249492356157, 20.18750000000000000, -4.000000000000026645 ) ) ;
#3284=CARTESIAN_POINT ( 'NONE',  ( 0.000000000000000000, 0.000000000000000000, -4.000000000000001776 ) ) ;
#3286=AXIS2_PLACEMENT_3D ( 'NONE', #71247, #19567, #13526 ) ;
#3292=CARTESIAN_POINT ( 'NONE',  ( -1.881053915767121554, 14.62499999863440969, -4.541265875000002339 ) ) ;
#3312=CARTESIAN_POINT ( 'NONE',  ( 1.656854249492381248, 15.18750000000000000, -4.000000000000001776 ) ) ;
#3329=CARTESIAN_POINT ( 'NONE',  ( -4.000000000000001776, 20.43750000000000000, -1.656854249492381470 ) ) ;
#3330=ORIENTED_EDGE ( 'NONE', *, *, #26684, .F. ) ;
#3338=CARTESIAN_POINT ( 'NONE',  ( 2.828427124746191623, 14.12500000000000000, -2.828427124746191623 ) ) ;
#3340=CARTESIAN_POINT ( 'NONE',  ( -1.881053915767124440, 16.99999999863440436, 4.541265875000001451 ) ) ;
#3420=CARTESIAN_POINT ( 'NONE',  ( 1.881053915767122664, 20.24999999863440436, 4.541265875000001451 ) ) ;
#3421=ORIENTED_EDGE ( 'NONE', *, *, #50964, .F. ) ;
#3423=CARTESIAN_POINT ( 'NONE',  ( -3.211159895383562723, 3.062499998634407028, 3.211159895383561391 ) ) ;
#3429=CARTESIAN_POINT ( 'NONE',  ( 1.656854249492381914, 4.812500000000000888, 4.000000000000000888 ) ) ;
#3430=CARTESIAN_POINT ( 'NONE',  ( -4.000000000000001776, 17.18749999726881228, -1.656854249492381470 ) ) ;
#3431=CARTESIAN_POINT ( 'NONE',  ( 4.541265875000001451, 5.249999998634407028, 1.881053915767124440 ) ) ;
#3435=( BOUNDED_CURVE ( )  B_SPLINE_CURVE ( 2, ( #18804, #11656, #40326, #6747, #52764, #1102, #41446, #64458, #12758 ),
 .UNSPECIFIED., .F., .F. ) 
 B_SPLINE_CURVE_WITH_KNOTS ( ( 3, 2, 2, 2, 3 ),
 ( 0.3522727272727273484, 0.3579545454545455252, 0.3636363636363636465, 0.3693181818181818232, 0.3750000000000000000 ),
 .UNSPECIFIED. ) 
 CURVE ( )  GEOMETRIC_REPRESENTATION_ITEM ( )  RATIONAL_B_SPLINE_CURVE ( ( 0.9999999999999992228, 0.9238795325112875156, 1.000000000000000000, 0.9238795325112867385, 1.000000000000000000, 0.9238795325112867385, 1.000000000000000000, 0.9238795325112867385, 1.000000000000000000 ) ) 
 REPRESENTATION_ITEM ( '' )  );
#3440=CARTESIAN_POINT ( 'NONE',  ( 4.541265875000002339, 17.37499999863440436, -1.881053915767121554 ) ) ;
#3472=CARTESIAN_POINT ( 'NONE',  ( 4.541265875000002339, 6.374999998634407028, -1.881053915767121554 ) ) ;
#3491=CARTESIAN_POINT ( 'NONE',  ( 1.881053915767122664, 20.24999999863440436, 4.541265875000001451 ) ) ;
#3513=CARTESIAN_POINT ( 'NONE',  ( -3.211159895383561391, 7.812499998634407028, -3.211159895383561835 ) ) ;
#3525=CARTESIAN_POINT ( 'NONE',  ( 2.449293598294707893E-16, 5.999999997268813168, -4.000000000000001776 ) ) ;
#3527=ORIENTED_EDGE ( 'NONE', *, *, #73874, .F. ) ;
#3530=CARTESIAN_POINT ( 'NONE',  ( 4.541265875000001451, 8.249999998634406140, 1.881053915767124440 ) ) ;
#3563=DIRECTION ( 'NONE',  ( -0.000000000000000000, -1.000000000000000000, -0.000000000000000000 ) ) ;
#3576=CARTESIAN_POINT ( 'NONE',  ( -3.211159895383561391, 9.812499998634406140, -3.211159895383561835 ) ) ;
#3594=ORIENTED_EDGE ( 'NONE', *, *, #68852, .F. ) ;
#3620=CARTESIAN_POINT ( 'NONE',  ( -4.541265875000002339, 15.87499999863440436, -1.881053915767121998 ) ) ;
#3632=CARTESIAN_POINT ( 'NONE',  ( -0.7010234751563706457, 22.00000000000001066, -4.000757560460977302 ) ) ;
#3662=CARTESIAN_POINT ( 'NONE',  ( 4.541265875000002339, 17.37499999863440436, -1.881053915767121554 ) ) ;
#3716=CARTESIAN_POINT ( 'NONE',  ( -4.000000000000001776, 17.50000000000000000, -4.898587196589415787E-16 ) ) ;
#3717=CARTESIAN_POINT ( 'NONE',  ( 1.881053915767122664, 20.12499999863441147, 4.541265875000001451 ) ) ;
#3800=CARTESIAN_POINT ( 'NONE',  ( 3.211159895383560947, 20.31249999863440436, 3.211159895383562723 ) ) ;
#3803=AXIS2_PLACEMENT_3D ( 'NONE', #16083, #44778, #49693 ) ;
#3804=CARTESIAN_POINT ( 'NONE',  ( -8.342170076843785083E-16, 5.187499998634407028, 4.541265875000002339 ) ) ;
#3811=CARTESIAN_POINT ( 'NONE',  ( 2.828427124746190291, 3.875000000000000000, 2.828427124746192067 ) ) ;
#3812=CARTESIAN_POINT ( 'NONE',  ( -7.347880794884122694E-16, 17.49999999726881583, 4.000000000000001776 ) ) ;
#3813=CARTESIAN_POINT ( 'NONE',  ( -1.881053915767124440, 7.999999998634407028, 4.541265875000001451 ) ) ;
#3820=CARTESIAN_POINT ( 'NONE',  ( -1.881053915767124440, 18.99999999863440436, 4.541265875000001451 ) ) ;
#3852=CARTESIAN_POINT ( 'NONE',  ( -1.881053915767121554, 6.624999998634407916, -4.541265875000002339 ) ) ;
#3854=CARTESIAN_POINT ( 'NONE',  ( -2.828427124746192067, 14.37499999726881406, 2.828427124746190735 ) ) ;
#3871=CARTESIAN_POINT ( 'NONE',  ( 3.211159895383561835, 20.56249999863440436, -3.211159895383561835 ) ) ;
#3877=CARTESIAN_POINT ( 'NONE',  ( -2.828427124746190735, 12.12499999726881406, -2.828427124746191623 ) ) ;
#3894=CARTESIAN_POINT ( 'NONE',  ( -4.541265875000003227, 6.999999998634407916, 1.881053915767121110 ) ) ;
#3902=( BOUNDED_CURVE ( )  B_SPLINE_CURVE ( 2, ( #46083, #33675, #23073, #68358, #28730, #34795, #51746, #45340, #16652 ),
 .UNSPECIFIED., .F., .F. ) 
 B_SPLINE_CURVE_WITH_KNOTS ( ( 3, 2, 2, 2, 3 ),
 ( 0.8750000000000000000, 0.8806818181818182323, 0.8863636363636363535, 0.8920454545454545858, 0.8977272727272727071 ),
 .UNSPECIFIED. ) 
 CURVE ( )  GEOMETRIC_REPRESENTATION_ITEM ( )  RATIONAL_B_SPLINE_CURVE ( ( 1.000000000000000000, 0.9238795325112867385, 1.000000000000000000, 0.9238795325112867385, 1.000000000000000000, 0.9238795325112867385, 1.000000000000000000, 0.9238795325112867385, 1.000000000000000000 ) ) 
 REPRESENTATION_ITEM ( '' )  );
#3907=CARTESIAN_POINT ( 'NONE',  ( -1.656854249492383691, 5.437499997268813168, 4.000000000000000888 ) ) ;
#3916=CARTESIAN_POINT ( 'NONE',  ( 4.541265875000002339, 7.312499998634407028, 0.000000000000000000 ) ) ;
#3918=CARTESIAN_POINT ( 'NONE',  ( -4.000000000000001776, 13.43750000000000000, -1.656854249492381470 ) ) ;
#3936=CARTESIAN_POINT ( 'NONE',  ( 4.000000000000001776, 0.3749999986344067504, 0.000000000000000000 ) ) ;
#3958=CARTESIAN_POINT ( 'NONE',  ( 1.881053915767121776, 7.624999998634408804, -4.541265875000002339 ) ) ;
#4003=CARTESIAN_POINT ( 'NONE',  ( -1.881053915767121554, 17.74999999863440792, -4.541265875000002339 ) ) ;
#4024=CARTESIAN_POINT ( 'NONE',  ( -4.000000000000001776, 2.249999997268813612, -4.898587196589415787E-16 ) ) ;
#4048=CARTESIAN_POINT ( 'NONE',  ( -8.342170076843785083E-16, 19.06249999863440436, 4.541265875000002339 ) ) ;
#4072=CYLINDRICAL_SURFACE ( 'NONE', #46114, 4.000000000000001776 ) ;
#4077=ORIENTED_EDGE ( 'NONE', *, *, #72067, .T. ) ;
#4078=CARTESIAN_POINT ( 'NONE',  ( -1.656854249492383468, 1.437499997268813390, 4.000000000000000888 ) ) ;
#4085=CARTESIAN_POINT ( 'NONE',  ( -4.000000000000001776, 20.50000000000000000, -4.898587196589415787E-16 ) ) ;
#4096=ORIENTED_EDGE ( 'NONE', *, *, #37547, .F. ) ;
#4097=CARTESIAN_POINT ( 'NONE',  ( 2.449293598294707893E-16, 18.25000000000000000, -4.000000000000001776 ) ) ;
#4098=CARTESIAN_POINT ( 'NONE',  ( -3.211159895383562723, 19.93749999863440436, 3.211159895383561391 ) ) ;
#4144=ORIENTED_EDGE ( 'NONE', *, *, #51043, .T. ) ;
#4179=CARTESIAN_POINT ( 'NONE',  ( -8.342170076843785083E-16, 19.18749999863440436, 4.541265875000002339 ) ) ;
#4183=CARTESIAN_POINT ( 'NONE',  ( 3.211159895383561835, 6.562499998634407028, -3.211159895383561835 ) ) ;
#4188=CARTESIAN_POINT ( 'NONE',  ( -4.000000000000001776, 7.437500000000000888, -1.656854249492381470 ) ) ;
#4189=CARTESIAN_POINT ( 'NONE',  ( 2.828427124746191623, 18.87499999726881228, -2.828427124746191623 ) ) ;
#4190=CARTESIAN_POINT ( 'NONE',  ( -4.541265875000003227, 8.874999998634407916, 1.881053915767121110 ) ) ;
#4196=CARTESIAN_POINT ( 'NONE',  ( 3.211159895383560947, 20.18749999863440436, 3.211159895383562723 ) ) ;
#4227=CARTESIAN_POINT ( 'NONE',  ( -1.881053915767121554, 5.624999998634407028, -4.541265875000002339 ) ) ;
#4245=CARTESIAN_POINT ( 'NONE',  ( -1.881053915767124440, 22.12499999863441502, 4.541265875000001451 ) ) ;
#4266=CARTESIAN_POINT ( 'NONE',  ( -4.541265875000002339, 9.937499998634406140, -5.561446717895856393E-16 ) ) ;
#4275=CARTESIAN_POINT ( 'NONE',  ( -4.000000000000002665, 7.312499997268812280, 1.656854249492380804 ) ) ;
#4281=CARTESIAN_POINT ( 'NONE',  ( -7.347880794884122694E-16, 12.49999999726881406, 4.000000000000001776 ) ) ;
#4282=CARTESIAN_POINT ( 'NONE',  ( 1.881053915767121776, 5.499999998634407028, -4.541265875000002339 ) ) ;
#4283=CARTESIAN_POINT ( 'NONE',  ( -2.828427124746190735, 13.37500000000000000, -2.828427124746191623 ) ) ;
#4289=CARTESIAN_POINT ( 'NONE',  ( -2.828427124746192067, 18.62500000000000000, 2.828427124746190735 ) ) ;
#4296=VECTOR ( 'NONE', #37566, 1000.000000000000000 ) ;
#4305=DIRECTION ( 'NONE',  ( 0.000000000000000000, -1.000000000000000000, 0.000000000000000000 ) ) ;
#4312=CARTESIAN_POINT ( 'NONE',  ( 0.000000000000000000, 0.000000000000000000, 0.000000000000000000 ) ) ;
#4315=FACE_OUTER_BOUND ( 'NONE', #62516, .T. ) ;
#4326=CARTESIAN_POINT ( 'NONE',  ( -3.211159895383561391, 6.812499998634407028, -3.211159895383561835 ) ) ;
#4367=CARTESIAN_POINT ( 'NONE',  ( 2.780723358947928197E-16, 16.68749999863440436, -4.541265875000002339 ) ) ;
#4392=CARTESIAN_POINT ( 'NONE',  ( -2.793570158735337650, 21.99999999999999645, 3.629683044105539214 ) ) ;
#4403=ORIENTED_EDGE ( 'NONE', *, *, #3156, .F. ) ;
#4410=CARTESIAN_POINT ( 'NONE',  ( -4.541265875000003227, 18.87499999863441147, 1.881053915767121110 ) ) ;
#4444=CARTESIAN_POINT ( 'NONE',  ( 2.449293598294707893E-16, 2.250000000000000444, -4.000000000000001776 ) ) ;
#4467=CARTESIAN_POINT ( 'NONE',  ( -4.000000000000002665, 21.56250000000000000, 1.656854249492380804 ) ) ;
#4468=CARTESIAN_POINT ( 'NONE',  ( -4.541265875000002339, 18.74999999863440436, -1.881053915767121998 ) ) ;
#4542=DIRECTION ( 'NONE',  ( -0.000000000000000000, -1.000000000000000000, -0.000000000000000000 ) ) ;
#4548=CARTESIAN_POINT ( 'NONE',  ( -3.211159895383562723, 6.062499998634407028, 3.211159895383561391 ) ) ;
#4555=CARTESIAN_POINT ( 'NONE',  ( 2.828427124746191623, 6.125000000000000000, -2.828427124746191623 ) ) ;
#4556=CARTESIAN_POINT ( 'NONE',  ( 4.000000000000000888, 20.68749999726881228, 1.656854249492384135 ) ) ;
#4557=CARTESIAN_POINT ( 'NONE',  ( -8.342170076843785083E-16, 8.062499998634406140, 4.541265875000002339 ) ) ;
#4559=VERTEX_POINT ( 'NONE', #19484 ) ;
#4567=ORIENTED_EDGE ( 'NONE', *, *, #26684, .T. ) ;
#4605=DIRECTION ( 'NONE',  ( 0.000000000000000000, 0.000000000000000000, 1.000000000000000000 ) ) ;
#4612=CARTESIAN_POINT ( 'NONE',  ( -8.342170076843785083E-16, 22.18749999863440792, 4.541265875000002339 ) ) ;
#4626=EDGE_CURVE ( 'NONE', #31876, #54025, #56696, .T. ) ;
#4636=CARTESIAN_POINT ( 'NONE',  ( 4.541265875000002339, 13.43749999863440792, 0.000000000000000000 ) ) ;
#4646=AXIS2_PLACEMENT_3D ( 'NONE', #65247, #6808, #1166 ) ;
#4649=CARTESIAN_POINT ( 'NONE',  ( -4.000000000000001776, 12.18749999726881406, -1.656854249492381470 ) ) ;
#4655=CARTESIAN_POINT ( 'NONE',  ( 1.656854249492356157, 12.93749999726881406, -4.000000000000026645 ) ) ;
#4656=CARTESIAN_POINT ( 'NONE',  ( -3.211159895383562723, 6.937499998634407028, 3.211159895383561391 ) ) ;
#4688=CARTESIAN_POINT ( 'NONE',  ( -1.656854249492383468, 7.437499997268813168, 4.000000000000000888 ) ) ;
#4699=CARTESIAN_POINT ( 'NONE',  ( -4.541265875000002339, 7.937499998634407028, -5.561446717895856393E-16 ) ) ;
#4718=EDGE_LOOP ( 'NONE', ( #27806, #8190, #59139, #37546 ) ) ;
#4732=CARTESIAN_POINT ( 'NONE',  ( -1.656854249492383468, 7.687500000000000000, 4.000000000000000888 ) ) ;
#4742=CARTESIAN_POINT ( 'NONE',  ( 4.000000000000001776, 3.062500000000000000, -1.656854249492381248 ) ) ;
#4743=CARTESIAN_POINT ( 'NONE',  ( -1.881053915767124440, 15.12499999863441147, 4.541265875000001451 ) ) ;
#4787=CARTESIAN_POINT ( 'NONE',  ( -4.541265875000002339, 18.81249999863440436, -5.561446717895856393E-16 ) ) ;
#4813=CARTESIAN_POINT ( 'NONE',  ( -7.347880794884122694E-16, 5.750000000000000000, 4.000000000000001776 ) ) ;
#4842=CARTESIAN_POINT ( 'NONE',  ( 1.656854249492381248, 19.18749999999999645, -4.000000000000001776 ) ) ;
#4843=CARTESIAN_POINT ( 'NONE',  ( -4.541265875000003227, 17.87499999863441147, 1.881053915767121110 ) ) ;
#4845=VECTOR ( 'NONE', #30191, 1000.000000000000000 ) ;
#4883=CARTESIAN_POINT ( 'NONE',  ( 1.656854249492381914, 16.81250000000000000, 4.000000000000000888 ) ) ;
#4903=( BOUNDED_CURVE ( )  B_SPLINE_CURVE ( 2, ( #70583, #23445, #47194, #18535, #18900, #41542, #35893, #58910, #29115 ),
 .UNSPECIFIED., .F., .F. ) 
 B_SPLINE_CURVE_WITH_KNOTS ( ( 3, 2, 2, 2, 3 ),
 ( 0.6931818181818182323, 0.6988636363636363535, 0.7045454545454545858, 0.7102272727272727071, 0.7159090909090909394 ),
 .UNSPECIFIED. ) 
 CURVE ( )  GEOMETRIC_REPRESENTATION_ITEM ( )  RATIONAL_B_SPLINE_CURVE ( ( 1.000000000000000000, 0.9238795325112867385, 1.000000000000000000, 0.9238795325112867385, 1.000000000000000000, 0.9238795325112867385, 1.000000000000000000, 0.9238795325112867385, 1.000000000000000000 ) ) 
 REPRESENTATION_ITEM ( '' )  );
#4907=DIRECTION ( 'NONE',  ( 0.000000000000000000, 0.000000000000000000, -1.000000000000000000 ) ) ;
#4927=CARTESIAN_POINT ( 'NONE',  ( 4.541265875000002339, 9.437499998634407916, 0.000000000000000000 ) ) ;
#4933=CARTESIAN_POINT ( 'NONE',  ( 4.000000000000001776, 10.06250000000000000, -1.656854249492381248 ) ) ;
#4934=CARTESIAN_POINT ( 'NONE',  ( 1.656854249492381914, 20.56249999726881583, 4.000000000000000888 ) ) ;
#4935=CARTESIAN_POINT ( 'NONE',  ( 1.881053915767121998, 8.499999998634407916, -4.541265875000002339 ) ) ;
#4942=CARTESIAN_POINT ( 'NONE',  ( -2.828427124746192067, 10.62500000000000000, 2.828427124746190735 ) ) ;
#4945=ORIENTED_EDGE ( 'NONE', *, *, #3156, .T. ) ;
#5005=( BOUNDED_CURVE ( )  B_SPLINE_CURVE ( 2, ( #46404, #67933, #38893, #63010, #68672, #52074, #4942, #27940, #74329 ),
 .UNSPECIFIED., .F., .F. ) 
 B_SPLINE_CURVE_WITH_KNOTS ( ( 3, 2, 2, 2, 3 ),
 ( 0.4659090909090909394, 0.4715909090909091717, 0.4772727272727272929, 0.4829545454545454697, 0.4886363636363636465 ),
 .UNSPECIFIED. ) 
 CURVE ( )  GEOMETRIC_REPRESENTATION_ITEM ( )  RATIONAL_B_SPLINE_CURVE ( ( 0.9999999999999992228, 0.9238795325112875156, 1.000000000000000000, 0.9238795325112867385, 1.000000000000000000, 0.9238795325112867385, 1.000000000000000000, 0.9238795325112867385, 1.000000000000000000 ) ) 
 REPRESENTATION_ITEM ( '' )  );
#5007=CARTESIAN_POINT ( 'NONE',  ( 0.000000000000000000, 0.000000000000000000, 0.000000000000000000 ) ) ;
#5012=CARTESIAN_POINT ( 'NONE',  ( 2.780723358947928197E-16, 12.68749999863440792, -4.541265875000002339 ) ) ;
#5024=CARTESIAN_POINT ( 'NONE',  ( -1.656854249492381248, 10.06249999726881406, -4.000000000000001776 ) ) ;
#5030=CARTESIAN_POINT ( 'NONE',  ( -4.541265875000003227, 10.87499999863440792, 1.881053915767121110 ) ) ;
#5032=CARTESIAN_POINT ( 'NONE',  ( 1.656854249492381914, 15.81250000000000000, 4.000000000000000888 ) ) ;
#5074=CARTESIAN_POINT ( 'NONE',  ( 4.541265875000002339, 11.49999999863440792, -1.881053915767121554 ) ) ;
#5103=CARTESIAN_POINT ( 'NONE',  ( 0.000000000000000000, 22.99999999999999645, 0.000000000000000000 ) ) ;
#5117=CARTESIAN_POINT ( 'NONE',  ( 1.881053915767122664, 21.24999999863440436, 4.541265875000001451 ) ) ;
#5135=EDGE_LOOP ( 'NONE', ( #23817, #12140, #70643 ) ) ;
#5140=CARTESIAN_POINT ( 'NONE',  ( -7.347880794884122694E-16, 17.75000000000000355, 4.000000000000001776 ) ) ;
#5162=CARTESIAN_POINT ( 'NONE',  ( -4.541265875000002339, 0.9374999986344068059, -5.561446717895856393E-16 ) ) ;
#5211=CARTESIAN_POINT ( 'NONE',  ( -1.656854249492381248, 21.31250000000000355, -4.000000000000001776 ) ) ;
#5212=CARTESIAN_POINT ( 'NONE',  ( -1.881053915767121776, 18.62499999863441147, -4.541265875000002339 ) ) ;
#5215=CARTESIAN_POINT ( 'NONE',  ( 4.000000000000001776, 4.749999997268813168, 0.000000000000000000 ) ) ;
#5243=VERTEX_POINT ( 'NONE', #53006 ) ;
#5294=CARTESIAN_POINT ( 'NONE',  ( -1.881053915767124440, 8.124999998634407916, 4.541265875000001451 ) ) ;
#5298=CARTESIAN_POINT ( 'NONE',  ( -1.656854249492381248, 7.312500000000000888, -4.000000000000001776 ) ) ;
#5300=CARTESIAN_POINT ( 'NONE',  ( 3.211159895383561835, 6.437499998634407028, -3.211159895383561835 ) ) ;
#5342=CARTESIAN_POINT ( 'NONE',  ( 4.000000000000000888, 11.68749999726881406, 1.656854249492384135 ) ) ;
#5356=CARTESIAN_POINT ( 'NONE',  ( 4.541265875000002339, 22.43749999863440436, 0.000000000000000000 ) ) ;
#5371=ORIENTED_EDGE ( 'NONE', *, *, #8579, .T. ) ;
#5378=CARTESIAN_POINT ( 'NONE',  ( 3.211159895383560947, 11.31249999863440792, 3.211159895383562723 ) ) ;
#5389=CARTESIAN_POINT ( 'NONE',  ( 4.000000000000001776, 11.74999999726881406, 0.000000000000000000 ) ) ;
#5396=CARTESIAN_POINT ( 'NONE',  ( 3.211159895383560947, 10.18749999863440614, 3.211159895383562723 ) ) ;
#5397=CARTESIAN_POINT ( 'NONE',  ( -7.347880794884122694E-16, 15.75000000000000000, 4.000000000000001776 ) ) ;
#5421=CARTESIAN_POINT ( 'NONE',  ( 4.541265875000002339, 0.3124999986344066949, 0.000000000000000000 ) ) ;
#5422=DIRECTION ( 'NONE',  ( -0.000000000000000000, -1.000000000000000000, -0.000000000000000000 ) ) ;
#5440=CARTESIAN_POINT ( 'NONE',  ( -8.342170076843785083E-16, 14.18749999863440792, 4.541265875000002339 ) ) ;
#5470=CARTESIAN_POINT ( 'NONE',  ( 1.881053915767121998, 0.6249999986344068059, -4.541265875000002339 ) ) ;
#5482=CARTESIAN_POINT ( 'NONE',  ( 4.541265875000002339, 21.43749999863440792, 0.000000000000000000 ) ) ;
#5511=CARTESIAN_POINT ( 'NONE',  ( 0.000000000000000000, 0.000000000000000000, 0.000000000000000000 ) ) ;
#5527=CARTESIAN_POINT ( 'NONE',  ( 4.541265875000002339, 22.31249999863440436, 0.000000000000000000 ) ) ;
#5586=CARTESIAN_POINT ( 'NONE',  ( 2.828427124746191623, 18.12500000000000000, -2.828427124746191623 ) ) ;
#5621=CARTESIAN_POINT ( 'NONE',  ( 4.541265875000002339, 9.312499998634407916, 0.000000000000000000 ) ) ;
#5662=CARTESIAN_POINT ( 'NONE',  ( 3.211159895383560947, 6.312499998634407028, 3.211159895383562723 ) ) ;
#5669=CARTESIAN_POINT ( 'NONE',  ( 4.000000000000001776, 8.000000000000000000, 0.000000000000000000 ) ) ;
#5671=CARTESIAN_POINT ( 'NONE',  ( 4.541265875000002339, 13.37499999863440792, -1.881053915767121776 ) ) ;
#5674=ORIENTED_EDGE ( 'NONE', *, *, #55869, .F. ) ;
#5679=CARTESIAN_POINT ( 'NONE',  ( -4.541265875000002339, 21.74999999863440436, -1.881053915767121998 ) ) ;
#5745=B_SPLINE_CURVE_WITH_KNOTS ( 'NONE', 3,
 ( #53834, #53466, #24038, #24413, #2515, #48151, #71161, #59858, #70083, #8171, #64415, #54206, #71527, #12713, #19854, #35745, #65877, #70443, #18758, #41766, #3632, #73036, #26630 ),
 .UNSPECIFIED., .F., .F.,
 ( 4, 2, 2, 2, 2, 2, 2, 2, 1, 2, 2, 4 ),
 ( 0.000000000000000000, 0.001047525702552857358, 0.001571288553829286146, 0.002095051405105714717, 0.003142577107658572292, 0.004190102810211429434, 0.005237628512764286141, 0.005761391364040716230, 0.006285154215317145451, 0.006808917066593575540, 0.007332679917870004761, 0.008380205620422864071 ),
 .UNSPECIFIED. ) ;
#5747=CARTESIAN_POINT ( 'NONE',  ( -4.541265875000002339, 10.93749999863440792, -5.561446717895856393E-16 ) ) ;
#5750=ORIENTED_EDGE ( 'NONE', *, *, #6051, .T. ) ;
#5757=EDGE_CURVE ( 'NONE', #29151, #31018, #13824, .T. ) ;
#5760=CARTESIAN_POINT ( 'NONE',  ( 1.656854249492381914, 10.56249999726881406, 4.000000000000000888 ) ) ;
#5768=CARTESIAN_POINT ( 'NONE',  ( -4.541265875000002339, 11.81249999863440614, -5.561446717895856393E-16 ) ) ;
#5773=CARTESIAN_POINT ( 'NONE',  ( 4.898587196589415787E-16, 0.000000000000000000, 4.000000000000001776 ) ) ;
#5812=AXIS2_PLACEMENT_3D ( 'NONE', #19589, #42605, #65620 ) ;
#5815=CARTESIAN_POINT ( 'NONE',  ( -3.211159895383562723, 11.06249999863440792, 3.211159895383561391 ) ) ;
#5818=CARTESIAN_POINT ( 'NONE',  ( 4.000000000000001776, 7.749999997268813168, 0.000000000000000000 ) ) ;
#5846=CARTESIAN_POINT ( 'NONE',  ( -3.211159895383562723, 2.062499998634407028, 3.211159895383561391 ) ) ;
#5856=CARTESIAN_POINT ( 'NONE',  ( 1.656854249492381248, 3.187500000000000444, -4.000000000000001776 ) ) ;
#5857=CARTESIAN_POINT ( 'NONE',  ( -4.541265875000002339, 18.87499999863441147, -1.881053915767121998 ) ) ;
#5902=CARTESIAN_POINT ( 'NONE',  ( -1.881053915767121554, 20.62499999863441147, -4.541265875000002339 ) ) ;
#5937=ORIENTED_EDGE ( 'NONE', *, *, #73198, .T. ) ;
#5973=CARTESIAN_POINT ( 'NONE',  ( 4.000000000000001776, 21.00000000000000000, 0.000000000000000000 ) ) ;
#5978=ORIENTED_EDGE ( 'NONE', *, *, #9397, .T. ) ;
#5991=CARTESIAN_POINT ( 'NONE',  ( 4.000000000000001776, 17.81249999726881938, -1.656854249492381248 ) ) ;
#5993=CARTESIAN_POINT ( 'NONE',  ( 4.541265875000002339, 12.31249999863440792, 0.000000000000000000 ) ) ;
#6033=CARTESIAN_POINT ( 'NONE',  ( 2.780723358947928197E-16, 12.68749999863440792, -4.541265875000002339 ) ) ;
#6038=CARTESIAN_POINT ( 'NONE',  ( -4.000000000000001776, 11.43750000000000000, -1.656854249492381470 ) ) ;
#6039=CARTESIAN_POINT ( 'NONE',  ( 4.000000000000001776, 20.81249999726881583, -1.656854249492381248 ) ) ;
#6040=CARTESIAN_POINT ( 'NONE',  ( -4.541265875000002339, 11.74999999863440792, -1.881053915767121998 ) ) ;
#6043=EDGE_LOOP ( 'NONE', ( #65120, #32017, #50748, #20469 ) ) ;
#6049=ORIENTED_EDGE ( 'NONE', *, *, #57387, .F. ) ;
#6050=CARTESIAN_POINT ( 'NONE',  ( -3.211159895383561391, 20.68749999863440436, -3.211159895383561835 ) ) ;
#6051=EDGE_CURVE ( 'NONE', #25548, #45848, #32334, .T. ) ;
#6124=CARTESIAN_POINT ( 'NONE',  ( -4.541265875000003227, 10.99999999863440969, 1.881053915767121110 ) ) ;
#6133=CYLINDRICAL_SURFACE ( 'NONE', #52292, 4.000000000000001776 ) ;
#6134=CARTESIAN_POINT ( 'NONE',  ( -4.000000000000002665, 8.312499997268814056, 1.656854249492380804 ) ) ;
#6135=CARTESIAN_POINT ( 'NONE',  ( 1.881053915767121998, 1.499999998634406806, -4.541265875000002339 ) ) ;
#6137=FACE_OUTER_BOUND ( 'NONE', #27094, .T. ) ;
#6141=CARTESIAN_POINT ( 'NONE',  ( 3.211159895383560947, 9.187499998634407916, 3.211159895383562723 ) ) ;
#6158=CARTESIAN_POINT ( 'NONE',  ( -1.737867177246331662, 21.99999999999999645, 4.195582608135537406 ) ) ;
#6173=VERTEX_POINT ( 'NONE', #40588 ) ;
#6182=FACE_OUTER_BOUND ( 'NONE', #42941, .T. ) ;
#6186=CARTESIAN_POINT ( 'NONE',  ( 4.541265875000002339, 12.43749999863440792, 0.000000000000000000 ) ) ;
#6190=EDGE_LOOP ( 'NONE', ( #2004, #26027, #51420, #5371 ) ) ;
#6202=AXIS2_PLACEMENT_3D ( 'NONE', #26956, #3210, #15629 ) ;
#6216=CARTESIAN_POINT ( 'NONE',  ( -1.881053915767121776, 0.7499999986344069169, -4.541265875000002339 ) ) ;
#6232=CARTESIAN_POINT ( 'NONE',  ( -8.342170076843785083E-16, 20.18749999863440436, 4.541265875000002339 ) ) ;
#6252=ORIENTED_EDGE ( 'NONE', *, *, #13058, .T. ) ;
#6274=CARTESIAN_POINT ( 'NONE',  ( 2.449293598294707893E-16, 11.25000000000000000, -4.000000000000001776 ) ) ;
#6278=CARTESIAN_POINT ( 'NONE',  ( -8.342170076843785083E-16, 1.187499998634406806, 4.541265875000002339 ) ) ;
#6284=CARTESIAN_POINT ( 'NONE',  ( -2.828427124746192067, 19.37499999726881228, 2.828427124746190735 ) ) ;
#6288=AXIS2_PLACEMENT_3D ( 'NONE', #17315, #34330, #69754 ) ;
#6305=CARTESIAN_POINT ( 'NONE',  ( 2.828427124746191623, 6.125000000000000000, -2.828427124746191623 ) ) ;
#6314=CARTESIAN_POINT ( 'NONE',  ( 1.656854249492381914, 20.56249999726881583, 4.000000000000000888 ) ) ;
#6372=CARTESIAN_POINT ( 'NONE',  ( 4.541265875000001451, 10.24999999863440792, 1.881053915767124440 ) ) ;
#6379=EDGE_LOOP ( 'NONE', ( #67725, #35718, #41421, #44547 ) ) ;
#6396=ORIENTED_EDGE ( 'NONE', *, *, #73603, .T. ) ;
#6397=CARTESIAN_POINT ( 'NONE',  ( 2.449293598294707893E-16, 4.250000000000000000, -4.000000000000001776 ) ) ;
#6408=CARTESIAN_POINT ( 'NONE',  ( 4.541265875000002339, 0.3749999986344067504, 0.000000000000000000 ) ) ;
#6414=CARTESIAN_POINT ( 'NONE',  ( -4.000000000000001776, 10.50000000000000000, -4.898587196589415787E-16 ) ) ;
#6416=CARTESIAN_POINT ( 'NONE',  ( -1.881053915767124440, 11.99999999863440792, 4.541265875000001451 ) ) ;
#6445=CYLINDRICAL_SURFACE ( 'NONE', #19248, 4.000000000000001776 ) ;
#6495=CARTESIAN_POINT ( 'NONE',  ( 4.541265875000002339, 16.49999999863440436, -1.881053915767121776 ) ) ;
#6504=CARTESIAN_POINT ( 'NONE',  ( 1.656854249492381914, 1.812500000000000444, 4.000000000000000888 ) ) ;
#6505=CARTESIAN_POINT ( 'NONE',  ( -4.000000000000002665, 13.31249999726881406, 1.656854249492380804 ) ) ;
#6512=CARTESIAN_POINT ( 'NONE',  ( -8.342170076843785083E-16, 13.06249999863440792, 4.541265875000002339 ) ) ;
#6534=FACE_OUTER_BOUND ( 'NONE', #6618, .T. ) ;
#6539=CARTESIAN_POINT ( 'NONE',  ( 2.780723358947928197E-16, 2.562499998634407028, -4.541265875000002339 ) ) ;
#6540=CARTESIAN_POINT ( 'NONE',  ( 4.000000000000001776, 1.812499997268813390, -1.656854249492381248 ) ) ;
#6556=CARTESIAN_POINT ( 'NONE',  ( 1.881053915767122664, 13.24999999863441147, 4.541265875000001451 ) ) ;
#6583=CARTESIAN_POINT ( 'NONE',  ( -4.541265875000002339, 0.8749999986344069169, -1.881053915767121998 ) ) ;
#6594=CARTESIAN_POINT ( 'NONE',  ( -4.541265875000003227, 19.99999999863440436, 1.881053915767121110 ) ) ;
#6604=DIRECTION ( 'NONE',  ( 0.000000000000000000, 0.000000000000000000, -1.000000000000000000 ) ) ;
#6609=DIRECTION ( 'NONE',  ( 0.000000000000000000, 0.000000000000000000, -1.000000000000000000 ) ) ;
#6618=EDGE_LOOP ( 'NONE', ( #22908, #2657, #26124, #14038 ) ) ;
#6644=CARTESIAN_POINT ( 'NONE',  ( 1.881053915767121776, 20.49999999863440436, -4.541265875000002339 ) ) ;
#6647=CARTESIAN_POINT ( 'NONE',  ( -1.656854249492383468, 1.687500000000000222, 4.000000000000000888 ) ) ;
#6661=CARTESIAN_POINT ( 'NONE',  ( -4.000000000000002665, 6.312499997268813168, 1.656854249492380582 ) ) ;
#6722=CARTESIAN_POINT ( 'NONE',  ( 1.656854249492381914, 18.81250000000000000, 4.000000000000000888 ) ) ;
#6730=EDGE_CURVE ( 'NONE', #13507, #36205, #43221, .T. ) ;
#6734=CARTESIAN_POINT ( 'NONE',  ( -1.881053915767124440, 10.99999999863440969, 4.541265875000001451 ) ) ;
#6747=CARTESIAN_POINT ( 'NONE',  ( 4.000000000000000888, 8.687499997268814056, 1.656854249492384135 ) ) ;
#6767=CYLINDRICAL_SURFACE ( 'NONE', #9543, 4.000000000000001776 ) ;
#6779=CARTESIAN_POINT ( 'NONE',  ( 2.828427124746191623, 12.12500000000000000, -2.828427124746191623 ) ) ;
#6781=CARTESIAN_POINT ( 'NONE',  ( -3.211159895383562723, 12.93749999863440792, 3.211159895383561391 ) ) ;
#6786=CARTESIAN_POINT ( 'NONE',  ( 2.449293598294707893E-16, 11.25000000000000000, -4.000000000000001776 ) ) ;
#6808=DIRECTION ( 'NONE',  ( -0.000000000000000000, -1.000000000000000000, -0.000000000000000000 ) ) ;
#6826=CARTESIAN_POINT ( 'NONE',  ( 2.449293598294707893E-16, 21.25000000000000000, -4.000000000000001776 ) ) ;
#6842=CYLINDRICAL_SURFACE ( 'NONE', #23189, 4.000000000000001776 ) ;
#6857=CARTESIAN_POINT ( 'NONE',  ( 3.211159895383561835, 16.56249999863440436, -3.211159895383561835 ) ) ;
#6858=ORIENTED_EDGE ( 'NONE', *, *, #70064, .F. ) ;
#6866=CARTESIAN_POINT ( 'NONE',  ( 2.449293598294707893E-16, 0.2500000000000001665, -4.000000000000001776 ) ) ;
#6867=CARTESIAN_POINT ( 'NONE',  ( 4.000000000000000888, 15.68749999726881406, 1.656854249492384135 ) ) ;
#6877=CARTESIAN_POINT ( 'NONE',  ( -1.881053915767121554, 14.62499999863440969, -4.541265875000002339 ) ) ;
#6903=CARTESIAN_POINT ( 'NONE',  ( 4.541265875000002339, 3.374999998634406584, -1.881053915767121554 ) ) ;
#6904=FACE_OUTER_BOUND ( 'NONE', #46594, .T. ) ;
#6906=CARTESIAN_POINT ( 'NONE',  ( 1.656854249492381914, 4.812500000000000888, 4.000000000000000888 ) ) ;
#6921=CARTESIAN_POINT ( 'NONE',  ( -4.541265875000002339, 17.87499999863441147, -1.881053915767121998 ) ) ;
#6923=CARTESIAN_POINT ( 'NONE',  ( 4.000000000000001776, 10.81249999726881406, -1.656854249492381248 ) ) ;
#6947=CARTESIAN_POINT ( 'NONE',  ( 3.211159895383561835, 3.562499998634407028, -3.211159895383561835 ) ) ;
#6959=CARTESIAN_POINT ( 'NONE',  ( 4.000000000000000888, 2.687499997268813612, 1.656854249492384135 ) ) ;
#6965=CARTESIAN_POINT ( 'NONE',  ( 4.541265875000002339, 2.312499998634407028, 0.000000000000000000 ) ) ;
#6982=( BOUNDED_CURVE ( )  B_SPLINE_CURVE ( 2, ( #72733, #55765, #43302, #26312, #42922, #20280, #14995, #65941, #61032 ),
 .UNSPECIFIED., .F., .F. ) 
 B_SPLINE_CURVE_WITH_KNOTS ( ( 3, 2, 2, 2, 3 ),
 ( 0.8750000000000000000, 0.8806818181818182323, 0.8863636363636363535, 0.8920454545454545858, 0.8977272727272727071 ),
 .UNSPECIFIED. ) 
 CURVE ( )  GEOMETRIC_REPRESENTATION_ITEM ( )  RATIONAL_B_SPLINE_CURVE ( ( 1.000000000000000000, 0.9238795325112867385, 1.000000000000000000, 0.9238795325112867385, 1.000000000000000000, 0.9238795325112867385, 1.000000000000000000, 0.9238795325112867385, 1.000000000000000000 ) ) 
 REPRESENTATION_ITEM ( '' )  );
#7011=CARTESIAN_POINT ( 'NONE',  ( -4.541265875000002339, 5.937499998634407028, -5.561446717895856393E-16 ) ) ;
#7021=ORIENTED_EDGE ( 'NONE', *, *, #15763, .F. ) ;
#7038=CARTESIAN_POINT ( 'NONE',  ( 2.449293598294707893E-16, 9.250000000000000000, -4.000000000000001776 ) ) ;
#7053=VERTEX_POINT ( 'NONE', #1984 ) ;
#7102=CARTESIAN_POINT ( 'NONE',  ( 3.211159895383561835, 9.437499998634406140, -3.211159895383561835 ) ) ;
#7111=DIRECTION ( 'NONE',  ( -0.000000000000000000, -1.000000000000000000, -0.000000000000000000 ) ) ;
#7133=CARTESIAN_POINT ( 'NONE',  ( 2.828427124746191623, 21.87499999726881583, -2.828427124746191623 ) ) ;
#7136=EDGE_CURVE ( 'NONE', #23575, #48578, #52928, .T. ) ;
#7147=CARTESIAN_POINT ( 'NONE',  ( -1.656854249492381248, 12.31250000000000000, -4.000000000000001776 ) ) ;
#7149=CARTESIAN_POINT ( 'NONE',  ( 4.541265875000002339, 11.37499999863440969, -1.881053915767121776 ) ) ;
#7183=CARTESIAN_POINT ( 'NONE',  ( -4.000000000000001776, 16.43750000000000000, -1.656854249492381470 ) ) ;
#7231=CARTESIAN_POINT ( 'NONE',  ( -4.541265875000003227, 15.99999999863440614, 1.881053915767121110 ) ) ;
#7240=CARTESIAN_POINT ( 'NONE',  ( -2.828427124746190735, 13.12499999726881406, -2.828427124746191623 ) ) ;
#7246=CARTESIAN_POINT ( 'NONE',  ( -3.211159895383562723, 15.93749999863440436, 3.211159895383561391 ) ) ;
#7268=CARTESIAN_POINT ( 'NONE',  ( 4.000000000000001776, 8.062500000000000000, -1.656854249492381248 ) ) ;
#7276=CARTESIAN_POINT ( 'NONE',  ( -4.541265875000002339, 1.812499998634406584, -5.561446717895856393E-16 ) ) ;
#7278=CARTESIAN_POINT ( 'NONE',  ( 2.449293598294707893E-16, 4.250000000000000000, -4.000000000000001776 ) ) ;
#7293=CARTESIAN_POINT ( 'NONE',  ( 3.211159895383561835, 14.56249999863440792, -3.211159895383561835 ) ) ;
#7320=CARTESIAN_POINT ( 'NONE',  ( 4.541265875000001451, 6.374999998634408804, 1.881053915767124440 ) ) ;
#7331=CARTESIAN_POINT ( 'NONE',  ( 4.000000000000001776, 0.7499999972688131678, 0.000000000000000000 ) ) ;
#7337=CARTESIAN_POINT ( 'NONE',  ( -3.211159895383562723, 0.9374999986344068059, 3.211159895383561391 ) ) ;
#7371=ORIENTED_EDGE ( 'NONE', *, *, #48312, .T. ) ;
#7374=CARTESIAN_POINT ( 'NONE',  ( -7.347880794884122694E-16, 14.75000000000000178, 4.000000000000001776 ) ) ;
#7379=AXIS2_PLACEMENT_3D ( 'NONE', #5007, #51013, #55950 ) ;
#7381=CARTESIAN_POINT ( 'NONE',  ( -4.541265875000002339, 2.937499998634407028, -5.561446717895856393E-16 ) ) ;
#7395=DIRECTION ( 'NONE',  ( -1.000000000000000000, 0.000000000000000000, 1.224646799147353207E-16 ) ) ;
#7427=CARTESIAN_POINT ( 'NONE',  ( 3.211159895383560947, 13.31249999863440792, 3.211159895383562723 ) ) ;
#7449=( BOUNDED_CURVE ( )  B_SPLINE_CURVE ( 2, ( #10382, #73748, #55674, #22055, #74121, #9644, #32665, #45082, #39056 ),
 .UNSPECIFIED., .F., .F. ) 
 B_SPLINE_CURVE_WITH_KNOTS ( ( 3, 2, 2, 2, 3 ),
 ( 0.1931818181818181768, 0.1988636363636363535, 0.2045454545454545581, 0.2102272727272727348, 0.2159090909090909116 ),
 .UNSPECIFIED. ) 
 CURVE ( )  GEOMETRIC_REPRESENTATION_ITEM ( )  RATIONAL_B_SPLINE_CURVE ( ( 1.000000000000000000, 0.9238795325112867385, 1.000000000000000000, 0.9238795325112867385, 1.000000000000000000, 0.9238795325112867385, 1.000000000000000000, 0.9238795325112867385, 1.000000000000000000 ) ) 
 REPRESENTATION_ITEM ( '' )  );
#7473=CARTESIAN_POINT ( 'NONE',  ( -4.541265875000002339, 15.74999999863440614, -1.881053915767121998 ) ) ;
#7478=CARTESIAN_POINT ( 'NONE',  ( 4.000000000000002665, 22.00000000000000000, 0.000000000000000000 ) ) ;
#7490=CARTESIAN_POINT ( 'NONE',  ( 1.656854249492381914, 12.81250000000000178, 4.000000000000000888 ) ) ;
#7503=CARTESIAN_POINT ( 'NONE',  ( 2.828427124746190291, 21.62499999726881583, 2.828427124746192067 ) ) ;
#7506=ORIENTED_EDGE ( 'NONE', *, *, #48180, .T. ) ;
#7516=CARTESIAN_POINT ( 'NONE',  ( 1.656854249492381248, 13.18749999999999822, -4.000000000000001776 ) ) ;
#7518=CARTESIAN_POINT ( 'NONE',  ( 1.881053915767122664, 14.12499999863440792, 4.541265875000001451 ) ) ;
#7533=( BOUNDED_CURVE ( )  B_SPLINE_CURVE ( 2, ( #54332, #25632, #2643, #2267, #13930, #53954, #54705, #47907, #59614 ),
 .UNSPECIFIED., .F., .F. ) 
 B_SPLINE_CURVE_WITH_KNOTS ( ( 3, 2, 2, 2, 3 ),
 ( 0.6477272727272727071, 0.6534090909090909394, 0.6590909090909091717, 0.6647727272727274039, 0.6704545454545455252 ),
 .UNSPECIFIED. ) 
 CURVE ( )  GEOMETRIC_REPRESENTATION_ITEM ( )  RATIONAL_B_SPLINE_CURVE ( ( 1.000000000000000000, 0.9238795325112867385, 1.000000000000000000, 0.9238795325112867385, 1.000000000000000000, 0.9238795325112867385, 1.000000000000000000, 0.9238795325112852952, 1.000000000000001554 ) ) 
 REPRESENTATION_ITEM ( '' )  );
#7554=CARTESIAN_POINT ( 'NONE',  ( -4.000000000000001776, 12.43750000000000000, -1.656854249492381470 ) ) ;
#7595=CARTESIAN_POINT ( 'NONE',  ( -4.541265875000002339, 14.93749999863440792, -5.561446717895856393E-16 ) ) ;
#7604=EDGE_CURVE ( 'NONE', #40293, #41608, #58238, .T. ) ;
#7605=CARTESIAN_POINT ( 'NONE',  ( -2.828427124746192067, 1.625000000000000444, 2.828427124746190735 ) ) ;
#7606=CARTESIAN_POINT ( 'NONE',  ( -4.000000000000001776, 14.24999999726881406, -4.898587196589415787E-16 ) ) ;
#7607=CARTESIAN_POINT ( 'NONE',  ( -1.881053915767121776, 5.624999998634407028, -4.541265875000002339 ) ) ;
#7615=CARTESIAN_POINT ( 'NONE',  ( -3.211159895383561391, 12.68749999863440792, -3.211159895383561835 ) ) ;
#7646=CARTESIAN_POINT ( 'NONE',  ( 4.541265875000002339, 3.312499998634407028, 0.000000000000000000 ) ) ;
#7663=CARTESIAN_POINT ( 'NONE',  ( -4.541265875000002339, 15.93749999863440436, -5.561446717895856393E-16 ) ) ;
#7686=CARTESIAN_POINT ( 'NONE',  ( 4.541265875000001451, 4.374999998634407028, 1.881053915767124440 ) ) ;
#7699=CARTESIAN_POINT ( 'NONE',  ( 4.541265875000002339, 22.43749999863440436, 0.000000000000000000 ) ) ;
#7704=CARTESIAN_POINT ( 'NONE',  ( -4.541265875000002339, 1.749999998634406584, -1.881053915767121998 ) ) ;
#7748=CARTESIAN_POINT ( 'NONE',  ( 4.541265875000001451, 6.374999998634407028, 1.881053915767124440 ) ) ;
#7753=ORIENTED_EDGE ( 'NONE', *, *, #255, .T. ) ;
#7770=VERTEX_POINT ( 'NONE', #37255 ) ;
#7795=CARTESIAN_POINT ( 'NONE',  ( 4.541265875000002339, 13.49999999863440969, -1.881053915767121554 ) ) ;
#7815=CARTESIAN_POINT ( 'NONE',  ( -7.347880794884122694E-16, 9.499999997268814056, 4.000000000000001776 ) ) ;
#7835=CARTESIAN_POINT ( 'NONE',  ( -1.881053915767121554, 12.62499999863441147, -4.541265875000002339 ) ) ;
#7841=EDGE_LOOP ( 'NONE', ( #44322, #39638, #59251, #41828 ) ) ;
#7883=CARTESIAN_POINT ( 'NONE',  ( 2.828427124746190291, 17.87500000000000355, 2.828427124746192067 ) ) ;
#7884=CARTESIAN_POINT ( 'NONE',  ( -4.541265875000002339, 17.81249999863440792, -5.561446717895856393E-16 ) ) ;
#7965=CARTESIAN_POINT ( 'NONE',  ( -3.211159895383562723, 15.06249999863440792, 3.211159895383561391 ) ) ;
#7966=VERTEX_POINT ( 'NONE', #27784 ) ;
#7976=CARTESIAN_POINT ( 'NONE',  ( 1.656854249492381248, 14.93749999726881406, -4.000000000000001776 ) ) ;
#7977=CARTESIAN_POINT ( 'NONE',  ( -4.541265875000002339, 2.812499998634407028, -5.561446717895856393E-16 ) ) ;
#7981=CARTESIAN_POINT ( 'NONE',  ( 3.211159895383560947, 15.18749999863440792, 3.211159895383562723 ) ) ;
#8007=CARTESIAN_POINT ( 'NONE',  ( -4.541265875000002339, 0.8124999986344066949, -5.561446717895856393E-16 ) ) ;
#8025=CARTESIAN_POINT ( 'NONE',  ( 1.881053915767121776, 17.62499999863440436, -4.541265875000002339 ) ) ;
#8047=EDGE_LOOP ( 'NONE', ( #72276, #42422, #37965, #36149 ) ) ;
#8049=CARTESIAN_POINT ( 'NONE',  ( 3.211159895383560947, 6.312499998634407028, 3.211159895383562723 ) ) ;
#8063=CARTESIAN_POINT ( 'NONE',  ( 4.000000000000001776, 1.749999997268813168, 0.000000000000000000 ) ) ;
#8069=CARTESIAN_POINT ( 'NONE',  ( -3.211159895383561391, 2.687499998634407028, -3.211159895383561835 ) ) ;
#8100=CARTESIAN_POINT ( 'NONE',  ( -7.347880794884122694E-16, 11.49999999726881406, 4.000000000000001776 ) ) ;
#8102=AXIS2_PLACEMENT_3D ( 'NONE', #32990, #32611, #71443 ) ;
#8113=CARTESIAN_POINT ( 'NONE',  ( 4.541265875000002339, 2.437499998634407028, 0.000000000000000000 ) ) ;
#8127=CARTESIAN_POINT ( 'NONE',  ( 0.000000000000000000, 15.99999999999998579, 0.000000000000000000 ) ) ;
#8134=EDGE_LOOP ( 'NONE', ( #19210, #53607, #21070, #7371 ) ) ;
#8149=CARTESIAN_POINT ( 'NONE',  ( 0.000000000000000000, 0.000000000000000000, 0.000000000000000000 ) ) ;
#8158=CARTESIAN_POINT ( 'NONE',  ( -8.342170076843785083E-16, 13.18749999863440792, 4.541265875000002339 ) ) ;
#8167=EDGE_LOOP ( 'NONE', ( #73114, #64949, #53039, #38841 ) ) ;
#8171=CARTESIAN_POINT ( 'NONE',  ( -4.002048012587626324, 22.00000000000000355, -1.673623243082883016 ) ) ;
#8190=ORIENTED_EDGE ( 'NONE', *, *, #9936, .T. ) ;
#8200=CARTESIAN_POINT ( 'NONE',  ( -4.541265875000002339, 14.74999999863440969, -1.881053915767121998 ) ) ;
#8208=CARTESIAN_POINT ( 'NONE',  ( 4.898587196589415787E-16, 0.000000000000000000, 4.000000000000001776 ) ) ;
#8210=CARTESIAN_POINT ( 'NONE',  ( 2.449293598294707893E-16, 14.25000000000000000, -4.000000000000001776 ) ) ;
#8224=AXIS2_PLACEMENT_3D ( 'NONE', #33556, #45227, #10524 ) ;
#8230=VERTEX_POINT ( 'NONE', #1002 ) ;
#8232=FACE_OUTER_BOUND ( 'NONE', #59011, .T. ) ;
#8238=VERTEX_POINT ( 'NONE', #23245 ) ;
#8244=CARTESIAN_POINT ( 'NONE',  ( 2.828427124746190291, 16.87500000000000000, 2.828427124746192067 ) ) ;
#8245=CARTESIAN_POINT ( 'NONE',  ( -3.211159895383561391, 14.68749999863440792, -3.211159895383561835 ) ) ;
#8252=CARTESIAN_POINT ( 'NONE',  ( 1.656854249492381248, 13.93749999726881406, -4.000000000000001776 ) ) ;
#8259=EDGE_LOOP ( 'NONE', ( #50198, #64403, #8833, #45434 ) ) ;
#8327=CARTESIAN_POINT ( 'NONE',  ( 1.881053915767121998, 21.62499999863441147, -4.541265875000002339 ) ) ;
#8330=CARTESIAN_POINT ( 'NONE',  ( -4.541265875000002339, 2.937499998634407028, -5.561446717895856393E-16 ) ) ;
#8337=CARTESIAN_POINT ( 'NONE',  ( 4.000000000000001776, 3.062500000000000000, -1.656854249492381248 ) ) ;
#8338=CARTESIAN_POINT ( 'NONE',  ( 1.656854249492381248, 16.93749999726881583, -4.000000000000001776 ) ) ;
#8339=CARTESIAN_POINT ( 'NONE',  ( -3.211159895383562723, 1.937499998634406806, 3.211159895383561391 ) ) ;
#8344=CARTESIAN_POINT ( 'NONE',  ( -1.881053915767121554, 19.62499999863441147, -4.541265875000002339 ) ) ;
#8345=CARTESIAN_POINT ( 'NONE',  ( -7.347880794884122694E-16, 11.75000000000000000, 4.000000000000001776 ) ) ;
#8360=ORIENTED_EDGE ( 'NONE', *, *, #5757, .F. ) ;
#8368=CARTESIAN_POINT ( 'NONE',  ( 2.449293598294707893E-16, 2.999999997268813168, -4.000000000000001776 ) ) ;
#8374=CARTESIAN_POINT ( 'NONE',  ( -1.881053915767124440, 7.999999998634407028, 4.541265875000001451 ) ) ;
#8376=CARTESIAN_POINT ( 'NONE',  ( -1.656854249492381248, 14.06249999726881406, -4.000000000000001776 ) ) ;
#8393=CARTESIAN_POINT ( 'NONE',  ( -3.211159895383561391, 17.81249999863440792, -3.211159895383561835 ) ) ;
#8418=CARTESIAN_POINT ( 'NONE',  ( 4.541265875000001451, 3.374999998634407028, 1.881053915767124440 ) ) ;
#8429=CARTESIAN_POINT ( 'NONE',  ( 1.656854249492381248, 1.937499997268813168, -4.000000000000001776 ) ) ;
#8434=CARTESIAN_POINT ( 'NONE',  ( -3.211159895383562723, 3.937499998634406584, 3.211159895383561391 ) ) ;
#8440=ORIENTED_EDGE ( 'NONE', *, *, #61987, .T. ) ;
#8479=CARTESIAN_POINT ( 'NONE',  ( 2.780723358947928197E-16, 5.687499998634407028, -4.541265875000002339 ) ) ;
#8495=CARTESIAN_POINT ( 'NONE',  ( 4.898587196589415787E-16, 0.000000000000000000, 4.000000000000001776 ) ) ;
#8511=VERTEX_POINT ( 'NONE', #26572 ) ;
#8528=CARTESIAN_POINT ( 'NONE',  ( -4.541265875000003227, 13.99999999863440792, 1.881053915767121110 ) ) ;
#8548=EDGE_CURVE ( 'NONE', #54437, #27667, #11508, .T. ) ;
#8568=EDGE_CURVE ( 'NONE', #29918, #1512, #19195, .T. ) ;
#8573=CARTESIAN_POINT ( 'NONE',  ( 4.541265875000002339, 13.31249999863440792, 0.000000000000000000 ) ) ;
#8578=ORIENTED_EDGE ( 'NONE', *, *, #42246, .T. ) ;
#8579=EDGE_CURVE ( 'NONE', #58773, #52476, #58664, .T. ) ;
#8624=CARTESIAN_POINT ( 'NONE',  ( 1.656854249492381914, 14.81250000000000000, 4.000000000000000888 ) ) ;
#8626=CARTESIAN_POINT ( 'NONE',  ( 2.780723358947928197E-16, 15.56249999863440614, -4.541265875000002339 ) ) ;
#8660=CARTESIAN_POINT ( 'NONE',  ( -7.347880794884122694E-16, 16.75000000000000000, 4.000000000000001776 ) ) ;
#8666=CARTESIAN_POINT ( 'NONE',  ( -7.347880794884122694E-16, 6.750000000000000000, 4.000000000000001776 ) ) ;
#8700=EDGE_CURVE ( 'NONE', #36205, #61146, #48055, .T. ) ;
#8708=CARTESIAN_POINT ( 'NONE',  ( -1.881053915767121554, 5.749999998634407028, -4.541265875000002339 ) ) ;
#8717=CARTESIAN_POINT ( 'NONE',  ( -1.656854249492383691, 3.687500000000000444, 4.000000000000000888 ) ) ;
#8718=CARTESIAN_POINT ( 'NONE',  ( 2.449293598294707893E-16, 19.99999999726881228, -4.000000000000001776 ) ) ;
#8719=CARTESIAN_POINT ( 'NONE',  ( 3.211159895383561835, 4.437499998634407028, -3.211159895383561835 ) ) ;
#8725=CARTESIAN_POINT ( 'NONE',  ( -3.211159895383561391, 16.68749999863440436, -3.211159895383561835 ) ) ;
#8751=CARTESIAN_POINT ( 'NONE',  ( 0.000000000000000000, 0.000000000000000000, 0.000000000000000000 ) ) ;
#8757=CARTESIAN_POINT ( 'NONE',  ( 1.881053915767121776, 6.499999998634407028, -4.541265875000002339 ) ) ;
#8775=CARTESIAN_POINT ( 'NONE',  ( 4.541265875000001451, 22.37499999863441147, 1.881053915767124440 ) ) ;
#8799=CARTESIAN_POINT ( 'NONE',  ( 1.881053915767121998, 7.624999998634407916, -4.541265875000002339 ) ) ;
#8811=CARTESIAN_POINT ( 'NONE',  ( 4.000000000000001776, 4.749999997268813168, 0.000000000000000000 ) ) ;
#8816=CARTESIAN_POINT ( 'NONE',  ( -4.541265875000003227, 7.874999998634407028, 1.881053915767121110 ) ) ;
#8833=ORIENTED_EDGE ( 'NONE', *, *, #70378, .T. ) ;
#8837=CYLINDRICAL_SURFACE ( 'NONE', #8102, 4.000000000000001776 ) ;
#8861=CARTESIAN_POINT ( 'NONE',  ( -1.881053915767124440, 9.124999998634407916, 4.541265875000001451 ) ) ;
#8904=CARTESIAN_POINT ( 'NONE',  ( -8.342170076843785083E-16, 16.18749999863440436, 4.541265875000002339 ) ) ;
#8948=CARTESIAN_POINT ( 'NONE',  ( 2.780723358947928197E-16, 12.56249999863440792, -4.541265875000002339 ) ) ;
#8998=CARTESIAN_POINT ( 'NONE',  ( 4.000000000000001776, 17.06250000000000355, -1.656854249492381248 ) ) ;
#8999=CARTESIAN_POINT ( 'NONE',  ( -4.541265875000002339, 16.81249999863440436, -5.561446717895856393E-16 ) ) ;
#9022=CARTESIAN_POINT ( 'NONE',  ( 1.656854249492381248, 14.18750000000000000, -4.000000000000001776 ) ) ;
#9085=CARTESIAN_POINT ( 'NONE',  ( -3.211159895383562723, 2.062499998634407028, 3.211159895383561391 ) ) ;
#9094=CARTESIAN_POINT ( 'NONE',  ( 1.656854249492381248, 3.187500000000000000, -4.000000000000001776 ) ) ;
#9095=CARTESIAN_POINT ( 'NONE',  ( -4.000000000000002665, 18.31249999726881938, 1.656854249492380804 ) ) ;
#9096=CARTESIAN_POINT ( 'NONE',  ( 1.881053915767121998, 2.499999998634407028, -4.541265875000002339 ) ) ;
#9101=CARTESIAN_POINT ( 'NONE',  ( 3.211159895383561835, 17.43749999863440792, -3.211159895383561835 ) ) ;
#9129=CARTESIAN_POINT ( 'NONE',  ( 1.881053915767122664, 6.124999998634407916, 4.541265875000001451 ) ) ;
#9147=CARTESIAN_POINT ( 'NONE',  ( -8.342170076843785083E-16, 21.18749999863440792, 4.541265875000002339 ) ) ;
#9148=CARTESIAN_POINT ( 'NONE',  ( -7.347880794884122694E-16, 7.750000000000000000, 4.000000000000001776 ) ) ;
#9170=CARTESIAN_POINT ( 'NONE',  ( -1.881053915767124440, 8.124999998634406140, 4.541265875000001451 ) ) ;
#9180=CARTESIAN_POINT ( 'NONE',  ( 4.000000000000000888, 4.687499997268812280, 1.656854249492384135 ) ) ;
#9185=CARTESIAN_POINT ( 'NONE',  ( 3.211159895383560947, 8.187499998634406140, 3.211159895383562723 ) ) ;
#9187=CARTESIAN_POINT ( 'NONE',  ( -4.000000000000002665, 13.56250000000000000, 1.656854249492380582 ) ) ;
#9221=CARTESIAN_POINT ( 'NONE',  ( -4.000000000000001776, 7.187499997268813168, -1.656854249492381470 ) ) ;
#9231=CARTESIAN_POINT ( 'NONE',  ( 3.211159895383560947, 7.312499998634407028, 3.211159895383562723 ) ) ;
#9235=CARTESIAN_POINT ( 'NONE',  ( 2.449293598294707893E-16, 1.250000000000000222, -4.000000000000001776 ) ) ;
#9275=CARTESIAN_POINT ( 'NONE',  ( 4.541265875000002339, 14.49999999863440969, -1.881053915767121554 ) ) ;
#9282=ORIENTED_EDGE ( 'NONE', *, *, #8700, .F. ) ;
#9290=DIRECTION ( 'NONE',  ( 0.000000000000000000, 0.000000000000000000, -1.000000000000000000 ) ) ;
#9324=CARTESIAN_POINT ( 'NONE',  ( 4.541265875000001451, 20.24999999863440436, 1.881053915767124440 ) ) ;
#9359=AXIS2_PLACEMENT_3D ( 'NONE', #16267, #17022, #4605 ) ;
#9372=CARTESIAN_POINT ( 'NONE',  ( -2.828427124746190735, 14.37500000000000000, -2.828427124746191623 ) ) ;
#9373=CARTESIAN_POINT ( 'NONE',  ( 3.211159895383560947, 21.18749999863440792, 3.211159895383562723 ) ) ;
#9397=EDGE_CURVE ( 'NONE', #28738, #23461, #52053, .T. ) ;
#9402=( BOUNDED_CURVE ( )  B_SPLINE_CURVE ( 2, ( #28283, #23359, #46738, #34705, #34339, #73929, #51289, #16568, #379 ),
 .UNSPECIFIED., .F., .F. ) 
 B_SPLINE_CURVE_WITH_KNOTS ( ( 3, 2, 2, 2, 3 ),
 ( 0.8068181818181818787, 0.8125000000000001110, 0.8181818181818183433, 0.8238636363636363535, 0.8295454545454545858 ),
 .UNSPECIFIED. ) 
 CURVE ( )  GEOMETRIC_REPRESENTATION_ITEM ( )  RATIONAL_B_SPLINE_CURVE ( ( 0.9999999999999985567, 0.9238795325112881818, 1.000000000000000000, 0.9238795325112867385, 1.000000000000000000, 0.9238795325112867385, 1.000000000000000000, 0.9238795325112867385, 1.000000000000000000 ) ) 
 REPRESENTATION_ITEM ( '' )  );
#9406=VECTOR ( 'NONE', #64889, 1000.000000000000000 ) ;
#9443=ORIENTED_EDGE ( 'NONE', *, *, #59841, .F. ) ;
#9461=CARTESIAN_POINT ( 'NONE',  ( 3.211159895383561835, 19.56249999863440436, -3.211159895383561835 ) ) ;
#9464=CARTESIAN_POINT ( 'NONE',  ( 3.211159895383561835, 4.562499998634407028, -3.211159895383561835 ) ) ;
#9471=CARTESIAN_POINT ( 'NONE',  ( -2.828427124746192067, 5.625000000000000000, 2.828427124746190735 ) ) ;
#9472=CARTESIAN_POINT ( 'NONE',  ( -2.828427124746192067, 18.37499999726881583, 2.828427124746190735 ) ) ;
#9473=CARTESIAN_POINT ( 'NONE',  ( -1.881053915767121776, 6.624999998634407916, -4.541265875000002339 ) ) ;
#9482=CARTESIAN_POINT ( 'NONE',  ( -4.541265875000002339, 18.81249999863440436, -5.561446717895856393E-16 ) ) ;
#9487=ORIENTED_EDGE ( 'NONE', *, *, #41732, .T. ) ;
#9510=( BOUNDED_CURVE ( )  B_SPLINE_CURVE ( 2, ( #72037, #43371, #24627, #47638, #37734, #6923, #18977, #58989, #26381 ),
 .UNSPECIFIED., .F., .F. ) 
 B_SPLINE_CURVE_WITH_KNOTS ( ( 3, 2, 2, 2, 3 ),
 ( 0.4431818181818181768, 0.4488636363636363535, 0.4545454545454545858, 0.4602272727272727626, 0.4659090909090909394 ),
 .UNSPECIFIED. ) 
 CURVE ( )  GEOMETRIC_REPRESENTATION_ITEM ( )  RATIONAL_B_SPLINE_CURVE ( ( 1.000000000000000000, 0.9238795325112867385, 1.000000000000000000, 0.9238795325112867385, 1.000000000000000000, 0.9238795325112867385, 1.000000000000000000, 0.9238795325112859613, 1.000000000000000666 ) ) 
 REPRESENTATION_ITEM ( '' )  );
#9515=CARTESIAN_POINT ( 'NONE',  ( 4.541265875000002339, 7.374999998634408804, -1.881053915767121554 ) ) ;
#9533=CARTESIAN_POINT ( 'NONE',  ( -4.541265875000003227, 18.99999999863440436, 1.881053915767121110 ) ) ;
#9540=CARTESIAN_POINT ( 'NONE',  ( -1.656854249492381248, 12.06249999726881406, -4.000000000000001776 ) ) ;
#9543=AXIS2_PLACEMENT_3D ( 'NONE', #12048, #52048, #40720 ) ;
#9556=CARTESIAN_POINT ( 'NONE',  ( -4.541265875000002339, 7.874999998634407028, -1.881053915767121998 ) ) ;
#9565=CARTESIAN_POINT ( 'NONE',  ( 2.828427124746191623, 5.874999997268813168, -2.828427124746191623 ) ) ;
#9572=CARTESIAN_POINT ( 'NONE',  ( 1.881053915767122664, 6.124999998634407916, 4.541265875000001451 ) ) ;
#9578=CARTESIAN_POINT ( 'NONE',  ( -4.000000000000001776, 21.50000000000000000, -4.898587196589415787E-16 ) ) ;
#9614=CARTESIAN_POINT ( 'NONE',  ( 4.541265875000001451, 8.374999998634406140, 1.881053915767124440 ) ) ;
#9618=CARTESIAN_POINT ( 'NONE',  ( -2.828427124746190735, 4.124999997268813168, -2.828427124746191623 ) ) ;
#9644=CARTESIAN_POINT ( 'NONE',  ( -4.000000000000002665, 4.562500000000001776, 1.656854249492380582 ) ) ;
#9659=CARTESIAN_POINT ( 'NONE',  ( 4.541265875000002339, 16.49999999863440436, -1.881053915767121554 ) ) ;
#9666=EDGE_CURVE ( 'NONE', #66256, #43772, #36623, .T. ) ;
#9702=CARTESIAN_POINT ( 'NONE',  ( 1.881053915767121776, 18.49999999863440436, -4.541265875000002339 ) ) ;
#9705=DIRECTION ( 'NONE',  ( 0.000000000000000000, 1.000000000000000000, 0.000000000000000000 ) ) ;
#9745=( BOUNDED_CURVE ( )  B_SPLINE_CURVE ( 2, ( #28427, #17097, #23882, #11084, #158, #6540, #29546, #11821, #34858 ),
 .UNSPECIFIED., .F., .F. ) 
 B_SPLINE_CURVE_WITH_KNOTS ( ( 3, 2, 2, 2, 3 ),
 ( 0.03409090909090908839, 0.03977272727272727210, 0.04545454545454545581, 0.05113636363636364646, 0.05681818181818182323 ),
 .UNSPECIFIED. ) 
 CURVE ( )  GEOMETRIC_REPRESENTATION_ITEM ( )  RATIONAL_B_SPLINE_CURVE ( ( 1.000000000000000000, 0.9238795325112867385, 1.000000000000000000, 0.9238795325112867385, 1.000000000000000000, 0.9238795325112867385, 1.000000000000000000, 0.9238795325112866275, 1.000000000000000000 ) ) 
 REPRESENTATION_ITEM ( '' )  );
#9754=CARTESIAN_POINT ( 'NONE',  ( 1.656854249492381914, 20.81250000000000000, 4.000000000000000888 ) ) ;
#9755=CARTESIAN_POINT ( 'NONE',  ( -3.211159895383561391, 19.68749999863440436, -3.211159895383561835 ) ) ;
#9768=EDGE_LOOP ( 'NONE', ( #44265, #28243, #50661, #391 ) ) ;
#9782=VERTEX_POINT ( 'NONE', #48456 ) ;
#9786=FACE_BOUND ( 'NONE', #39775, .T. ) ;
#9830=CARTESIAN_POINT ( 'NONE',  ( 3.211159895383560947, 19.31249999863440436, 3.211159895383562723 ) ) ;
#9834=CARTESIAN_POINT ( 'NONE',  ( 4.541265875000001451, 4.374999998634407028, 1.881053915767124440 ) ) ;
#9841=CARTESIAN_POINT ( 'NONE',  ( 4.000000000000001776, 5.000000000000000000, 0.000000000000000000 ) ) ;
#9842=CARTESIAN_POINT ( 'NONE',  ( -7.347880794884122694E-16, 19.49999999726881228, 4.000000000000001776 ) ) ;
#9843=CARTESIAN_POINT ( 'NONE',  ( -4.541265875000003227, 7.874999998634407028, 1.881053915767121110 ) ) ;
#9850=( BOUNDED_CURVE ( )  B_SPLINE_CURVE ( 2, ( #15797, #50883, #74647, #22576, #33934, #5991, #62948, #27493, #61835 ),
 .UNSPECIFIED., .F., .F. ) 
 B_SPLINE_CURVE_WITH_KNOTS ( ( 3, 2, 2, 2, 3 ),
 ( 0.7613636363636363535, 0.7670454545454545858, 0.7727272727272727071, 0.7784090909090909394, 0.7840909090909090606 ),
 .UNSPECIFIED. ) 
 CURVE ( )  GEOMETRIC_REPRESENTATION_ITEM ( )  RATIONAL_B_SPLINE_CURVE ( ( 1.000000000000000000, 0.9238795325112867385, 1.000000000000000000, 0.9238795325112867385, 1.000000000000000000, 0.9238795325112867385, 1.000000000000000000, 0.9238795325112867385, 1.000000000000000000 ) ) 
 REPRESENTATION_ITEM ( '' )  );
#9851=CARTESIAN_POINT ( 'NONE',  ( -3.211159895383561391, 19.68749999863440436, -3.211159895383561835 ) ) ;
#9861=CARTESIAN_POINT ( 'NONE',  ( 2.449293598294707893E-16, 3.999999997268813168, -4.000000000000001776 ) ) ;
#9882=CARTESIAN_POINT ( 'NONE',  ( -1.881053915767121554, 7.624999998634408804, -4.541265875000002339 ) ) ;
#9898=CARTESIAN_POINT ( 'NONE',  ( -4.541265875000002339, 21.93749999863440792, -5.561446717895856393E-16 ) ) ;
#9917=CARTESIAN_POINT ( 'NONE',  ( -3.211159895383561391, 9.812499998634406140, -3.211159895383561835 ) ) ;
#9929=CARTESIAN_POINT ( 'NONE',  ( -4.000000000000001776, 5.187499997268813168, -1.656854249492381470 ) ) ;
#9930=CARTESIAN_POINT ( 'NONE',  ( 4.541265875000002339, 0.4374999986344068059, 0.000000000000000000 ) ) ;
#9936=EDGE_CURVE ( 'NONE', #60340, #8511, #37150, .T. ) ;
#9937=CARTESIAN_POINT ( 'NONE',  ( -4.541265875000002339, 5.812499998634406140, -5.561446717895856393E-16 ) ) ;
#9972=ORIENTED_EDGE ( 'NONE', *, *, #66470, .F. ) ;
#9982=CARTESIAN_POINT ( 'NONE',  ( -4.541265875000003227, 8.999999998634406140, 1.881053915767121110 ) ) ;
#9983=CARTESIAN_POINT ( 'NONE',  ( 2.449293598294707893E-16, 1.999999997268813168, -4.000000000000001776 ) ) ;
#9985=CARTESIAN_POINT ( 'NONE',  ( 4.000000000000000888, 0.9375000000000001110, 1.656854249492384135 ) ) ;
#9987=VERTEX_POINT ( 'NONE', #62753 ) ;
#9995=ORIENTED_EDGE ( 'NONE', *, *, #53722, .T. ) ;
#10000=CARTESIAN_POINT ( 'NONE',  ( 2.828427124746190291, 14.62499999726881406, 2.828427124746192067 ) ) ;
#10027=CARTESIAN_POINT ( 'NONE',  ( -3.211159895383561391, 16.81249999863440436, -3.211159895383561835 ) ) ;
#10046=CARTESIAN_POINT ( 'NONE',  ( -1.656854249492382580, 2.062499997268813168, -4.000000000000000000 ) ) ;
#10069=CARTESIAN_POINT ( 'NONE',  ( 4.541265875000001451, 18.24999999863440792, 1.881053915767124440 ) ) ;
#10076=CYLINDRICAL_SURFACE ( 'NONE', #3803, 4.000000000000001776 ) ;
#10087=CARTESIAN_POINT ( 'NONE',  ( -8.000000000000003553, 22.99999999999999645, -1.000000000000000000 ) ) ;
#10101=CARTESIAN_POINT ( 'NONE',  ( -4.000000000000001776, 1.187499997268813390, -1.656854249492381470 ) ) ;
#10108=ORIENTED_EDGE ( 'NONE', *, *, #64781, .F. ) ;
#10119=CARTESIAN_POINT ( 'NONE',  ( -2.828427124746190735, 20.37500000000000000, -2.828427124746191623 ) ) ;
#10120=CARTESIAN_POINT ( 'NONE',  ( -4.541265875000002339, 20.81249999863440436, -5.561446717895856393E-16 ) ) ;
#10133=EDGE_LOOP ( 'NONE', ( #63669, #45840, #22603, #41258, #68474, #73357 ) ) ;
#10154=CARTESIAN_POINT ( 'NONE',  ( 1.656854249492381248, 16.93749999726881583, -4.000000000000001776 ) ) ;
#10186=FACE_OUTER_BOUND ( 'NONE', #29060, .T. ) ;
#10187=( BOUNDED_CURVE ( )  B_SPLINE_CURVE ( 2, ( #43338, #21451, #37324, #33179, #14661, #37702, #71632, #9022, #61451 ),
 .UNSPECIFIED., .F., .F. ) 
 B_SPLINE_CURVE_WITH_KNOTS ( ( 3, 2, 2, 2, 3 ),
 ( 0.6250000000000000000, 0.6306818181818182323, 0.6363636363636363535, 0.6420454545454545858, 0.6477272727272727071 ),
 .UNSPECIFIED. ) 
 CURVE ( )  GEOMETRIC_REPRESENTATION_ITEM ( )  RATIONAL_B_SPLINE_CURVE ( ( 1.000000000000000000, 0.9238795325112867385, 1.000000000000000000, 0.9238795325112867385, 1.000000000000000000, 0.9238795325112867385, 1.000000000000000000, 0.9238795325112867385, 1.000000000000000000 ) ) 
 REPRESENTATION_ITEM ( '' )  );
#10196=ADVANCED_FACE ( 'NONE', ( #6182 ), #18971, .T. ) ;
#10204=VECTOR ( 'NONE', #54874, 1000.000000000000000 ) ;
#10205=CARTESIAN_POINT ( 'NONE',  ( -3.211159895383562723, 8.062499998634406140, 3.211159895383561391 ) ) ;
#10211=CARTESIAN_POINT ( 'NONE',  ( 4.000000000000000888, 6.937500000000000000, 1.656854249492384135 ) ) ;
#10213=CARTESIAN_POINT ( 'NONE',  ( -1.881053915767121776, 9.624999998634404363, -4.541265875000002339 ) ) ;
#10220=CARTESIAN_POINT ( 'NONE',  ( 4.541265875000002339, 21.37499999863441147, -1.881053915767121554 ) ) ;
#10238=EDGE_CURVE ( 'NONE', #31431, #31876, #46530, .T. ) ;
#10271=CARTESIAN_POINT ( 'NONE',  ( -4.541265875000002339, 19.93749999863440436, -5.561446717895856393E-16 ) ) ;
#10293=CARTESIAN_POINT ( 'NONE',  ( 1.881053915767122664, 7.249999998634407916, 4.541265875000001451 ) ) ;
#10303=CARTESIAN_POINT ( 'NONE',  ( 2.449293598294707893E-16, 7.999999997268813168, -4.000000000000001776 ) ) ;
#10304=CARTESIAN_POINT ( 'NONE',  ( 2.828427124746190291, 17.87500000000000355, 2.828427124746192067 ) ) ;
#10305=VERTEX_POINT ( 'NONE', #65725 ) ;
#10308=CARTESIAN_POINT ( 'NONE',  ( 4.000000000000001776, 12.81249999726881406, -1.656854249492381248 ) ) ;
#10309=CARTESIAN_POINT ( 'NONE',  ( -4.541265875000002339, 6.749999998634407916, -1.881053915767121998 ) ) ;
#10342=CARTESIAN_POINT ( 'NONE',  ( -1.656854249492381248, 7.062499997268814056, -4.000000000000001776 ) ) ;
#10353=CARTESIAN_POINT ( 'NONE',  ( 4.541265875000001451, 7.374999998634408804, 1.881053915767124440 ) ) ;
#10366=LINE ( 'NONE', #60549, #39328 ) ;
#10382=CARTESIAN_POINT ( 'NONE',  ( 2.449293598294707893E-16, 4.250000000000000000, -4.000000000000001776 ) ) ;
#10385=CARTESIAN_POINT ( 'NONE',  ( -2.828427124746192067, 7.625000000000000000, 2.828427124746190735 ) ) ;
#10397=CARTESIAN_POINT ( 'NONE',  ( 4.541265875000002339, 17.49999999863440436, -1.881053915767121554 ) ) ;
#10439=CARTESIAN_POINT ( 'NONE',  ( -1.881053915767121554, 19.62499999863441147, -4.541265875000002339 ) ) ;
#10490=CARTESIAN_POINT ( 'NONE',  ( 2.449293598294707893E-16, 19.25000000000000000, -4.000000000000001776 ) ) ;
#10491=CARTESIAN_POINT ( 'NONE',  ( -3.211159895383561391, 21.68749999863440792, -3.211159895383561835 ) ) ;
#10524=DIRECTION ( 'NONE',  ( 0.000000000000000000, -0.000000000000000000, 1.000000000000000000 ) ) ;
#10533=CARTESIAN_POINT ( 'NONE',  ( 4.000000000000001776, 17.06250000000000000, -1.656854249492381248 ) ) ;
#10574=CARTESIAN_POINT ( 'NONE',  ( 1.881053915767122664, 7.249999998634408804, 4.541265875000001451 ) ) ;
#10580=CARTESIAN_POINT ( 'NONE',  ( -1.656854249492381248, 9.312499999999998224, -4.000000000000001776 ) ) ;
#10581=CARTESIAN_POINT ( 'NONE',  ( -1.656854249492383691, 21.43749999726881228, 4.000000000000000888 ) ) ;
#10582=CARTESIAN_POINT ( 'NONE',  ( -4.541265875000002339, 7.812499998634407028, -5.561446717895856393E-16 ) ) ;
#10633=SPHERICAL_SURFACE ( 'NONE', #9359, 10.00000000000001243 ) ;
#10659=CARTESIAN_POINT ( 'NONE',  ( 4.541265875000002339, 12.43749999863440792, 0.000000000000000000 ) ) ;
#10670=CARTESIAN_POINT ( 'NONE',  ( -2.828427124746190735, 9.124999997268814056, -2.828427124746191623 ) ) ;
#10678=CARTESIAN_POINT ( 'NONE',  ( 4.541265875000002339, 8.374999998634406140, -1.881053915767121554 ) ) ;
#10679=CARTESIAN_POINT ( 'NONE',  ( -7.347880794884122694E-16, 10.49999999726881406, 4.000000000000001776 ) ) ;
#10719=CARTESIAN_POINT ( 'NONE',  ( -3.211159895383562723, 14.06249999863440614, 3.211159895383561391 ) ) ;
#10735=CARTESIAN_POINT ( 'NONE',  ( 1.656854249492381248, 14.93749999726881406, -4.000000000000001776 ) ) ;
#10749=CARTESIAN_POINT ( 'NONE',  ( 3.211159895383560947, 2.312499998634407028, 3.211159895383562723 ) ) ;
#10761=CARTESIAN_POINT ( 'NONE',  ( 1.881053915767122664, 18.24999999863440792, 4.541265875000001451 ) ) ;
#10799=EDGE_LOOP ( 'NONE', ( #71111, #39489, #16601, #30567 ) ) ;
#10802=DIRECTION ( 'NONE',  ( -0.000000000000000000, -1.000000000000000000, -0.000000000000000000 ) ) ;
#10809=CARTESIAN_POINT ( 'NONE',  ( 3.211159895383560947, 19.18749999863440436, 3.211159895383562723 ) ) ;
#10827=DIRECTION ( 'NONE',  ( -1.000000000000000000, 0.000000000000000000, -0.000000000000000000 ) ) ;
#10855=ORIENTED_EDGE ( 'NONE', *, *, #69600, .T. ) ;
#10863=CARTESIAN_POINT ( 'NONE',  ( 2.828427124746190291, 18.87500000000000000, 2.828427124746192067 ) ) ;
#10864=CARTESIAN_POINT ( 'NONE',  ( -4.541265875000002339, 21.81249999863440792, -5.561446717895856393E-16 ) ) ;
#10868=CARTESIAN_POINT ( 'NONE',  ( 1.656854249492388576, 4.562499997268813168, 3.999999999999994671 ) ) ;
#10915=CARTESIAN_POINT ( 'NONE',  ( -7.347880794884122694E-16, 1.499999997268813168, 4.000000000000001776 ) ) ;
#10949=CARTESIAN_POINT ( 'NONE',  ( 2.780723358947928197E-16, 9.687499998634406140, -4.541265875000002339 ) ) ;
#10956=CARTESIAN_POINT ( 'NONE',  ( 1.656854249492381914, 7.812500000000000000, 4.000000000000000888 ) ) ;
#10957=CARTESIAN_POINT ( 'NONE',  ( 4.000000000000001776, 20.74999999726881583, 0.000000000000000000 ) ) ;
#10958=CARTESIAN_POINT ( 'NONE',  ( -1.881053915767124440, 5.999999998634406140, 4.541265875000001451 ) ) ;
#11038=CARTESIAN_POINT ( 'NONE',  ( 3.211159895383560947, 13.31249999863440792, 3.211159895383562723 ) ) ;
#11049=DIRECTION ( 'NONE',  ( -0.000000000000000000, -1.000000000000000000, -0.000000000000000000 ) ) ;
#11050=CARTESIAN_POINT ( 'NONE',  ( 1.656854249492381914, 9.562499997268814056, 4.000000000000000888 ) ) ;
#11056=CARTESIAN_POINT ( 'NONE',  ( -8.342170076843785083E-16, 9.062499998634407916, 4.541265875000002339 ) ) ;
#11057=CARTESIAN_POINT ( 'NONE',  ( -2.828427124746192067, 10.37499999726881406, 2.828427124746190735 ) ) ;
#11084=CARTESIAN_POINT ( 'NONE',  ( 4.000000000000000888, 1.687499997268813168, 1.656854249492384135 ) ) ;
#11102=CARTESIAN_POINT ( 'NONE',  ( 4.541265875000001451, 13.37499999863440969, 1.881053915767124440 ) ) ;
#11143=CARTESIAN_POINT ( 'NONE',  ( 1.881053915767122664, 19.24999999863440436, 4.541265875000001451 ) ) ;
#11180=CARTESIAN_POINT ( 'NONE',  ( 2.828427124746190291, 1.875000000000000222, 2.828427124746192067 ) ) ;
#11186=CARTESIAN_POINT ( 'NONE',  ( 1.881053915767121776, 1.624999998634407028, -4.541265875000002339 ) ) ;
#11239=ORIENTED_EDGE ( 'NONE', *, *, #56245, .T. ) ;
#11240=CARTESIAN_POINT ( 'NONE',  ( -2.828427124746192067, 19.62500000000000000, 2.828427124746190735 ) ) ;
#11272=CARTESIAN_POINT ( 'NONE',  ( 4.000000000000001776, 16.81249999726881583, -1.656854249492381248 ) ) ;
#11274=CARTESIAN_POINT ( 'NONE',  ( 4.541265875000002339, 10.37499999863440792, -1.881053915767121554 ) ) ;
#11320=CARTESIAN_POINT ( 'NONE',  ( 1.881053915767122664, 9.249999998634406140, 4.541265875000001451 ) ) ;
#11325=CARTESIAN_POINT ( 'NONE',  ( 1.656854249492381248, 6.187500000000000888, -4.000000000000001776 ) ) ;
#11326=CARTESIAN_POINT ( 'NONE',  ( -4.000000000000001776, 22.24999999726881583, -4.898587196589415787E-16 ) ) ;
#11327=CARTESIAN_POINT ( 'NONE',  ( 4.541265875000002339, 10.31249999863440792, 0.000000000000000000 ) ) ;
#11329=ORIENTED_EDGE ( 'NONE', *, *, #74547, .F. ) ;
#11334=CARTESIAN_POINT ( 'NONE',  ( -1.881053915767124440, 21.99999999863440792, 4.541265875000001451 ) ) ;
#11405=CARTESIAN_POINT ( 'NONE',  ( -8.342170076843785083E-16, 11.18749999863440792, 4.541265875000002339 ) ) ;
#11415=CARTESIAN_POINT ( 'NONE',  ( 0.000000000000000000, 0.000000000000000000, 0.000000000000000000 ) ) ;
#11416=CARTESIAN_POINT ( 'NONE',  ( -2.828427124746192067, 11.37499999726881406, 2.828427124746190735 ) ) ;
#11419=CARTESIAN_POINT ( 'NONE',  ( 0.000000000000000000, 0.000000000000000000, 0.000000000000000000 ) ) ;
#11422=DIRECTION ( 'NONE',  ( 0.000000000000000000, 0.000000000000000000, 1.000000000000000000 ) ) ;
#11423=CARTESIAN_POINT ( 'NONE',  ( 3.211159895383561835, 9.437499998634406140, -3.211159895383561835 ) ) ;
#11445=DIRECTION ( 'NONE',  ( -0.000000000000000000, -1.000000000000000000, -0.000000000000000000 ) ) ;
#11470=CARTESIAN_POINT ( 'NONE',  ( -4.541265875000003227, 10.99999999863440969, 1.881053915767121110 ) ) ;
#11473=CARTESIAN_POINT ( 'NONE',  ( -7.347880794884122694E-16, 7.499999997268813168, 4.000000000000001776 ) ) ;
#11508=( BOUNDED_CURVE ( )  B_SPLINE_CURVE ( 2, ( #33016, #22032, #45057, #68069, #61666, #56017, #27318, #60912, #32257 ),
 .UNSPECIFIED., .F., .F. ) 
 B_SPLINE_CURVE_WITH_KNOTS ( ( 3, 2, 2, 2, 3 ),
 ( 0.1931818181818181768, 0.1988636363636363535, 0.2045454545454545581, 0.2102272727272727348, 0.2159090909090909116 ),
 .UNSPECIFIED. ) 
 CURVE ( )  GEOMETRIC_REPRESENTATION_ITEM ( )  RATIONAL_B_SPLINE_CURVE ( ( 1.000000000000000000, 0.9238795325112867385, 1.000000000000000000, 0.9238795325112867385, 1.000000000000000000, 0.9238795325112867385, 1.000000000000000000, 0.9238795325112867385, 1.000000000000000000 ) ) 
 REPRESENTATION_ITEM ( '' )  );
#11510=CARTESIAN_POINT ( 'NONE',  ( 2.780723358947928197E-16, 19.68749999863440436, -4.541265875000002339 ) ) ;
#11511=VERTEX_POINT ( 'NONE', #13075 ) ;
#11537=FACE_OUTER_BOUND ( 'NONE', #59002, .T. ) ;
#11552=CARTESIAN_POINT ( 'NONE',  ( -4.541265875000002339, 21.81249999863440792, -5.561446717895856393E-16 ) ) ;
#11558=ORIENTED_EDGE ( 'NONE', *, *, #59665, .T. ) ;
#11559=CYLINDRICAL_SURFACE ( 'NONE', #38762, 4.000000000000001776 ) ;
#11606=CARTESIAN_POINT ( 'NONE',  ( 1.881053915767122664, 3.124999998634407028, 4.541265875000001451 ) ) ;
#11610=EDGE_CURVE ( 'NONE', #38403, #7966, #26457, .T. ) ;
#11619=ADVANCED_FACE ( 'NONE', ( #31179 ), #25506, .T. ) ;
#11644=CARTESIAN_POINT ( 'NONE',  ( 4.541265875000001451, 12.24999999863440969, 1.881053915767124440 ) ) ;
#11656=CARTESIAN_POINT ( 'NONE',  ( 1.656854249492394349, 8.562499997268817609, 3.999999999999988898 ) ) ;
#11685=CARTESIAN_POINT ( 'NONE',  ( -4.541265875000002339, 10.93749999863440792, -5.561446717895856393E-16 ) ) ;
#11689=CARTESIAN_POINT ( 'NONE',  ( 4.000000000000001776, 9.062499999999998224, -1.656854249492381248 ) ) ;
#11691=CARTESIAN_POINT ( 'NONE',  ( -3.211159895383561391, 12.68749999863440792, -3.211159895383561835 ) ) ;
#11772=CARTESIAN_POINT ( 'NONE',  ( 4.541265875000002339, 14.43749999863440792, 0.000000000000000000 ) ) ;
#11773=VERTEX_POINT ( 'NONE', #49649 ) ;
#11785=CARTESIAN_POINT ( 'NONE',  ( -4.000000000000002665, 9.312499997268814056, 1.656854249492380804 ) ) ;
#11786=CARTESIAN_POINT ( 'NONE',  ( 4.541265875000002339, 1.374999998634407250, -1.881053915767121776 ) ) ;
#11788=DIRECTION ( 'NONE',  ( -0.000000000000000000, -1.000000000000000000, -0.000000000000000000 ) ) ;
#11792=CARTESIAN_POINT ( 'NONE',  ( -8.342170076843785083E-16, 12.06249999863440614, 4.541265875000002339 ) ) ;
#11793=CARTESIAN_POINT ( 'NONE',  ( 1.656854249492381248, 16.18750000000000000, -4.000000000000001776 ) ) ;
#11814=FACE_OUTER_BOUND ( 'NONE', #5135, .T. ) ;
#11821=CARTESIAN_POINT ( 'NONE',  ( 1.656854249492379472, 1.937499997268812946, -4.000000000000002665 ) ) ;
#11838=CARTESIAN_POINT ( 'NONE',  ( 4.541265875000002339, 12.49999999863440969, -1.881053915767121554 ) ) ;
#11841=ORIENTED_EDGE ( 'NONE', *, *, #11610, .F. ) ;
#11879=CARTESIAN_POINT ( 'NONE',  ( -4.541265875000002339, 20.87499999863441147, -1.881053915767121998 ) ) ;
#11920=FACE_OUTER_BOUND ( 'NONE', #71891, .T. ) ;
#11925=CARTESIAN_POINT ( 'NONE',  ( -8.342170076843785083E-16, 22.06249999863440792, 4.541265875000002339 ) ) ;
#12016=CARTESIAN_POINT ( 'NONE',  ( -4.541265875000003227, 8.874999998634407916, 1.881053915767121110 ) ) ;
#12048=CARTESIAN_POINT ( 'NONE',  ( 0.000000000000000000, 0.000000000000000000, 0.000000000000000000 ) ) ;
#12049=VERTEX_POINT ( 'NONE', #46587 ) ;
#12058=CARTESIAN_POINT ( 'NONE',  ( 2.828427124746191623, 10.12500000000000000, -2.828427124746191623 ) ) ;
#12060=CARTESIAN_POINT ( 'NONE',  ( 1.881053915767121998, 12.49999999863440969, -4.541265875000002339 ) ) ;
#12125=DIRECTION ( 'NONE',  ( -0.000000000000000000, -1.000000000000000000, -0.000000000000000000 ) ) ;
#12139=CARTESIAN_POINT ( 'NONE',  ( -3.211159895383561391, 14.81249999863440792, -3.211159895383561835 ) ) ;
#12140=ORIENTED_EDGE ( 'NONE', *, *, #66470, .T. ) ;
#12150=CARTESIAN_POINT ( 'NONE',  ( -7.347880794884122694E-16, 1.750000000000000222, 4.000000000000001776 ) ) ;
#12151=CARTESIAN_POINT ( 'NONE',  ( -7.347880794884122694E-16, 8.499999997268814056, 4.000000000000001776 ) ) ;
#12153=CARTESIAN_POINT ( 'NONE',  ( -1.881053915767121776, 0.6249999986344065839, -4.541265875000002339 ) ) ;
#12159=CARTESIAN_POINT ( 'NONE',  ( 4.541265875000002339, 10.31249999863440792, 0.000000000000000000 ) ) ;
#12179=DIRECTION ( 'NONE',  ( -0.000000000000000000, -1.000000000000000000, -0.000000000000000000 ) ) ;
#12199=CARTESIAN_POINT ( 'NONE',  ( 2.780723358947928197E-16, 11.68749999863440614, -4.541265875000002339 ) ) ;
#12218=EDGE_CURVE ( 'NONE', #56773, #35916, #24342, .T. ) ;
#12229=CARTESIAN_POINT ( 'NONE',  ( -1.881053915767121776, 1.749999998634407250, -4.541265875000002339 ) ) ;
#12243=CARTESIAN_POINT ( 'NONE',  ( -4.541265875000002339, 19.87499999863440792, -1.881053915767121998 ) ) ;
#12293=CARTESIAN_POINT ( 'NONE',  ( 4.541265875000002339, 1.437499998634406806, 0.000000000000000000 ) ) ;
#12301=CARTESIAN_POINT ( 'NONE',  ( 1.656854249492381248, 15.93749999726881406, -4.000000000000001776 ) ) ;
#12381=CARTESIAN_POINT ( 'NONE',  ( -3.211159895383562723, 11.93749999863440614, 3.211159895383561391 ) ) ;
#12407=CARTESIAN_POINT ( 'NONE',  ( 1.656854249492388576, 3.812500000000000888, 3.999999999999994671 ) ) ;
#12422=CARTESIAN_POINT ( 'NONE',  ( -4.000000000000001776, 12.43750000000000000, -1.656854249492381470 ) ) ;
#12424=CARTESIAN_POINT ( 'NONE',  ( 4.541265875000001451, 12.24999999863440792, 1.881053915767124440 ) ) ;
#12431=CARTESIAN_POINT ( 'NONE',  ( 2.449293598294707893E-16, 6.999999997268813168, -4.000000000000001776 ) ) ;
#12451=EDGE_CURVE ( 'NONE', #61992, #33914, #71446, .T. ) ;
#12476=EDGE_CURVE ( 'NONE', #9987, #12049, #68032, .T. ) ;
#12481=( BOUNDED_CURVE ( )  B_SPLINE_CURVE ( 2, ( #17065, #67647, #10304, #33331, #74413, #62712, #22722, #49915, #45737 ),
 .UNSPECIFIED., .F., .F. ) 
 B_SPLINE_CURVE_WITH_KNOTS ( ( 3, 2, 2, 2, 3 ),
 ( 0.8068181818181818787, 0.8125000000000001110, 0.8181818181818183433, 0.8238636363636363535, 0.8295454545454545858 ),
 .UNSPECIFIED. ) 
 CURVE ( )  GEOMETRIC_REPRESENTATION_ITEM ( )  RATIONAL_B_SPLINE_CURVE ( ( 0.9999999999999985567, 0.9238795325112881818, 1.000000000000000000, 0.9238795325112867385, 1.000000000000000000, 0.9238795325112867385, 1.000000000000000000, 0.9238795325112867385, 1.000000000000000000 ) ) 
 REPRESENTATION_ITEM ( '' )  );
#12495=CARTESIAN_POINT ( 'NONE',  ( -2.828427124746190735, 3.375000000000000000, -2.828427124746191623 ) ) ;
#12505=CARTESIAN_POINT ( 'NONE',  ( 3.211159895383561835, 15.56249999863440614, -3.211159895383561835 ) ) ;
#12510=CARTESIAN_POINT ( 'NONE',  ( -1.881053915767124440, 1.124999998634406584, 4.541265875000001451 ) ) ;
#12516=CARTESIAN_POINT ( 'NONE',  ( -2.828427124746192067, 12.37499999726881406, 2.828427124746190735 ) ) ;
#12517=CARTESIAN_POINT ( 'NONE',  ( 2.449293598294707893E-16, 13.99999999726881406, -4.000000000000001776 ) ) ;
#12519=ADVANCED_FACE ( 'NONE', ( #71823 ), #19398, .T. ) ;
#12520=CARTESIAN_POINT ( 'NONE',  ( 0.000000000000000000, 22.00000000000000355, 0.000000000000000000 ) ) ;
#12525=CARTESIAN_POINT ( 'NONE',  ( 3.211159895383561835, 12.43749999863440792, -3.211159895383561835 ) ) ;
#12526=CARTESIAN_POINT ( 'NONE',  ( 4.000000000000001776, 12.06250000000000000, -1.656854249492381248 ) ) ;
#12555=CARTESIAN_POINT ( 'NONE',  ( -8.342170076843785083E-16, 4.062499998634407028, 4.541265875000002339 ) ) ;
#12571=CARTESIAN_POINT ( 'NONE',  ( 4.541265875000002339, 16.49999999863440436, -1.881053915767121554 ) ) ;
#12572=CARTESIAN_POINT ( 'NONE',  ( 2.828427124746190291, 10.87500000000000178, 2.828427124746192067 ) ) ;
#12595=( BOUNDED_CURVE ( )  B_SPLINE_CURVE ( 2, ( #47928, #24553, #12495, #34798, #47559, #41907, #57803, #52498, #64915 ),
 .UNSPECIFIED., .F., .F. ) 
 B_SPLINE_CURVE_WITH_KNOTS ( ( 3, 2, 2, 2, 3 ),
 ( 0.1477272727272727348, 0.1534090909090909116, 0.1590909090909091161, 0.1647727272727272929, 0.1704545454545454697 ),
 .UNSPECIFIED. ) 
 CURVE ( )  GEOMETRIC_REPRESENTATION_ITEM ( )  RATIONAL_B_SPLINE_CURVE ( ( 1.000000000000000000, 0.9238795325112867385, 1.000000000000000000, 0.9238795325112867385, 1.000000000000000000, 0.9238795325112867385, 1.000000000000000000, 0.9238795325112864054, 1.000000000000000444 ) ) 
 REPRESENTATION_ITEM ( '' )  );
#12596=EDGE_LOOP ( 'NONE', ( #52306, #65838, #54584, #72321 ) ) ;
#12599=CARTESIAN_POINT ( 'NONE',  ( 1.881053915767121998, 4.624999998634407028, -4.541265875000002339 ) ) ;
#12609=CARTESIAN_POINT ( 'NONE',  ( 4.000000000000000888, 1.687499997268813168, 1.656854249492384135 ) ) ;
#12616=CARTESIAN_POINT ( 'NONE',  ( 4.898587196589414801E-16, 1.806524977843537691E-16, 4.000000000000000000 ) ) ;
#12621=CYLINDRICAL_SURFACE ( 'NONE', #44856, 4.000000000000001776 ) ;
#12654=CARTESIAN_POINT ( 'NONE',  ( 1.881053915767121776, 0.6249999986344068059, -4.541265875000002339 ) ) ;
#12711=CARTESIAN_POINT ( 'NONE',  ( -3.211159895383562723, 21.93749999863440792, 3.211159895383561391 ) ) ;
#12713=CARTESIAN_POINT ( 'NONE',  ( -2.786452729588720256, 21.99999999999999289, -3.148080783184952658 ) ) ;
#12733=CARTESIAN_POINT ( 'NONE',  ( 4.000000000000001776, 19.00000000000000000, 0.000000000000000000 ) ) ;
#12746=CARTESIAN_POINT ( 'NONE',  ( -4.541265875000002339, 10.74999999863440969, -1.881053915767121998 ) ) ;
#12758=CARTESIAN_POINT ( 'NONE',  ( 2.449293598294707893E-16, 8.999999997268814056, -4.000000000000001776 ) ) ;
#12770=CARTESIAN_POINT ( 'NONE',  ( 1.656854249492381248, 4.187500000000000000, -4.000000000000001776 ) ) ;
#12772=DIRECTION ( 'NONE',  ( -0.8660254037844401509, 0.4999999999999973910, 0.000000000000000000 ) ) ;
#12789=CARTESIAN_POINT ( 'NONE',  ( -2.828427124746190735, 11.37500000000000000, -2.828427124746191623 ) ) ;
#12791=CARTESIAN_POINT ( 'NONE',  ( -1.881053915767121776, 13.62499999863440792, -4.541265875000002339 ) ) ;
#12830=DIRECTION ( 'NONE',  ( 0.000000000000000000, -0.000000000000000000, 1.000000000000000000 ) ) ;
#12868=CARTESIAN_POINT ( 'NONE',  ( -3.211159895383561391, 15.81249999863440436, -3.211159895383561835 ) ) ;
#12878=CARTESIAN_POINT ( 'NONE',  ( 1.656854249492381914, 13.56249999726881583, 4.000000000000000888 ) ) ;
#12879=CARTESIAN_POINT ( 'NONE',  ( -8.342170076843785083E-16, 1.062499998634406584, 4.541265875000002339 ) ) ;
#12881=VECTOR ( 'NONE', #37404, 1000.000000000000000 ) ;
#12888=CARTESIAN_POINT ( 'NONE',  ( -4.541265875000003227, 13.87499999863440969, 1.881053915767121110 ) ) ;
#12915=CARTESIAN_POINT ( 'NONE',  ( -1.881053915767121554, 2.624999998634406584, -4.541265875000002339 ) ) ;
#12929=ADVANCED_FACE ( 'NONE', ( #6534 ), #69158, .T. ) ;
#12932=CARTESIAN_POINT ( 'NONE',  ( -4.541265875000002339, 16.87499999863440436, -1.881053915767121998 ) ) ;
#12933=CARTESIAN_POINT ( 'NONE',  ( 4.000000000000001776, 11.00000000000000000, 0.000000000000000000 ) ) ;
#12956=CARTESIAN_POINT ( 'NONE',  ( -8.342170076843785083E-16, 6.187499998634407028, 4.541265875000002339 ) ) ;
#12969=CARTESIAN_POINT ( 'NONE',  ( -4.000000000000002665, 3.312499997268814056, 1.656854249492380804 ) ) ;
#12972=ADVANCED_FACE ( 'NONE', ( #11814 ), #57858, .F. ) ;
#12975=CARTESIAN_POINT ( 'NONE',  ( -3.211159895383561391, 1.687499998634406584, -3.211159895383561835 ) ) ;
#13017=CARTESIAN_POINT ( 'NONE',  ( -1.881053915767124440, 5.124999998634406140, 4.541265875000001451 ) ) ;
#13022=ORIENTED_EDGE ( 'NONE', *, *, #9666, .T. ) ;
#13030=DIRECTION ( 'NONE',  ( -0.000000000000000000, -1.000000000000000000, -0.000000000000000000 ) ) ;
#13032=LINE ( 'NONE', #41356, #38080 ) ;
#13043=DIRECTION ( 'NONE',  ( -0.000000000000000000, -1.000000000000000000, -0.000000000000000000 ) ) ;
#13058=EDGE_CURVE ( 'NONE', #28738, #43761, #23499, .T. ) ;
#13063=CARTESIAN_POINT ( 'NONE',  ( 4.541265875000002339, 11.43749999863440614, 0.000000000000000000 ) ) ;
#13075=CARTESIAN_POINT ( 'NONE',  ( 2.449293598294707893E-16, 12.99999999726881406, -4.000000000000001776 ) ) ;
#13101=AXIS2_PLACEMENT_3D ( 'NONE', #47431, #42510, #71920 ) ;
#13107=CARTESIAN_POINT ( 'NONE',  ( -4.541265875000003227, 14.87499999863441147, 1.881053915767121110 ) ) ;
#13121=CARTESIAN_POINT ( 'NONE',  ( 2.449293598294707893E-16, 12.99999999726881406, -4.000000000000001776 ) ) ;
#13125=( BOUNDED_SURFACE ( )  B_SPLINE_SURFACE ( 1, 2, ( 
 ( #1590, #1945, #64581, #58562, #6866, #69501, #40828, #30977, #52892, #1224, #69874, #24934, #47580, #47951, #17811, #18921, #41927, #53998, #24203, #47214, #64936, #23844, #2309, #46481, #36280, #59296, #7605, #63834, #12150, #6504, #46851, #18186, #41202, #64210, #67183, #20018, #43028, #37772, #2688, #43791, #19651, #13974, #31729, #72075, #66050, #60768, #55872, #14358, #49064, #8337, #25306, #9094, #32488, #20393, #37390, #60391, #48323, #42664, #15480, #8717, #54751, #48694, #3811, #66421, #26809, #71330, #32108, #20772, #49823, #3061, #26044, #43407, #31349, #61518, #65675, #14733, #55126, #3429, #26420, #49446, #9841, #54379, #37016, #72464, #66806, #38516, #15109, #38141, #61141, #25674, #9471, #71700, #55499, #32867, #44169, #60018, #72840, #21147, #4555, #11325, #50194, #62253, #74320, #45645, #73949, #22252, #51309, #68661, #22626, #16972, #73213, #10211, #45280, #57358, #39998, #21521, #63001, #5298, #44543, #4188, #44915, #68290, #28300, #23012, #56240, #10956, #50937, #56985, #5669, #15849, #34357, #28666, #51680, #16587, #25, #27550, #46019, #39626, #27930, #69040, #63364, #62625, #21886, #17343, #40364, #11689, #34728, #50563, #27177, #10580, #67553, #38884, #61888, #33240, #73578, #67922, #16215, #39255, #33991, #33611, #56618, #4933, #12058, #52062, #29786, #52797, #24109, #29420, #6414, #70880, #1507, #1131, #59206, #1855, #18463, #63740, #47123, #70156, #41839, #58836, #41473, #18094, #12789, #6038, #24486, #57733, #64489, #13152, #47489, #399, #35821, #40730, #41108, #35092, #6779, #47859, #58103, #7147, #64115, #12422, #30152, #766, #53169, #64848, #70512, #18832, #23752, #35456, #24841, #46754, #52429, #7516, #69777, #58469, #36190, #30522, #53539, #19194, #42197, #65212, #29043, #13517, #23378, #46391, #69409, #17715, #3338, #48970, #2219, #72367, #9372, #48603, #61050, #31637, #66712, #72750, #15014, #8624, #54658, #31256, #42937, #26329, #21055, #59932, #2966, #65586, #44078, #13884, #32013, #25951, #49350, #71984, #53906, #54286, #20297, #60295, #26715, #36924, #48231, #25215, #43315, #66332, #14636, #25587, #19927, #71606, #37679, #20678, #30888, #43697, #8244, #2597, #60678, #8998, #55032, #38050, #32392, #55407, #67090, #71239, #3716, #49735, #36555, #65958, #19559, #59568, #7883, #42573, #14262, #37299, #5586, #39163, #4097, #21428, #16125, #16500, #62165, #68203, #16882, #27090, #33900, #45562, #10863, #27839, #22539, #15759, #51223, #4842, #10490, #74233, #74610, #50846, #33157, #68575, #11240, #39905, #62911, #38798, #34268, #73485, #57271, #28585, #51593, #39540, #22923, #44451, #10119, #62536, #73860, #45937, #22167, #33525, #67462, #9754, #56525, #45193, #56898, #61801, #32773, #50106, #21791, #5211, #56151, #28211, #15387, #4467, #38423, #73120, #61427, #55781, #27456, #50471, #44821 ),
 ( #67833, #30710, #65406, #48420, #24666, #70698, #19017, #1323, #31454, #25770, #7337, #42022, #36376, #47677, #65030, #54479, #52991, #68949, #71058, #2042, #37113, #64676, #12975, #7704, #47318, #13703, #18656, #36747, #60115, #14078, #17259, #40279, #6965, #70344, #2411, #63279, #53362, #59759, #8069, #13339, #59391, #42390, #31070, #54098, #25406, #11606, #24306, #53730, #71423, #19751, #34643, #42758, #19376, #57649, #29974, #36011, #25029, #65775, #8434, #41665, #48049, #2784, #59030, #30343, #1688, #27275, #67281, #20118, #44269, #49921, #43132, #48791, #14827, #66903, #72936, #67653, #26146, #55598, #20869, #26905, #50291, #60490, #15577, #4282, #38618, #61242, #55972, #49165, #9937, #38238, #72566, #32969, #33336, #9572, #66515, #73312, #44639, #21613, #15953, #72174, #38979, #32206, #61986, #10309, #56337, #21245, #4656, #3157, #43504, #61621, #32591, #71798, #3916, #49547, #20486, #66147, #43891, #15207, #14453, #37868, #37489, #8816, #55225, #31828, #60863, #54847, #9185, #3530, #26522, #10678, #58210, #63098, #34830, #51406, #39717, #62719, #50658, #21988, #69510, #68388, #11056, #51038, #6141, #68760, #29147, #73677, #11423, #23106, #52166, #57081, #28399, #74419, #33710, #63843, #27649, #34085, #22727, #17071, #5396, #45746, #12159, #56713, #45014, #28765, #34460, #17822, #22347, #45372, #40093, #5030, #46119, #74047, #69136, #40836, #46489, #68020, #16313, #39350, #28028, #57836, #62347, #57463, #17444, #40465, #5768, #51781, #130, #63468, #11792, #497, #23477, #35194, #16686, #41937, #12525, #70611, #1600, #65317, #7615, #18931, #41576, #36290, #29519, #24944, #6512, #64945, #36659, #47961, #867, #13255, #64218, #64590, #35557, #30256, #71337, #58569, #59306, #12888, #35924, #30622, #24213, #53644, #13621, #1954, #70976, #47225, #58941, #25313, #70254, #6877, #30988, #29888, #52900, #19290, #1234, #18565, #42300, #59670, #7981, #52529, #54007, #37025, #53273, #24584, #19659, #2319, #48330, #46861, #42672, #65684, #7246, #13984, #47588, #23853, #69883, #18196, #41209, #55134, #54758, #66430, #26817, #44551, #8725, #32115, #14365, #21528, #37398, #55508, #26428, #49831, #20780, #2695, #3068, #3440, #9101, #50202, #60399, #71709, #48701, #49454, #72473, #43801, #49074, #43414, #72087, #66815, #44178, #54387, #21154, #31738, #26052, #15118, #38148, #61151, #67192, #15490, #9482, #67562, #20026, #3820, #72849, #32497, #20401, #43038, #15859, #60026, #38526, #61528, #73222, #8344, #9851, #66058, #14740, #60775, #32876, #37780, #31359, #55881, #4196, #27185, #25683, #23390, #21894, #69419, #40006, #45657, #6050, #33621, #56627, #51320, #16226, #57369, #62264, #34368, #29057, #57746, #61897, #10220, #50571, #39264, #46031, #33249, #22263, #5679, #28677, #34000, #56995, #11334, #51691, #38, #23023, #56248, #44926 ) ),
 .UNSPECIFIED., .F., .F., .F. ) 
 B_SPLINE_SURFACE_WITH_KNOTS ( ( 2, 2 ),
 ( 3, 2, 2, 2, 2, 2, 2, 2, 2, 2, 2, 2, 2, 2, 2, 2, 2, 2, 2, 2, 2, 2, 2, 2, 2, 2, 2, 2, 2, 2, 2, 2, 2, 2, 2, 2, 2, 2, 2, 2, 2, 2, 2, 2, 2, 2, 2, 2, 2, 2, 2, 2, 2, 2, 2, 2, 2, 2, 2, 2, 2, 2, 2, 2, 2, 2, 2, 2, 2, 2, 2, 2, 2, 2, 2, 2, 2, 2, 2, 2, 2, 2, 2, 2, 2, 2, 2, 2, 2, 2, 2, 2, 2, 2, 2, 2, 2, 2, 2, 2, 2, 2, 2, 2, 2, 2, 2, 2, 2, 2, 2, 2, 2, 2, 2, 2, 2, 2, 2, 2, 2, 2, 2, 2, 2, 2, 2, 2, 2, 2, 2, 2, 2, 2, 2, 2, 2, 2, 2, 2, 2, 2, 2, 2, 2, 2, 2, 2, 2, 2, 2, 2, 2, 2, 2, 2, 2, 2, 2, 2, 2, 2, 2, 2, 2, 2, 2, 2, 2, 2, 2, 2, 2, 2, 2, 2, 3 ),
 ( 0.000000000000000000, 1.000000000000000000 ),
 ( 0.000000000000000000, 0.005681818181818181976, 0.01136363636363636395, 0.01704545454545454419, 0.02272727272727272790, 0.02840909090909090814, 0.03409090909090908839, 0.03977272727272727210, 0.04545454545454545581, 0.05113636363636363952, 0.05681818181818181629, 0.06250000000000000000, 0.06818181818181817677, 0.07386363636363636742, 0.07954545454545454419, 0.08522727272727272096, 0.09090909090909091161, 0.09659090909090908839, 0.1022727272727272790, 0.1079545454545454558, 0.1136363636363636326, 0.1193181818181818232, 0.1250000000000000000, 0.1306818181818181768, 0.1363636363636363535, 0.1420454545454545581, 0.1477272727272727348, 0.1534090909090909116, 0.1590909090909090884, 0.1647727272727272652, 0.1704545454545454419, 0.1761363636363636465, 0.1818181818181818232, 0.1875000000000000000, 0.1931818181818181768, 0.1988636363636363535, 0.2045454545454545581, 0.2102272727272727348, 0.2159090909090909116, 0.2215909090909090884, 0.2272727272727272652, 0.2329545454545454419, 0.2386363636363636465, 0.2443181818181818232, 0.2500000000000000000, 0.2556818181818181768, 0.2613636363636363535, 0.2670454545454545303, 0.2727272727272727071, 0.2784090909090908839, 0.2840909090909091161, 0.2897727272727272929, 0.2954545454545454697, 0.3011363636363636465, 0.3068181818181818232, 0.3125000000000000000, 0.3181818181818181768, 0.3238636363636363535, 0.3295454545454545303, 0.3352272727272727071, 0.3409090909090908839, 0.3465909090909091161, 0.3522727272727272929, 0.3579545454545454697, 0.3636363636363636465, 0.3693181818181818232, 0.3750000000000000000, 0.3806818181818181768, 0.3863636363636363535, 0.3920454545454545303, 0.3977272727272727071, 0.4034090909090908839, 0.4090909090909091161, 0.4147727272727272929, 0.4204545454545454697, 0.4261363636363636465, 0.4318181818181818232, 0.4375000000000000000, 0.4431818181818181768, 0.4488636363636363535, 0.4545454545454545303, 0.4602272727272727071, 0.4659090909090908839, 0.4715909090909091161, 0.4772727272727272929, 0.4829545454545454697, 0.4886363636363636465, 0.4943181818181818232, 0.5000000000000000000, 0.5056818181818182323, 0.5113636363636363535, 0.5170454545454545858, 0.5227272727272727071, 0.5284090909090909394, 0.5340909090909090606, 0.5397727272727272929, 0.5454545454545454142, 0.5511363636363636465, 0.5568181818181817677, 0.5625000000000000000, 0.5681818181818182323, 0.5738636363636363535, 0.5795454545454545858, 0.5852272727272727071, 0.5909090909090909394, 0.5965909090909090606, 0.6022727272727272929, 0.6079545454545454142, 0.6136363636363636465, 0.6193181818181817677, 0.6250000000000000000, 0.6306818181818182323, 0.6363636363636363535, 0.6420454545454545858, 0.6477272727272727071, 0.6534090909090909394, 0.6590909090909090606, 0.6647727272727272929, 0.6704545454545454142, 0.6761363636363636465, 0.6818181818181817677, 0.6875000000000000000, 0.6931818181818182323, 0.6988636363636363535, 0.7045454545454545858, 0.7102272727272727071, 0.7159090909090909394, 0.7215909090909090606, 0.7272727272727272929, 0.7329545454545454142, 0.7386363636363636465, 0.7443181818181817677, 0.7500000000000000000, 0.7556818181818182323, 0.7613636363636363535, 0.7670454545454545858, 0.7727272727272727071, 0.7784090909090909394, 0.7840909090909090606, 0.7897727272727272929, 0.7954545454545454142, 0.8011363636363636465, 0.8068181818181817677, 0.8125000000000000000, 0.8181818181818182323, 0.8238636363636363535, 0.8295454545454545858, 0.8352272727272727071, 0.8409090909090909394, 0.8465909090909090606, 0.8522727272727272929, 0.8579545454545454142, 0.8636363636363636465, 0.8693181818181817677, 0.8750000000000000000, 0.8806818181818182323, 0.8863636363636363535, 0.8920454545454545858, 0.8977272727272727071, 0.9034090909090909394, 0.9090909090909090606, 0.9147727272727272929, 0.9204545454545454142, 0.9261363636363636465, 0.9318181818181817677, 0.9375000000000000000, 0.9431818181818182323, 0.9488636363636363535, 0.9545454545454545858, 0.9602272727272727071, 0.9659090909090909394, 0.9715909090909090606, 0.9772727272727272929, 0.9829545454545454142, 0.9886363636363636465, 0.9943181818181817677, 1.000000000000000000 ),
 .UNSPECIFIED. ) 
 GEOMETRIC_REPRESENTATION_ITEM ( )  RATIONAL_B_SPLINE_SURFACE ( (
 ( 1.000000000000000000, 0.9238795325112867385, 1.000000000000000000, 0.9238795325112867385, 1.000000000000000000, 0.9238795325112867385, 1.000000000000000000, 0.9238795325112867385, 1.000000000000000000, 0.9238795325112867385, 1.000000000000000000, 0.9238795325112867385, 1.000000000000000000, 0.9238795325112867385, 1.000000000000000000, 0.9238795325112867385, 1.000000000000000000, 0.9238795325112867385, 1.000000000000000000, 0.9238795325112867385, 1.000000000000000000, 0.9238795325112867385, 1.000000000000000000, 0.9238795325112867385, 1.000000000000000000, 0.9238795325112867385, 1.000000000000000000, 0.9238795325112867385, 1.000000000000000000, 0.9238795325112867385, 1.000000000000000000, 0.9238795325112867385, 1.000000000000000000, 0.9238795325112867385, 1.000000000000000000, 0.9238795325112867385, 1.000000000000000000, 0.9238795325112867385, 1.000000000000000000, 0.9238795325112867385, 1.000000000000000000, 0.9238795325112867385, 1.000000000000000000, 0.9238795325112867385, 1.000000000000000000, 0.9238795325112867385, 1.000000000000000000, 0.9238795325112867385, 1.000000000000000000, 0.9238795325112867385, 1.000000000000000000, 0.9238795325112867385, 1.000000000000000000, 0.9238795325112867385, 1.000000000000000000, 0.9238795325112867385, 1.000000000000000000, 0.9238795325112867385, 1.000000000000000000, 0.9238795325112867385, 1.000000000000000000, 0.9238795325112867385, 1.000000000000000000, 0.9238795325112867385, 1.000000000000000000, 0.9238795325112867385, 1.000000000000000000, 0.9238795325112867385, 1.000000000000000000, 0.9238795325112867385, 1.000000000000000000, 0.9238795325112867385, 1.000000000000000000, 0.9238795325112867385, 1.000000000000000000, 0.9238795325112867385, 1.000000000000000000, 0.9238795325112867385, 1.000000000000000000, 0.9238795325112867385, 1.000000000000000000, 0.9238795325112867385, 1.000000000000000000, 0.9238795325112867385, 1.000000000000000000, 0.9238795325112867385, 1.000000000000000000, 0.9238795325112867385, 1.000000000000000000, 0.9238795325112867385, 1.000000000000000000, 0.9238795325112867385, 1.000000000000000000, 0.9238795325112867385, 1.000000000000000000, 0.9238795325112867385, 1.000000000000000000, 0.9238795325112867385, 1.000000000000000000, 0.9238795325112867385, 1.000000000000000000, 0.9238795325112867385, 1.000000000000000000, 0.9238795325112867385, 1.000000000000000000, 0.9238795325112867385, 1.000000000000000000, 0.9238795325112867385, 1.000000000000000000, 0.9238795325112867385, 1.000000000000000000, 0.9238795325112867385, 1.000000000000000000, 0.9238795325112867385, 1.000000000000000000, 0.9238795325112867385, 1.000000000000000000, 0.9238795325112867385, 1.000000000000000000, 0.9238795325112867385, 1.000000000000000000, 0.9238795325112867385, 1.000000000000000000, 0.9238795325112867385, 1.000000000000000000, 0.9238795325112867385, 1.000000000000000000, 0.9238795325112867385, 1.000000000000000000, 0.9238795325112867385, 1.000000000000000000, 0.9238795325112867385, 1.000000000000000000, 0.9238795325112867385, 1.000000000000000000, 0.9238795325112867385, 1.000000000000000000, 0.9238795325112867385, 1.000000000000000000, 0.9238795325112867385, 1.000000000000000000, 0.9238795325112867385, 1.000000000000000000, 0.9238795325112867385, 1.000000000000000000, 0.9238795325112867385, 1.000000000000000000, 0.9238795325112867385, 1.000000000000000000, 0.9238795325112867385, 1.000000000000000000, 0.9238795325112867385, 1.000000000000000000, 0.9238795325112867385, 1.000000000000000000, 0.9238795325112867385, 1.000000000000000000, 0.9238795325112867385, 1.000000000000000000, 0.9238795325112867385, 1.000000000000000000, 0.9238795325112867385, 1.000000000000000000, 0.9238795325112867385, 1.000000000000000000, 0.9238795325112867385, 1.000000000000000000, 0.9238795325112867385, 1.000000000000000000, 0.9238795325112867385, 1.000000000000000000, 0.9238795325112867385, 1.000000000000000000, 0.9238795325112867385, 1.000000000000000000, 0.9238795325112867385, 1.000000000000000000, 0.9238795325112867385, 1.000000000000000000, 0.9238795325112867385, 1.000000000000000000, 0.9238795325112867385, 1.000000000000000000, 0.9238795325112867385, 1.000000000000000000, 0.9238795325112867385, 1.000000000000000000, 0.9238795325112867385, 1.000000000000000000, 0.9238795325112867385, 1.000000000000000000, 0.9238795325112867385, 1.000000000000000000, 0.9238795325112867385, 1.000000000000000000, 0.9238795325112867385, 1.000000000000000000, 0.9238795325112867385, 1.000000000000000000, 0.9238795325112867385, 1.000000000000000000, 0.9238795325112867385, 1.000000000000000000, 0.9238795325112867385, 1.000000000000000000, 0.9238795325112867385, 1.000000000000000000, 0.9238795325112867385, 1.000000000000000000, 0.9238795325112867385, 1.000000000000000000, 0.9238795325112867385, 1.000000000000000000, 0.9238795325112867385, 1.000000000000000000, 0.9238795325112867385, 1.000000000000000000, 0.9238795325112867385, 1.000000000000000000, 0.9238795325112867385, 1.000000000000000000, 0.9238795325112867385, 1.000000000000000000, 0.9238795325112867385, 1.000000000000000000, 0.9238795325112867385, 1.000000000000000000, 0.9238795325112867385, 1.000000000000000000, 0.9238795325112867385, 1.000000000000000000, 0.9238795325112867385, 1.000000000000000000, 0.9238795325112867385, 1.000000000000000000, 0.9238795325112867385, 1.000000000000000000, 0.9238795325112867385, 1.000000000000000000, 0.9238795325112867385, 1.000000000000000000, 0.9238795325112867385, 1.000000000000000000, 0.9238795325112867385, 1.000000000000000000, 0.9238795325112867385, 1.000000000000000000, 0.9238795325112867385, 1.000000000000000000, 0.9238795325112867385, 1.000000000000000000, 0.9238795325112867385, 1.000000000000000000, 0.9238795325112867385, 1.000000000000000000, 0.9238795325112867385, 1.000000000000000000, 0.9238795325112867385, 1.000000000000000000, 0.9238795325112867385, 1.000000000000000000, 0.9238795325112867385, 1.000000000000000000, 0.9238795325112867385, 1.000000000000000000, 0.9238795325112867385, 1.000000000000000000, 0.9238795325112867385, 1.000000000000000000, 0.9238795325112867385, 1.000000000000000000, 0.9238795325112867385, 1.000000000000000000, 0.9238795325112867385, 1.000000000000000000, 0.9238795325112867385, 1.000000000000000000, 0.9238795325112867385, 1.000000000000000000, 0.9238795325112867385, 1.000000000000000000, 0.9238795325112867385, 1.000000000000000000, 0.9238795325112867385, 1.000000000000000000, 0.9238795325112867385, 1.000000000000000000, 0.9238795325112867385, 1.000000000000000000, 0.9238795325112867385, 1.000000000000000000, 0.9238795325112867385, 1.000000000000000000, 0.9238795325112867385, 1.000000000000000000, 0.9238795325112867385, 1.000000000000000000, 0.9238795325112867385, 1.000000000000000000, 0.9238795325112867385, 1.000000000000000000, 0.9238795325112867385, 1.000000000000000000, 0.9238795325112867385, 1.000000000000000000, 0.9238795325112867385, 1.000000000000000000, 0.9238795325112867385, 1.000000000000000000, 0.9238795325112867385, 1.000000000000000000, 0.9238795325112867385, 1.000000000000000000, 0.9238795325112867385, 1.000000000000000000, 0.9238795325112867385, 1.000000000000000000, 0.9238795325112867385, 1.000000000000000000, 0.9238795325112867385, 1.000000000000000000, 0.9238795325112867385, 1.000000000000000000, 0.9238795325112867385, 1.000000000000000000, 0.9238795325112867385, 1.000000000000000000, 0.9238795325112867385, 1.000000000000000000, 0.9238795325112867385, 1.000000000000000000, 0.9238795325112867385, 1.000000000000000000, 0.9238795325112867385, 1.000000000000000000, 0.9238795325112867385, 1.000000000000000000, 0.9238795325112867385, 1.000000000000000000, 0.9238795325112867385, 1.000000000000000000, 0.9238795325112867385, 1.000000000000000000, 0.9238795325112867385, 1.000000000000000000, 0.9238795325112867385, 1.000000000000000000, 0.9238795325112867385, 1.000000000000000000, 0.9238795325112867385, 1.000000000000000000, 0.9238795325112867385, 1.000000000000000000),
 ( 1.000000000000000000, 0.9238795325112867385, 1.000000000000000000, 0.9238795325112867385, 1.000000000000000000, 0.9238795325112867385, 1.000000000000000000, 0.9238795325112867385, 1.000000000000000000, 0.9238795325112867385, 1.000000000000000000, 0.9238795325112867385, 1.000000000000000000, 0.9238795325112867385, 1.000000000000000000, 0.9238795325112867385, 1.000000000000000000, 0.9238795325112867385, 1.000000000000000000, 0.9238795325112867385, 1.000000000000000000, 0.9238795325112867385, 1.000000000000000000, 0.9238795325112867385, 1.000000000000000000, 0.9238795325112867385, 1.000000000000000000, 0.9238795325112867385, 1.000000000000000000, 0.9238795325112867385, 1.000000000000000000, 0.9238795325112867385, 1.000000000000000000, 0.9238795325112867385, 1.000000000000000000, 0.9238795325112867385, 1.000000000000000000, 0.9238795325112867385, 1.000000000000000000, 0.9238795325112867385, 1.000000000000000000, 0.9238795325112867385, 1.000000000000000000, 0.9238795325112867385, 1.000000000000000000, 0.9238795325112867385, 1.000000000000000000, 0.9238795325112867385, 1.000000000000000000, 0.9238795325112867385, 1.000000000000000000, 0.9238795325112867385, 1.000000000000000000, 0.9238795325112867385, 1.000000000000000000, 0.9238795325112867385, 1.000000000000000000, 0.9238795325112867385, 1.000000000000000000, 0.9238795325112867385, 1.000000000000000000, 0.9238795325112867385, 1.000000000000000000, 0.9238795325112867385, 1.000000000000000000, 0.9238795325112867385, 1.000000000000000000, 0.9238795325112867385, 1.000000000000000000, 0.9238795325112867385, 1.000000000000000000, 0.9238795325112867385, 1.000000000000000000, 0.9238795325112867385, 1.000000000000000000, 0.9238795325112867385, 1.000000000000000000, 0.9238795325112867385, 1.000000000000000000, 0.9238795325112867385, 1.000000000000000000, 0.9238795325112867385, 1.000000000000000000, 0.9238795325112867385, 1.000000000000000000, 0.9238795325112867385, 1.000000000000000000, 0.9238795325112867385, 1.000000000000000000, 0.9238795325112867385, 1.000000000000000000, 0.9238795325112867385, 1.000000000000000000, 0.9238795325112867385, 1.000000000000000000, 0.9238795325112867385, 1.000000000000000000, 0.9238795325112867385, 1.000000000000000000, 0.9238795325112867385, 1.000000000000000000, 0.9238795325112867385, 1.000000000000000000, 0.9238795325112867385, 1.000000000000000000, 0.9238795325112867385, 1.000000000000000000, 0.9238795325112867385, 1.000000000000000000, 0.9238795325112867385, 1.000000000000000000, 0.9238795325112867385, 1.000000000000000000, 0.9238795325112867385, 1.000000000000000000, 0.9238795325112867385, 1.000000000000000000, 0.9238795325112867385, 1.000000000000000000, 0.9238795325112867385, 1.000000000000000000, 0.9238795325112867385, 1.000000000000000000, 0.9238795325112867385, 1.000000000000000000, 0.9238795325112867385, 1.000000000000000000, 0.9238795325112867385, 1.000000000000000000, 0.9238795325112867385, 1.000000000000000000, 0.9238795325112867385, 1.000000000000000000, 0.9238795325112867385, 1.000000000000000000, 0.9238795325112867385, 1.000000000000000000, 0.9238795325112867385, 1.000000000000000000, 0.9238795325112867385, 1.000000000000000000, 0.9238795325112867385, 1.000000000000000000, 0.9238795325112867385, 1.000000000000000000, 0.9238795325112867385, 1.000000000000000000, 0.9238795325112867385, 1.000000000000000000, 0.9238795325112867385, 1.000000000000000000, 0.9238795325112867385, 1.000000000000000000, 0.9238795325112867385, 1.000000000000000000, 0.9238795325112867385, 1.000000000000000000, 0.9238795325112867385, 1.000000000000000000, 0.9238795325112867385, 1.000000000000000000, 0.9238795325112867385, 1.000000000000000000, 0.9238795325112867385, 1.000000000000000000, 0.9238795325112867385, 1.000000000000000000, 0.9238795325112867385, 1.000000000000000000, 0.9238795325112867385, 1.000000000000000000, 0.9238795325112867385, 1.000000000000000000, 0.9238795325112867385, 1.000000000000000000, 0.9238795325112867385, 1.000000000000000000, 0.9238795325112867385, 1.000000000000000000, 0.9238795325112867385, 1.000000000000000000, 0.9238795325112867385, 1.000000000000000000, 0.9238795325112867385, 1.000000000000000000, 0.9238795325112867385, 1.000000000000000000, 0.9238795325112867385, 1.000000000000000000, 0.9238795325112867385, 1.000000000000000000, 0.9238795325112867385, 1.000000000000000000, 0.9238795325112867385, 1.000000000000000000, 0.9238795325112867385, 1.000000000000000000, 0.9238795325112867385, 1.000000000000000000, 0.9238795325112867385, 1.000000000000000000, 0.9238795325112867385, 1.000000000000000000, 0.9238795325112867385, 1.000000000000000000, 0.9238795325112867385, 1.000000000000000000, 0.9238795325112867385, 1.000000000000000000, 0.9238795325112867385, 1.000000000000000000, 0.9238795325112867385, 1.000000000000000000, 0.9238795325112867385, 1.000000000000000000, 0.9238795325112867385, 1.000000000000000000, 0.9238795325112867385, 1.000000000000000000, 0.9238795325112867385, 1.000000000000000000, 0.9238795325112867385, 1.000000000000000000, 0.9238795325112867385, 1.000000000000000000, 0.9238795325112867385, 1.000000000000000000, 0.9238795325112867385, 1.000000000000000000, 0.9238795325112867385, 1.000000000000000000, 0.9238795325112867385, 1.000000000000000000, 0.9238795325112867385, 1.000000000000000000, 0.9238795325112867385, 1.000000000000000000, 0.9238795325112867385, 1.000000000000000000, 0.9238795325112867385, 1.000000000000000000, 0.9238795325112867385, 1.000000000000000000, 0.9238795325112867385, 1.000000000000000000, 0.9238795325112867385, 1.000000000000000000, 0.9238795325112867385, 1.000000000000000000, 0.9238795325112867385, 1.000000000000000000, 0.9238795325112867385, 1.000000000000000000, 0.9238795325112867385, 1.000000000000000000, 0.9238795325112867385, 1.000000000000000000, 0.9238795325112867385, 1.000000000000000000, 0.9238795325112867385, 1.000000000000000000, 0.9238795325112867385, 1.000000000000000000, 0.9238795325112867385, 1.000000000000000000, 0.9238795325112867385, 1.000000000000000000, 0.9238795325112867385, 1.000000000000000000, 0.9238795325112867385, 1.000000000000000000, 0.9238795325112867385, 1.000000000000000000, 0.9238795325112867385, 1.000000000000000000, 0.9238795325112867385, 1.000000000000000000, 0.9238795325112867385, 1.000000000000000000, 0.9238795325112867385, 1.000000000000000000, 0.9238795325112867385, 1.000000000000000000, 0.9238795325112867385, 1.000000000000000000, 0.9238795325112867385, 1.000000000000000000, 0.9238795325112867385, 1.000000000000000000, 0.9238795325112867385, 1.000000000000000000, 0.9238795325112867385, 1.000000000000000000, 0.9238795325112867385, 1.000000000000000000, 0.9238795325112867385, 1.000000000000000000, 0.9238795325112867385, 1.000000000000000000, 0.9238795325112867385, 1.000000000000000000, 0.9238795325112867385, 1.000000000000000000, 0.9238795325112867385, 1.000000000000000000, 0.9238795325112867385, 1.000000000000000000, 0.9238795325112867385, 1.000000000000000000, 0.9238795325112867385, 1.000000000000000000, 0.9238795325112867385, 1.000000000000000000, 0.9238795325112867385, 1.000000000000000000, 0.9238795325112867385, 1.000000000000000000, 0.9238795325112867385, 1.000000000000000000, 0.9238795325112867385, 1.000000000000000000, 0.9238795325112867385, 1.000000000000000000, 0.9238795325112867385, 1.000000000000000000, 0.9238795325112867385, 1.000000000000000000, 0.9238795325112867385, 1.000000000000000000, 0.9238795325112867385, 1.000000000000000000, 0.9238795325112867385, 1.000000000000000000, 0.9238795325112867385, 1.000000000000000000, 0.9238795325112867385, 1.000000000000000000, 0.9238795325112867385, 1.000000000000000000, 0.9238795325112867385, 1.000000000000000000, 0.9238795325112867385, 1.000000000000000000, 0.9238795325112867385, 1.000000000000000000, 0.9238795325112867385, 1.000000000000000000, 0.9238795325112867385, 1.000000000000000000, 0.9238795325112867385, 1.000000000000000000, 0.9238795325112867385, 1.000000000000000000) ) ) 
 REPRESENTATION_ITEM ( '' )  SURFACE ( )  );
#13147=VERTEX_POINT ( 'NONE', #20046 ) ;
#13149=ADVANCED_FACE ( 'NONE', ( #47610 ), #13274, .T. ) ;
#13152=CARTESIAN_POINT ( 'NONE',  ( -1.656854249492383691, 11.68750000000000000, 4.000000000000000888 ) ) ;
#13154=CARTESIAN_POINT ( 'NONE',  ( -4.541265875000002339, 14.81249999863440792, -5.561446717895856393E-16 ) ) ;
#13158=ORIENTED_EDGE ( 'NONE', *, *, #44244, .T. ) ;
#13168=EDGE_CURVE ( 'NONE', #59211, #56591, #41470, .T. ) ;
#13237=CARTESIAN_POINT ( 'NONE',  ( 3.211159895383561835, 18.56249999863440436, -3.211159895383561835 ) ) ;
#13248=CARTESIAN_POINT ( 'NONE',  ( 1.656854249492381914, 15.56249999726881406, 4.000000000000000888 ) ) ;
#13255=CARTESIAN_POINT ( 'NONE',  ( 4.541265875000002339, 13.37499999863440792, -1.881053915767121554 ) ) ;
#13274=CYLINDRICAL_SURFACE ( 'NONE', #57223, 4.000000000000001776 ) ;
#13280=CARTESIAN_POINT ( 'NONE',  ( 3.211159895383561835, 2.437499998634407028, -3.211159895383561835 ) ) ;
#13292=DIRECTION ( 'NONE',  ( -0.000000000000000000, -1.000000000000000000, -0.000000000000000000 ) ) ;
#13299=CARTESIAN_POINT ( 'NONE',  ( -4.541265875000003227, 14.99999999863440969, 1.881053915767121110 ) ) ;
#13303=VERTEX_POINT ( 'NONE', #21552 ) ;
#13322=CARTESIAN_POINT ( 'NONE',  ( -8.342170076843785083E-16, 4.187499998634407028, 4.541265875000002339 ) ) ;
#13333=CARTESIAN_POINT ( 'NONE',  ( 1.656854249492381248, 3.937499997268813168, -4.000000000000001776 ) ) ;
#13339=CARTESIAN_POINT ( 'NONE',  ( -4.541265875000002339, 2.749999998634406584, -1.881053915767121998 ) ) ;
#13346=CARTESIAN_POINT ( 'NONE',  ( 0.000000000000000000, 0.000000000000000000, -4.000000000000001776 ) ) ;
#13360=CARTESIAN_POINT ( 'NONE',  ( 0.000000000000000000, 0.000000000000000000, 0.000000000000000000 ) ) ;
#13384=CARTESIAN_POINT ( 'NONE',  ( 3.211159895383561835, 4.562499998634407028, -3.211159895383561835 ) ) ;
#13421=CARTESIAN_POINT ( 'NONE',  ( 0.5061642150818620456, 21.99999999999999289, 4.376614538100004559 ) ) ;
#13422=FACE_OUTER_BOUND ( 'NONE', #39076, .T. ) ;
#13429=CARTESIAN_POINT ( 'NONE',  ( 4.541265875000001451, 13.37499999863440969, 1.881053915767124440 ) ) ;
#13439=ORIENTED_EDGE ( 'NONE', *, *, #61208, .F. ) ;
#13441=CARTESIAN_POINT ( 'NONE',  ( 2.828427124746191623, 20.12500000000000000, -2.828427124746191623 ) ) ;
#13463=CARTESIAN_POINT ( 'NONE',  ( 2.828427124746190291, 18.87500000000000000, 2.828427124746192067 ) ) ;
#13474=CARTESIAN_POINT ( 'NONE',  ( 4.541265875000002339, 16.31249999863440436, 0.000000000000000000 ) ) ;
#13489=CARTESIAN_POINT ( 'NONE',  ( -1.656854249492383468, 13.43749999726881406, 4.000000000000000888 ) ) ;
#13507=VERTEX_POINT ( 'NONE', #36923 ) ;
#13517=CARTESIAN_POINT ( 'NONE',  ( 1.656854249492381914, 13.81250000000000000, 4.000000000000000888 ) ) ;
#13518=CARTESIAN_POINT ( 'NONE',  ( -1.881053915767121776, 17.62499999863440436, -4.541265875000002339 ) ) ;
#13526=DIRECTION ( 'NONE',  ( 0.000000000000000000, 0.000000000000000000, -1.000000000000000000 ) ) ;
#13555=CARTESIAN_POINT ( 'NONE',  ( -2.828427124746190735, 12.37500000000000000, -2.828427124746191623 ) ) ;
#13566=CARTESIAN_POINT ( 'NONE',  ( -2.828427124746192067, 8.374999997268814056, 2.828427124746190735 ) ) ;
#13602=CARTESIAN_POINT ( 'NONE',  ( 1.881053915767121998, 18.62499999863441147, -4.541265875000002339 ) ) ;
#13606=CARTESIAN_POINT ( 'NONE',  ( 1.881053915767121776, 0.6249999986344068059, -4.541265875000002339 ) ) ;
#13611=CARTESIAN_POINT ( 'NONE',  ( -7.347880794884122694E-16, 12.49999999726881406, 4.000000000000001776 ) ) ;
#13612=CARTESIAN_POINT ( 'NONE',  ( -4.541265875000002339, 3.749999998634407028, -1.881053915767121998 ) ) ;
#13621=CARTESIAN_POINT ( 'NONE',  ( 3.211159895383560947, 14.18749999863440792, 3.211159895383562723 ) ) ;
#13625=EDGE_CURVE ( 'NONE', #39246, #55774, #65899, .T. ) ;
#13643=DIRECTION ( 'NONE',  ( -0.000000000000000000, -1.000000000000000000, -0.000000000000000000 ) ) ;
#13649=CARTESIAN_POINT ( 'NONE',  ( 3.211159895383561835, 3.437499998634407028, -3.211159895383561835 ) ) ;
#13650=CARTESIAN_POINT ( 'NONE',  ( -4.000000000000002665, 14.31249999726881406, 1.656854249492380582 ) ) ;
#13665=CARTESIAN_POINT ( 'NONE',  ( 4.541265875000002339, 17.43749999863440792, 0.000000000000000000 ) ) ;
#13687=CARTESIAN_POINT ( 'NONE',  ( -4.541265875000003227, 4.999999998634407028, 1.881053915767121110 ) ) ;
#13696=CARTESIAN_POINT ( 'NONE',  ( 4.000000000000001776, 9.000000000000001776, 0.000000000000000000 ) ) ;
#13697=CARTESIAN_POINT ( 'NONE',  ( 2.828427124746191623, 2.874999997268813168, -2.828427124746191623 ) ) ;
#13703=CARTESIAN_POINT ( 'NONE',  ( -4.541265875000003227, 1.874999998634406806, 1.881053915767121110 ) ) ;
#13725=CARTESIAN_POINT ( 'NONE',  ( 0.000000000000000000, 0.000000000000000000, -4.000000000000001776 ) ) ;
#13727=DIRECTION ( 'NONE',  ( -0.000000000000000000, -1.000000000000000000, -0.000000000000000000 ) ) ;
#13747=CARTESIAN_POINT ( 'NONE',  ( -4.541265875000002339, 2.874999998634407028, -1.881053915767121998 ) ) ;
#13751=EDGE_LOOP ( 'NONE', ( #53902, #11558, #4945, #29317 ) ) ;
#13776=CARTESIAN_POINT ( 'NONE',  ( 4.000000000000001776, 20.74999999726881583, 0.000000000000000000 ) ) ;
#13792=CARTESIAN_POINT ( 'NONE',  ( 3.211159895383561835, 12.56249999863440792, -3.211159895383561835 ) ) ;
#13824=LINE ( 'NONE', #36129, #25358 ) ;
#13833=CARTESIAN_POINT ( 'NONE',  ( -4.541265875000002339, 12.74999999863440969, -1.881053915767121998 ) ) ;
#13835=ADVANCED_BREP_SHAPE_REPRESENTATION ( '', ( #41611, #57354 ), #58583 ) ;
#13857=ADVANCED_FACE ( 'NONE', ( #11920 ), #28523, .T. ) ;
#13884=CARTESIAN_POINT ( 'NONE',  ( -4.000000000000001776, 15.43749999999999822, -1.656854249492381470 ) ) ;
#13886=CARTESIAN_POINT ( 'NONE',  ( 1.881053915767121998, 14.49999999863440969, -4.541265875000002339 ) ) ;
#13894=CARTESIAN_POINT ( 'NONE',  ( -7.347880794884122694E-16, 13.49999999726881406, 4.000000000000001776 ) ) ;
#13921=CARTESIAN_POINT ( 'NONE',  ( -7.347880794884122694E-16, 0.7500000000000002220, 4.000000000000001776 ) ) ;
#13930=CARTESIAN_POINT ( 'NONE',  ( -4.000000000000001776, 14.50000000000000000, -4.898587196589415787E-16 ) ) ;
#13963=CARTESIAN_POINT ( 'NONE',  ( 2.780723358947928197E-16, 16.68749999863440436, -4.541265875000002339 ) ) ;
#13967=CARTESIAN_POINT ( 'NONE',  ( -8.342170076843785083E-16, 3.187499998634407028, 4.541265875000002339 ) ) ;
#13974=CARTESIAN_POINT ( 'NONE',  ( -4.000000000000002665, 2.562500000000000444, 1.656854249492380804 ) ) ;
#13975=CARTESIAN_POINT ( 'NONE',  ( -2.828427124746192067, 17.37499999726881583, 2.828427124746190735 ) ) ;
#13976=CARTESIAN_POINT ( 'NONE',  ( 3.211159895383561835, 2.437499998634407028, -3.211159895383561835 ) ) ;
#13984=CARTESIAN_POINT ( 'NONE',  ( -1.881053915767124440, 15.99999999863440614, 4.541265875000001451 ) ) ;
#13987=ORIENTED_EDGE ( 'NONE', *, *, #68470, .T. ) ;
#13990=CARTESIAN_POINT ( 'NONE',  ( 0.000000000000000000, 0.000000000000000000, -4.000000000000001776 ) ) ;
#14003=( BOUNDED_CURVE ( )  B_SPLINE_CURVE ( 2, ( #57154, #34902, #29221, #5470, #62424, #6216, #51480, #6583, #52235, #45819, #40535, #46190, #56783, #567, #68830, #17142, #29589, #40167, #69583, #63172, #34531, #12229, #52602, #63918, #57537, #57908, #5846, #51858, #23550, #15372, #10749, #940, #17896, #202, #63541, #23180, #35266, #17519, #58281, #23922, #31054, #65014, #25012, #58639, #64291, #19733, #69956, #8418, #42374, #19360, #6947, #48403, #48031, #29959, #65389, #14060, #36360, #59013, #1670, #71040, #13322, #18639, #42005, #7686, #70324, #30694, #47300, #12599, #30325, #52972, #31433, #53712, #60100, #13687, #54460, #2389, #36728, #24650, #59375, #2025, #1305, #18266, #41281, #47660, #35625, #70682, #53343, #41648, #46931, #64658, #24287, #59741, #12956, #35996, #8049, #7320, #18999, #54081, #65757, #37096, #25386, #71408, #42742, #2767, #66886, #3894, #3143, #26887, #15193, #10293, #38221, #31812, #67265, #26503, #32188, #8799, #55208, #44253, #3513, #9556, #15560, #66131, #37469, #9170, #56317, #33319, #60850, #44622, #61227, #32949, #54833, #73294, #20853, #43871, #49904, #60470, #43112, #21596, #48775, #61965, #21227, #72918, #32570, #67637, #55579, #38599, #49527, #61598, #25754, #72548, #9917, #55956, #4266, #72158, #27256, #50272, #49146, #15932, #26126, #14436, #38962, #71782, #20468, #43488, #20098, #66500, #14811, #37852, #5747, #6124, #63080, #51388, #11405, #56697, #5378, #69118, #74027, #28747, #27633, #17802, #45726, #28010, #50641, #40076, #39335, #22330, #22709, #39700, #34069, #62332, #23460, #46472, #10659, #33692, #16295, #29129, #5012, #23088, #57441, #74400, #68740, #63823, #17053, #51019, #46100, #28379, #11038, #45357, #4636, #34442, #73659, #21968, #57065, #68371, #44995, #16669, #57817, #62700, #17424, #40448, #51763, #63447, #40817, #110, #11772, #67999, #34810, #52145, #69492, #479, #12139, #35176, #7595, #65665, #7965, #24194, #24924, #48313, #2297, #71320, #53987, #29869, #12505, #25295, #30601, #58552, #12868, #35537, #19641, #7231, #41917, #47206, #30235, #47571, #29502, #42654, #70238, #6495, #6857, #41192, #13963, #52513, #70955, #18547, #58191, #19273, #35905, #53623, #36271, #23835, #42283, #52883, #1215, #850, #41553, #36639, #18177, #64202, #64571, #46841, #69864, #58923, #1935, #53253, #64928, #47938, #1581, #24565, #70594, #65297, #13237, #13602, #18911, #59647, #59287, #30968, #72063, #21136, #43780, #55116, #4179, #54367, #9830, #60009, #73205, #32477, #9461, #48683, #38507, #15097, #71689, #55486, #27166, #26407, #49055, #66411, #38130, #3420, #3800, #26799, #66793, #60378, #20762, #37377, #2678, #20381, #43018, #21510, #61131, #50183, #49813, #44532, #67174, #72829, #14721, #32096, #49435, #66040, #44160, #8327, #31337, #31720, #15470, #25665, #67543, #72454, #43397 ),
 .UNSPECIFIED., .F., .F. ) 
 B_SPLINE_CURVE_WITH_KNOTS ( ( 3, 2, 2, 2, 2, 2, 2, 2, 2, 2, 2, 2, 2, 2, 2, 2, 2, 2, 2, 2, 2, 2, 2, 2, 2, 2, 2, 2, 2, 2, 2, 2, 2, 2, 2, 2, 2, 2, 2, 2, 2, 2, 2, 2, 2, 2, 2, 2, 2, 2, 2, 2, 2, 2, 2, 2, 2, 2, 2, 2, 2, 2, 2, 2, 2, 2, 2, 2, 2, 2, 2, 2, 2, 2, 2, 2, 2, 2, 2, 2, 2, 2, 2, 2, 2, 2, 2, 2, 2, 2, 2, 2, 2, 2, 2, 2, 2, 2, 2, 2, 2, 2, 2, 2, 2, 2, 2, 2, 2, 2, 2, 2, 2, 2, 2, 2, 2, 2, 2, 2, 2, 2, 2, 2, 2, 2, 2, 2, 2, 2, 2, 2, 2, 2, 2, 2, 2, 2, 2, 2, 2, 2, 2, 2, 2, 2, 2, 2, 2, 2, 2, 2, 2, 2, 2, 2, 2, 2, 2, 2, 2, 2, 2, 2, 2, 2, 2, 2, 2, 2, 2, 2, 2, 3 ),
 ( 0.000000000000000000, 0.005681818181818181976, 0.01136363636363636395, 0.01704545454545454419, 0.02272727272727272790, 0.02840909090909090814, 0.03409090909090908839, 0.03977272727272727210, 0.04545454545454545581, 0.05113636363636363952, 0.05681818181818181629, 0.06250000000000000000, 0.06818181818181817677, 0.07386363636363636742, 0.07954545454545454419, 0.08522727272727272096, 0.09090909090909091161, 0.09659090909090908839, 0.1022727272727272790, 0.1079545454545454558, 0.1136363636363636326, 0.1193181818181818232, 0.1250000000000000000, 0.1306818181818181768, 0.1363636363636363535, 0.1420454545454545581, 0.1477272727272727348, 0.1534090909090909116, 0.1590909090909090884, 0.1647727272727272652, 0.1704545454545454419, 0.1761363636363636465, 0.1818181818181818232, 0.1875000000000000000, 0.1931818181818181768, 0.1988636363636363535, 0.2045454545454545581, 0.2102272727272727348, 0.2159090909090909116, 0.2215909090909090884, 0.2272727272727272652, 0.2329545454545454419, 0.2386363636363636465, 0.2443181818181818232, 0.2500000000000000000, 0.2556818181818181768, 0.2613636363636363535, 0.2670454545454545303, 0.2727272727272727071, 0.2784090909090908839, 0.2840909090909091161, 0.2897727272727272929, 0.2954545454545454697, 0.3011363636363636465, 0.3068181818181818232, 0.3125000000000000000, 0.3181818181818181768, 0.3238636363636363535, 0.3295454545454545303, 0.3352272727272727071, 0.3409090909090908839, 0.3465909090909091161, 0.3522727272727272929, 0.3579545454545454697, 0.3636363636363636465, 0.3693181818181818232, 0.3750000000000000000, 0.3806818181818181768, 0.3863636363636363535, 0.3920454545454545303, 0.3977272727272727071, 0.4034090909090908839, 0.4090909090909091161, 0.4147727272727272929, 0.4204545454545454697, 0.4261363636363636465, 0.4318181818181818232, 0.4375000000000000000, 0.4431818181818181768, 0.4488636363636363535, 0.4545454545454545303, 0.4602272727272727071, 0.4659090909090908839, 0.4715909090909091161, 0.4772727272727272929, 0.4829545454545454697, 0.4886363636363636465, 0.4943181818181818232, 0.5000000000000000000, 0.5056818181818182323, 0.5113636363636363535, 0.5170454545454545858, 0.5227272727272727071, 0.5284090909090909394, 0.5340909090909090606, 0.5397727272727272929, 0.5454545454545454142, 0.5511363636363636465, 0.5568181818181817677, 0.5625000000000001110, 0.5681818181818182323, 0.5738636363636363535, 0.5795454545454545858, 0.5852272727272727071, 0.5909090909090909394, 0.5965909090909090606, 0.6022727272727272929, 0.6079545454545454142, 0.6136363636363636465, 0.6193181818181817677, 0.6250000000000000000, 0.6306818181818182323, 0.6363636363636363535, 0.6420454545454545858, 0.6477272727272727071, 0.6534090909090909394, 0.6590909090909090606, 0.6647727272727272929, 0.6704545454545454142, 0.6761363636363636465, 0.6818181818181817677, 0.6874999999999998890, 0.6931818181818182323, 0.6988636363636363535, 0.7045454545454545858, 0.7102272727272727071, 0.7159090909090909394, 0.7215909090909090606, 0.7272727272727272929, 0.7329545454545454142, 0.7386363636363636465, 0.7443181818181817677, 0.7500000000000000000, 0.7556818181818182323, 0.7613636363636363535, 0.7670454545454545858, 0.7727272727272727071, 0.7784090909090909394, 0.7840909090909090606, 0.7897727272727272929, 0.7954545454545454142, 0.8011363636363636465, 0.8068181818181817677, 0.8125000000000001110, 0.8181818181818182323, 0.8238636363636363535, 0.8295454545454545858, 0.8352272727272727071, 0.8409090909090909394, 0.8465909090909090606, 0.8522727272727272929, 0.8579545454545454142, 0.8636363636363636465, 0.8693181818181817677, 0.8750000000000000000, 0.8806818181818182323, 0.8863636363636363535, 0.8920454545454545858, 0.8977272727272727071, 0.9034090909090909394, 0.9090909090909090606, 0.9147727272727272929, 0.9204545454545454142, 0.9261363636363636465, 0.9318181818181817677, 0.9374999999999998890, 0.9431818181818182323, 0.9488636363636363535, 0.9545454545454545858, 0.9602272727272727071, 0.9659090909090909394, 0.9715909090909090606, 0.9772727272727272929, 0.9801136364233462572 ),
 .UNSPECIFIED. ) 
 CURVE ( )  GEOMETRIC_REPRESENTATION_ITEM ( )  RATIONAL_B_SPLINE_CURVE ( ( 1.000000000000000000, 0.9238795325112867385, 1.000000000000000000, 0.9238795325112867385, 1.000000000000000000, 0.9238795325112867385, 1.000000000000000000, 0.9238795325112867385, 1.000000000000000000, 0.9238795325112867385, 1.000000000000000000, 0.9238795325112867385, 1.000000000000000000, 0.9238795325112867385, 1.000000000000000000, 0.9238795325112867385, 1.000000000000000000, 0.9238795325112867385, 1.000000000000000000, 0.9238795325112867385, 1.000000000000000000, 0.9238795325112867385, 1.000000000000000000, 0.9238795325112867385, 1.000000000000000000, 0.9238795325112867385, 1.000000000000000000, 0.9238795325112867385, 1.000000000000000000, 0.9238795325112867385, 1.000000000000000000, 0.9238795325112867385, 1.000000000000000000, 0.9238795325112867385, 1.000000000000000000, 0.9238795325112867385, 1.000000000000000000, 0.9238795325112867385, 1.000000000000000000, 0.9238795325112867385, 1.000000000000000000, 0.9238795325112867385, 1.000000000000000000, 0.9238795325112867385, 1.000000000000000000, 0.9238795325112867385, 1.000000000000000000, 0.9238795325112867385, 1.000000000000000000, 0.9238795325112867385, 1.000000000000000000, 0.9238795325112867385, 1.000000000000000000, 0.9238795325112867385, 1.000000000000000000, 0.9238795325112867385, 1.000000000000000000, 0.9238795325112867385, 1.000000000000000000, 0.9238795325112867385, 1.000000000000000000, 0.9238795325112867385, 1.000000000000000000, 0.9238795325112867385, 1.000000000000000000, 0.9238795325112867385, 1.000000000000000000, 0.9238795325112867385, 1.000000000000000000, 0.9238795325112867385, 1.000000000000000000, 0.9238795325112867385, 1.000000000000000000, 0.9238795325112867385, 1.000000000000000000, 0.9238795325112867385, 1.000000000000000000, 0.9238795325112867385, 1.000000000000000000, 0.9238795325112867385, 1.000000000000000000, 0.9238795325112867385, 1.000000000000000000, 0.9238795325112867385, 1.000000000000000000, 0.9238795325112867385, 1.000000000000000000, 0.9238795325112867385, 1.000000000000000000, 0.9238795325112867385, 1.000000000000000000, 0.9238795325112867385, 1.000000000000000000, 0.9238795325112867385, 1.000000000000000000, 0.9238795325112867385, 1.000000000000000000, 0.9238795325112867385, 1.000000000000000000, 0.9238795325112867385, 1.000000000000000000, 0.9238795325112867385, 1.000000000000000000, 0.9238795325112867385, 1.000000000000000000, 0.9238795325112867385, 1.000000000000000000, 0.9238795325112867385, 1.000000000000000000, 0.9238795325112867385, 1.000000000000000000, 0.9238795325112867385, 1.000000000000000000, 0.9238795325112867385, 1.000000000000000000, 0.9238795325112867385, 1.000000000000000000, 0.9238795325112867385, 1.000000000000000000, 0.9238795325112867385, 1.000000000000000000, 0.9238795325112867385, 1.000000000000000000, 0.9238795325112867385, 1.000000000000000000, 0.9238795325112867385, 1.000000000000000000, 0.9238795325112867385, 1.000000000000000000, 0.9238795325112867385, 1.000000000000000000, 0.9238795325112867385, 1.000000000000000000, 0.9238795325112867385, 1.000000000000000000, 0.9238795325112867385, 1.000000000000000000, 0.9238795325112867385, 1.000000000000000000, 0.9238795325112867385, 1.000000000000000000, 0.9238795325112867385, 1.000000000000000000, 0.9238795325112867385, 1.000000000000000000, 0.9238795325112867385, 1.000000000000000000, 0.9238795325112867385, 1.000000000000000000, 0.9238795325112867385, 1.000000000000000000, 0.9238795325112867385, 1.000000000000000000, 0.9238795325112867385, 1.000000000000000000, 0.9238795325112867385, 1.000000000000000000, 0.9238795325112867385, 1.000000000000000000, 0.9238795325112867385, 1.000000000000000000, 0.9238795325112867385, 1.000000000000000000, 0.9238795325112867385, 1.000000000000000000, 0.9238795325112867385, 1.000000000000000000, 0.9238795325112867385, 1.000000000000000000, 0.9238795325112867385, 1.000000000000000000, 0.9238795325112867385, 1.000000000000000000, 0.9238795325112867385, 1.000000000000000000, 0.9238795325112867385, 1.000000000000000000, 0.9238795325112867385, 1.000000000000000000, 0.9238795325112867385, 1.000000000000000000, 0.9238795325112867385, 1.000000000000000000, 0.9238795325112867385, 1.000000000000000000, 0.9238795325112867385, 1.000000000000000000, 0.9238795325112867385, 1.000000000000000000, 0.9238795325112867385, 1.000000000000000000, 0.9238795325112867385, 1.000000000000000000, 0.9238795325112867385, 1.000000000000000000, 0.9238795325112867385, 1.000000000000000000, 0.9238795325112867385, 1.000000000000000000, 0.9238795325112867385, 1.000000000000000000, 0.9238795325112867385, 1.000000000000000000, 0.9238795325112867385, 1.000000000000000000, 0.9238795325112867385, 1.000000000000000000, 0.9238795325112867385, 1.000000000000000000, 0.9238795325112867385, 1.000000000000000000, 0.9238795325112867385, 1.000000000000000000, 0.9238795325112867385, 1.000000000000000000, 0.9238795325112867385, 1.000000000000000000, 0.9238795325112867385, 1.000000000000000000, 0.9238795325112867385, 1.000000000000000000, 0.9238795325112867385, 1.000000000000000000, 0.9238795325112867385, 1.000000000000000000, 0.9238795325112867385, 1.000000000000000000, 0.9238795325112867385, 1.000000000000000000, 0.9238795325112867385, 1.000000000000000000, 0.9238795325112867385, 1.000000000000000000, 0.9238795325112867385, 1.000000000000000000, 0.9238795325112867385, 1.000000000000000000, 0.9238795325112867385, 1.000000000000000000, 0.9238795325112867385, 1.000000000000000000, 0.9238795325112867385, 1.000000000000000000, 0.9238795325112867385, 1.000000000000000000, 0.9238795325112867385, 1.000000000000000000, 0.9238795325112867385, 1.000000000000000000, 0.9238795325112867385, 1.000000000000000000, 0.9238795325112867385, 1.000000000000000000, 0.9238795325112867385, 1.000000000000000000, 0.9238795325112867385, 1.000000000000000000, 0.9238795325112867385, 1.000000000000000000, 0.9238795325112867385, 1.000000000000000000, 0.9238795325112867385, 1.000000000000000000, 0.9238795325112867385, 1.000000000000000000, 0.9238795325112867385, 1.000000000000000000, 0.9238795325112867385, 1.000000000000000000, 0.9238795325112867385, 1.000000000000000000, 0.9238795325112867385, 1.000000000000000000, 0.9238795325112867385, 1.000000000000000000, 0.9238795325112867385, 1.000000000000000000, 0.9238795325112867385, 1.000000000000000000, 0.9238795325112867385, 1.000000000000000000, 0.9238795325112867385, 1.000000000000000000, 0.9238795325112867385, 1.000000000000000000, 0.9238795325112867385, 1.000000000000000000, 0.9238795325112867385, 1.000000000000000000, 0.9238795325112867385, 1.000000000000000000, 0.9238795325112867385, 1.000000000000000000, 0.9238795325112867385, 1.000000000000000000, 0.9238795325112867385, 1.000000000000000000, 0.9238795325112867385, 1.000000000000000000, 0.9238795325112867385, 1.000000000000000000, 0.9238795325112867385, 1.000000000000000000, 0.9238795325112867385, 1.000000000000000000, 0.9238795325112867385, 1.000000000000000000, 0.9238795325112867385, 1.000000000000000000, 0.9238795325112867385, 1.000000000000000000, 0.9238795325112867385, 1.000000000000000000, 0.9238795325112867385, 1.000000000000000000, 0.9238795325112867385, 1.000000000000000000, 0.9238795325112867385, 1.000000000000000000, 0.9238795325112867385, 1.000000000000000000, 0.9238795325112867385, 1.000000000000000000, 0.9238795325112867385, 1.000000000000000000, 0.9238795325112867385, 1.000000000000000000, 0.9238795325112867385, 1.000000000000000000, 0.9238795325112867385, 1.000000000000000000, 0.9238795325112867385, 1.000000000000000000, 0.9238795325112867385, 1.000000000000000000, 0.9238795325112867385, 1.000000000000000000, 0.9238795325112867385, 1.000000000000000000, 0.9238795325112867385, 1.000000000000000000, 0.9238795325112867385, 1.000000000000000000, 0.9238795325112867385, 1.000000000000000000, 0.9619397654556977040, 0.9619397662556433692 ) ) 
 REPRESENTATION_ITEM ( '' )  );
#14016=CARTESIAN_POINT ( 'NONE',  ( -4.541265875000002339, 7.812499998634407028, -5.561446717895856393E-16 ) ) ;
#14034=CARTESIAN_POINT ( 'NONE',  ( 4.541265875000002339, 17.49999999863440436, -1.881053915767121554 ) ) ;
#14035=CARTESIAN_POINT ( 'NONE',  ( 2.828427124746191623, 11.12500000000000000, -2.828427124746191623 ) ) ;
#14036=AXIS2_PLACEMENT_3D ( 'NONE', #5511, #34193, #45483 ) ;
#14038=ORIENTED_EDGE ( 'NONE', *, *, #46301, .T. ) ;
#14058=EDGE_LOOP ( 'NONE', ( #58841, #15777, #62453, #42216 ) ) ;
#14060=CARTESIAN_POINT ( 'NONE',  ( -4.541265875000002339, 3.874999998634407028, -1.881053915767121998 ) ) ;
#14064=DIRECTION ( 'NONE',  ( -0.000000000000000000, -1.000000000000000000, -0.000000000000000000 ) ) ;
#14072=CARTESIAN_POINT ( 'NONE',  ( -1.656854249492383691, 1.437499997268813390, 4.000000000000000888 ) ) ;
#14078=CARTESIAN_POINT ( 'NONE',  ( 1.881053915767122664, 2.124999998634406584, 4.541265875000001451 ) ) ;
#14100=CARTESIAN_POINT ( 'NONE',  ( 2.449293598294707893E-16, 9.250000000000000000, -4.000000000000001776 ) ) ;
#14110=LINE ( 'NONE', #31101, #22880 ) ;
#14124=CARTESIAN_POINT ( 'NONE',  ( -8.342170076843785083E-16, 3.187499998634407028, 4.541265875000002339 ) ) ;
#14139=CARTESIAN_POINT ( 'NONE',  ( 2.449293598294707893E-16, 17.25000000000000000, -4.000000000000001776 ) ) ;
#14171=CARTESIAN_POINT ( 'NONE',  ( 3.211159895383561835, 13.56249999863440614, -3.211159895383561835 ) ) ;
#14213=CARTESIAN_POINT ( 'NONE',  ( 3.211159895383560947, 14.18749999863440792, 3.211159895383562723 ) ) ;
#14262=CARTESIAN_POINT ( 'NONE',  ( 4.000000000000001776, 18.00000000000000355, 0.000000000000000000 ) ) ;
#14263=CARTESIAN_POINT ( 'NONE',  ( 1.881053915767121998, 16.49999999863440436, -4.541265875000002339 ) ) ;
#14329=ORIENTED_EDGE ( 'NONE', *, *, #47764, .F. ) ;
#14342=AXIS2_PLACEMENT_3D ( 'NONE', #48906, #64789, #19494 ) ;
#14351=CARTESIAN_POINT ( 'NONE',  ( 3.211159895383561835, 5.562499998634407028, -3.211159895383561835 ) ) ;
#14358=CARTESIAN_POINT ( 'NONE',  ( 4.000000000000000888, 2.937500000000000444, 1.656854249492384135 ) ) ;
#14359=CARTESIAN_POINT ( 'NONE',  ( 2.828427124746190291, 19.62499999726881228, 2.828427124746192067 ) ) ;
#14360=CARTESIAN_POINT ( 'NONE',  ( 4.541265875000002339, 4.312499998634407028, 0.000000000000000000 ) ) ;
#14365=CARTESIAN_POINT ( 'NONE',  ( -4.541265875000002339, 16.81249999863440436, -5.561446717895856393E-16 ) ) ;
#14387=CARTESIAN_POINT ( 'NONE',  ( -1.656854249492383468, 5.687500000000000000, 4.000000000000000888 ) ) ;
#14396=CARTESIAN_POINT ( 'NONE',  ( -3.211159895383562723, 4.937499998634407028, 3.211159895383561391 ) ) ;
#14415=CARTESIAN_POINT ( 'NONE',  ( -3.211159895383561391, 19.81249999863440436, -3.211159895383561835 ) ) ;
#14436=CARTESIAN_POINT ( 'NONE',  ( 4.541265875000001451, 10.37499999863440969, 1.881053915767124440 ) ) ;
#14448=CARTESIAN_POINT ( 'NONE',  ( 4.000000000000001776, 6.812499997268813168, -1.656854249492381248 ) ) ;
#14453=CARTESIAN_POINT ( 'NONE',  ( -3.211159895383561391, 7.687499998634407028, -3.211159895383561835 ) ) ;
#14496=CARTESIAN_POINT ( 'NONE',  ( -4.541265875000002339, 3.937499998634406584, -5.561446717895856393E-16 ) ) ;
#14530=CARTESIAN_POINT ( 'NONE',  ( 1.978034651643857389, 21.99999999999999645, 3.835510656344423452 ) ) ;
#14542=CARTESIAN_POINT ( 'NONE',  ( -4.541265875000003227, 17.99999999863440436, 1.881053915767121110 ) ) ;
#14589=CARTESIAN_POINT ( 'NONE',  ( 3.211159895383561835, 15.43749999863440614, -3.211159895383561835 ) ) ;
#14619=ORIENTED_EDGE ( 'NONE', *, *, #18513, .T. ) ;
#14623=CARTESIAN_POINT ( 'NONE',  ( -4.000000000000002665, 11.31249999726881406, 1.656854249492380582 ) ) ;
#14636=CARTESIAN_POINT ( 'NONE',  ( -2.828427124746190735, 16.37500000000000000, -2.828427124746191623 ) ) ;
#14637=CARTESIAN_POINT ( 'NONE',  ( -3.211159895383562723, 14.93749999863440792, 3.211159895383561391 ) ) ;
#14649=ORIENTED_EDGE ( 'NONE', *, *, #73603, .F. ) ;
#14661=CARTESIAN_POINT ( 'NONE',  ( 4.000000000000001776, 14.00000000000000000, 0.000000000000000000 ) ) ;
#14708=CARTESIAN_POINT ( 'NONE',  ( 2.828427124746190291, 21.87500000000000355, 2.828427124746192067 ) ) ;
#14721=CARTESIAN_POINT ( 'NONE',  ( 3.211159895383560947, 21.31249999863440792, 3.211159895383562723 ) ) ;
#14724=CARTESIAN_POINT ( 'NONE',  ( -4.541265875000002339, 5.937499998634407028, -5.561446717895856393E-16 ) ) ;
#14733=CARTESIAN_POINT ( 'NONE',  ( -1.656854249492383691, 4.687500000000000888, 4.000000000000000888 ) ) ;
#14734=CARTESIAN_POINT ( 'NONE',  ( 4.000000000000000888, 19.68749999726881228, 1.656854249492384135 ) ) ;
#14735=CARTESIAN_POINT ( 'NONE',  ( 1.881053915767122664, 5.124999998634407028, 4.541265875000001451 ) ) ;
#14740=CARTESIAN_POINT ( 'NONE',  ( -4.541265875000002339, 19.81249999863440436, -5.561446717895856393E-16 ) ) ;
#14749=CARTESIAN_POINT ( 'NONE',  ( 2.449293598294707893E-16, 20.99999999726881583, -4.000000000000001776 ) ) ;
#14770=CARTESIAN_POINT ( 'NONE',  ( 4.541265875000002339, 5.374999998634406140, -1.881053915767121554 ) ) ;
#14772=CARTESIAN_POINT ( 'NONE',  ( -4.000000000000001776, 14.18749999726881406, -1.656854249492381470 ) ) ;
#14787=CARTESIAN_POINT ( 'NONE',  ( -1.881053915767121554, 20.74999999863440436, -4.541265875000002339 ) ) ;
#14797=DIRECTION ( 'NONE',  ( -0.000000000000000000, -1.000000000000000000, -0.000000000000000000 ) ) ;
#14811=CARTESIAN_POINT ( 'NONE',  ( -3.211159895383561391, 10.81249999863440792, -3.211159895383561835 ) ) ;
#14820=CARTESIAN_POINT ( 'NONE',  ( 2.449293598294707893E-16, 6.999999997268813168, -4.000000000000001776 ) ) ;
#14827=CARTESIAN_POINT ( 'NONE',  ( -4.541265875000002339, 4.812499998634407028, -5.561446717895856393E-16 ) ) ;
#14832=CARTESIAN_POINT ( 'NONE',  ( 2.449293598294707893E-16, 21.25000000000000000, -4.000000000000001776 ) ) ;
#14872=CARTESIAN_POINT ( 'NONE',  ( 1.881053915767122664, 10.24999999863440792, 4.541265875000001451 ) ) ;
#14906=CARTESIAN_POINT ( 'NONE',  ( -7.347880794884122694E-16, 7.750000000000000000, 4.000000000000001776 ) ) ;
#14916=CARTESIAN_POINT ( 'NONE',  ( 3.211159895383560947, 16.31249999863440436, 3.211159895383562723 ) ) ;
#14935=ORIENTED_EDGE ( 'NONE', *, *, #7604, .T. ) ;
#14951=DIRECTION ( 'NONE',  ( -0.000000000000000000, -1.000000000000000000, -0.000000000000000000 ) ) ;
#14963=CARTESIAN_POINT ( 'NONE',  ( -8.342170076843785083E-16, 20.06249999863440436, 4.541265875000002339 ) ) ;
#14984=CARTESIAN_POINT ( 'NONE',  ( 2.828427124746190291, 14.87500000000000178, 2.828427124746192067 ) ) ;
#14995=CARTESIAN_POINT ( 'NONE',  ( -2.828427124746192067, 19.62500000000000000, 2.828427124746190735 ) ) ;
#14999=CARTESIAN_POINT ( 'NONE',  ( -7.347880794884122694E-16, 20.75000000000000000, 4.000000000000001776 ) ) ;
#15014=CARTESIAN_POINT ( 'NONE',  ( -7.347880794884122694E-16, 14.75000000000000178, 4.000000000000001776 ) ) ;
#15015=CARTESIAN_POINT ( 'NONE',  ( 1.881053915767121998, 18.49999999863440436, -4.541265875000002339 ) ) ;
#15059=CARTESIAN_POINT ( 'NONE',  ( 4.000000000000001776, 17.00000000000000000, 0.000000000000000000 ) ) ;
#15062=CARTESIAN_POINT ( 'NONE',  ( -4.000000000000001776, 8.187499997268814056, -1.656854249492381470 ) ) ;
#15097=CARTESIAN_POINT ( 'NONE',  ( -1.881053915767121776, 19.74999999863440081, -4.541265875000002339 ) ) ;
#15098=ORIENTED_EDGE ( 'NONE', *, *, #41732, .F. ) ;
#15100=CARTESIAN_POINT ( 'NONE',  ( -4.541265875000002339, 4.874999998634407916, -1.881053915767121998 ) ) ;
#15109=CARTESIAN_POINT ( 'NONE',  ( -2.828427124746190735, 5.375000000000000000, -2.828427124746191623 ) ) ;
#15110=CARTESIAN_POINT ( 'NONE',  ( -7.347880794884122694E-16, 16.49999999726881228, 4.000000000000001776 ) ) ;
#15111=CARTESIAN_POINT ( 'NONE',  ( -4.541265875000003227, 2.874999998634407028, 1.881053915767121110 ) ) ;
#15118=CARTESIAN_POINT ( 'NONE',  ( 1.881053915767121776, 18.49999999863440436, -4.541265875000002339 ) ) ;
#15149=CARTESIAN_POINT ( 'NONE',  ( -1.881053915767124440, 4.999999998634406140, 4.541265875000001451 ) ) ;
#15158=CARTESIAN_POINT ( 'NONE',  ( 1.656854249492381914, 19.56249999726881228, 4.000000000000000888 ) ) ;
#15169=CARTESIAN_POINT ( 'NONE',  ( -3.211159895383561391, 18.81249999863440436, -3.211159895383561835 ) ) ;
#15175=CARTESIAN_POINT ( 'NONE',  ( -2.828427124746192067, 12.37499999726881406, 2.828427124746190735 ) ) ;
#15193=CARTESIAN_POINT ( 'NONE',  ( -8.342170076843785083E-16, 7.187499998634407028, 4.541265875000002339 ) ) ;
#15202=CARTESIAN_POINT ( 'NONE',  ( 4.000000000000001776, 6.749999997268813168, 0.000000000000000000 ) ) ;
#15207=CARTESIAN_POINT ( 'NONE',  ( -1.881053915767121554, 7.624999998634408804, -4.541265875000002339 ) ) ;
#15212=CARTESIAN_POINT ( 'NONE',  ( -7.347880794884122694E-16, 21.75000000000000355, 4.000000000000001776 ) ) ;
#15248=CARTESIAN_POINT ( 'NONE',  ( -8.342170076843785083E-16, 9.187499998634407916, 4.541265875000002339 ) ) ;
#15289=CARTESIAN_POINT ( 'NONE',  ( 0.000000000000000000, 0.000000000000000000, 0.000000000000000000 ) ) ;
#15290=CARTESIAN_POINT ( 'NONE',  ( 2.780723358947928197E-16, 17.68749999863440792, -4.541265875000002339 ) ) ;
#15335=CARTESIAN_POINT ( 'NONE',  ( -3.211159895383562723, 16.93749999863440436, 3.211159895383561391 ) ) ;
#15372=CARTESIAN_POINT ( 'NONE',  ( 1.881053915767122664, 2.249999998634407028, 4.541265875000001451 ) ) ;
#15387=CARTESIAN_POINT ( 'NONE',  ( -4.000000000000001776, 21.50000000000000000, -4.898587196589415787E-16 ) ) ;
#15388=CARTESIAN_POINT ( 'NONE',  ( 1.881053915767121998, 19.49999999863440436, -4.541265875000002339 ) ) ;
#15400=EDGE_LOOP ( 'NONE', ( #26833, #65919, #50260, #8440 ) ) ;
#15429=CARTESIAN_POINT ( 'NONE',  ( -7.347880794884122694E-16, 16.75000000000000000, 4.000000000000001776 ) ) ;
#15459=DIRECTION ( 'NONE',  ( 0.000000000000000000, 0.000000000000000000, -1.000000000000000000 ) ) ;
#15470=CARTESIAN_POINT ( 'NONE',  ( -3.211159895383561391, 21.81249999863440792, -3.211159895383561835 ) ) ;
#15473=CARTESIAN_POINT ( 'NONE',  ( -1.881053915767121554, 2.749999998634406584, -4.541265875000002339 ) ) ;
#15480=CARTESIAN_POINT ( 'NONE',  ( -2.828427124746192067, 3.625000000000000000, 2.828427124746190735 ) ) ;
#15481=CARTESIAN_POINT ( 'NONE',  ( 4.000000000000000888, 18.68749999726881583, 1.656854249492384135 ) ) ;
#15482=CARTESIAN_POINT ( 'NONE',  ( 1.881053915767122664, 8.124999998634406140, 4.541265875000001451 ) ) ;
#15490=CARTESIAN_POINT ( 'NONE',  ( -4.541265875000002339, 18.74999999863440436, -1.881053915767121998 ) ) ;
#15520=CARTESIAN_POINT ( 'NONE',  ( 4.541265875000001451, 5.249999998634406140, 1.881053915767124440 ) ) ;
#15538=CARTESIAN_POINT ( 'NONE',  ( 1.881053915767122664, 19.24999999863440436, 4.541265875000001451 ) ) ;
#15560=CARTESIAN_POINT ( 'NONE',  ( -4.541265875000002339, 7.937499998634407028, -5.561446717895856393E-16 ) ) ;
#15571=CARTESIAN_POINT ( 'NONE',  ( -4.000000000000001776, 6.187499997268813168, -1.656854249492381470 ) ) ;
#15577=CARTESIAN_POINT ( 'NONE',  ( 3.211159895383561835, 5.437499998634407028, -3.211159895383561835 ) ) ;
#15583=CARTESIAN_POINT ( 'NONE',  ( -1.656854249492381248, 21.31250000000000000, -4.000000000000001776 ) ) ;
#15586=CARTESIAN_POINT ( 'NONE',  ( -2.828427124746190735, 18.37500000000000000, -2.828427124746191623 ) ) ;
#15607=DIRECTION ( 'NONE',  ( -0.000000000000000000, -1.000000000000000000, -0.000000000000000000 ) ) ;
#15621=CARTESIAN_POINT ( 'NONE',  ( 3.211159895383561835, 8.562499998634407916, -3.211159895383561835 ) ) ;
#15629=DIRECTION ( 'NONE',  ( 0.000000000000000000, 0.000000000000000000, -1.000000000000000000 ) ) ;
#15641=LINE ( 'NONE', #27336, #23842 ) ;
#15661=( BOUNDED_CURVE ( )  B_SPLINE_CURVE ( 2, ( #4813, #51948, #22893, #51193, #45166, #39875, #6305, #34238, #23266 ),
 .UNSPECIFIED., .F., .F. ) 
 B_SPLINE_CURVE_WITH_KNOTS ( ( 3, 2, 2, 2, 3 ),
 ( 0.2613636363636363535, 0.2670454545454545303, 0.2727272727272727071, 0.2784090909090908839, 0.2840909090909091161 ),
 .UNSPECIFIED. ) 
 CURVE ( )  GEOMETRIC_REPRESENTATION_ITEM ( )  RATIONAL_B_SPLINE_CURVE ( ( 1.000000000000000000, 0.9238795325112867385, 1.000000000000000000, 0.9238795325112867385, 1.000000000000000000, 0.9238795325112867385, 1.000000000000000000, 0.9238795325112867385, 1.000000000000000000 ) ) 
 REPRESENTATION_ITEM ( '' )  );
#15664=CARTESIAN_POINT ( 'NONE',  ( -1.881053915767124440, 14.12499999863440969, 4.541265875000001451 ) ) ;
#15669=EDGE_CURVE ( 'NONE', #46255, #33515, #43654, .T. ) ;
#15709=CARTESIAN_POINT ( 'NONE',  ( 1.881053915767121776, 16.49999999863440436, -4.541265875000002339 ) ) ;
#15759=CARTESIAN_POINT ( 'NONE',  ( 4.000000000000001776, 19.06250000000000000, -1.656854249492381248 ) ) ;
#15760=CARTESIAN_POINT ( 'NONE',  ( 4.541265875000002339, 19.31249999863440436, 0.000000000000000000 ) ) ;
#15763=EDGE_CURVE ( 'NONE', #2415, #41608, #46258, .T. ) ;
#15766=CARTESIAN_POINT ( 'NONE',  ( 4.000000000000001776, 4.812499997268813168, -1.656854249492381248 ) ) ;
#15777=ORIENTED_EDGE ( 'NONE', *, *, #21054, .F. ) ;
#15797=CARTESIAN_POINT ( 'NONE',  ( -7.347880794884122694E-16, 17.49999999726881583, 4.000000000000001776 ) ) ;
#15844=CARTESIAN_POINT ( 'NONE',  ( 3.211159895383560947, 7.312499998634407028, 3.211159895383562723 ) ) ;
#15849=CARTESIAN_POINT ( 'NONE',  ( 4.000000000000001776, 8.062500000000000000, -1.656854249492381248 ) ) ;
#15851=CARTESIAN_POINT ( 'NONE',  ( 3.211159895383561835, 9.437499998634406140, -3.211159895383561835 ) ) ;
#15859=CARTESIAN_POINT ( 'NONE',  ( 4.541265875000002339, 19.31249999863440436, 0.000000000000000000 ) ) ;
#15877=ORIENTED_EDGE ( 'NONE', *, *, #42246, .F. ) ;
#15895=CARTESIAN_POINT ( 'NONE',  ( 4.898587196589415787E-16, 0.000000000000000000, 4.000000000000001776 ) ) ;
#15911=CARTESIAN_POINT ( 'NONE',  ( 1.881053915767121776, 20.62499999863441147, -4.541265875000002339 ) ) ;
#15932=CARTESIAN_POINT ( 'NONE',  ( 1.881053915767122664, 10.24999999863440792, 4.541265875000001451 ) ) ;
#15944=CARTESIAN_POINT ( 'NONE',  ( 2.828427124746190291, 7.624999997268813168, 2.828427124746192067 ) ) ;
#15953=CARTESIAN_POINT ( 'NONE',  ( 3.211159895383561835, 6.437499998634407028, -3.211159895383561835 ) ) ;
#15960=CARTESIAN_POINT ( 'NONE',  ( -7.347880794884122694E-16, 10.75000000000000000, 4.000000000000001776 ) ) ;
#15995=CARTESIAN_POINT ( 'NONE',  ( 4.541265875000001451, 9.374999998634407916, 1.881053915767124440 ) ) ;
#16038=CARTESIAN_POINT ( 'NONE',  ( 3.211159895383561835, 14.56249999863440792, -3.211159895383561835 ) ) ;
#16072=CARTESIAN_POINT ( 'NONE',  ( 2.449293598294707893E-16, 2.250000000000000444, -4.000000000000001776 ) ) ;
#16077=CARTESIAN_POINT ( 'NONE',  ( 1.881053915767122664, 19.12499999863441147, 4.541265875000001451 ) ) ;
#16083=CARTESIAN_POINT ( 'NONE',  ( 0.000000000000000000, 0.000000000000000000, 0.000000000000000000 ) ) ;
#16125=CARTESIAN_POINT ( 'NONE',  ( -2.828427124746190735, 18.37500000000000000, -2.828427124746191623 ) ) ;
#16126=CARTESIAN_POINT ( 'NONE',  ( 2.780723358947928197E-16, 21.56249999863440792, -4.541265875000002339 ) ) ;
#16128=ORIENTED_EDGE ( 'NONE', *, *, #46092, .F. ) ;
#16166=ORIENTED_EDGE ( 'NONE', *, *, #19639, .T. ) ;
#16179=PRODUCT_DEFINITION_SHAPE ( 'NONE', 'NONE',  #29780 ) ;
#16208=CARTESIAN_POINT ( 'NONE',  ( -8.342170076843785083E-16, 8.187499998634406140, 4.541265875000002339 ) ) ;
#16212=( BOUNDED_CURVE ( )  B_SPLINE_CURVE ( 2, ( #29311, #28931, #51949, #45906, #39876, #64378, #70045, #29674, #28556 ),
 .UNSPECIFIED., .F., .F. ) 
 B_SPLINE_CURVE_WITH_KNOTS ( ( 3, 2, 2, 2, 3 ),
 ( 0.3977272727272727626, 0.4034090909090909394, 0.4090909090909091717, 0.4147727272727272929, 0.4204545454545454697 ),
 .UNSPECIFIED. ) 
 CURVE ( )  GEOMETRIC_REPRESENTATION_ITEM ( )  RATIONAL_B_SPLINE_CURVE ( ( 0.9999999999999992228, 0.9238795325112875156, 1.000000000000000000, 0.9238795325112867385, 1.000000000000000000, 0.9238795325112867385, 1.000000000000000000, 0.9238795325112867385, 1.000000000000000000 ) ) 
 REPRESENTATION_ITEM ( '' )  );
#16215=CARTESIAN_POINT ( 'NONE',  ( -7.347880794884122694E-16, 9.750000000000000000, 4.000000000000001776 ) ) ;
#16216=CARTESIAN_POINT ( 'NONE',  ( 2.449293598294707893E-16, 20.99999999726881583, -4.000000000000001776 ) ) ;
#16217=CARTESIAN_POINT ( 'NONE',  ( 4.541265875000002339, 6.312499998634407028, 0.000000000000000000 ) ) ;
#16220=ORIENTED_EDGE ( 'NONE', *, *, #18092, .T. ) ;
#16226=CARTESIAN_POINT ( 'NONE',  ( -3.211159895383562723, 20.93749999863440436, 3.211159895383561391 ) ) ;
#16227=VECTOR ( 'NONE', #70816, 1000.000000000000000 ) ;
#16258=LINE ( 'NONE', #15895, #64780 ) ;
#16267=CARTESIAN_POINT ( 'NONE',  ( 0.000000000000000000, 15.99999999999998579, 0.000000000000000000 ) ) ;
#16295=CARTESIAN_POINT ( 'NONE',  ( 3.211159895383561835, 12.56249999863440792, -3.211159895383561835 ) ) ;
#16305=CARTESIAN_POINT ( 'NONE',  ( 1.656854249492381914, 8.562499997268814056, 4.000000000000000888 ) ) ;
#16308=ADVANCED_FACE ( 'NONE', ( #60542 ), #67332, .T. ) ;
#16313=CARTESIAN_POINT ( 'NONE',  ( 4.541265875000002339, 11.31249999863440614, 0.000000000000000000 ) ) ;
#16315=CARTESIAN_POINT ( 'NONE',  ( -2.828427124746190735, 10.12499999726881406, -2.828427124746191623 ) ) ;
#16346=VERTEX_POINT ( 'NONE', #60168 ) ;
#16355=CARTESIAN_POINT ( 'NONE',  ( -3.211159895383561391, 13.81249999863440614, -3.211159895383561835 ) ) ;
#16401=CARTESIAN_POINT ( 'NONE',  ( 3.211159895383561835, 19.56249999863440436, -3.211159895383561835 ) ) ;
#16402=ORIENTED_EDGE ( 'NONE', *, *, #6051, .F. ) ;
#16407=VECTOR ( 'NONE', #1381, 1000.000000000000000 ) ;
#16447=CARTESIAN_POINT ( 'NONE',  ( 1.881053915767122664, 18.12499999863440792, 4.541265875000001451 ) ) ;
#16484=CARTESIAN_POINT ( 'NONE',  ( 2.449293598294707893E-16, 0.9999999972688131678, -4.000000000000001776 ) ) ;
#16489=ORIENTED_EDGE ( 'NONE', *, *, #27773, .F. ) ;
#16500=CARTESIAN_POINT ( 'NONE',  ( -4.000000000000001776, 18.43749999999999645, -1.656854249492381470 ) ) ;
#16501=CARTESIAN_POINT ( 'NONE',  ( -4.541265875000003227, 19.87499999863441147, 1.881053915767121110 ) ) ;
#16503=CARTESIAN_POINT ( 'NONE',  ( 2.828427124746190291, 4.624999997268813168, 2.828427124746192067 ) ) ;
#16510=ORIENTED_EDGE ( 'NONE', *, *, #55945, .T. ) ;
#16541=CARTESIAN_POINT ( 'NONE',  ( 2.449293598294707893E-16, 17.25000000000000000, -4.000000000000001776 ) ) ;
#16568=CARTESIAN_POINT ( 'NONE',  ( 1.656854249492381248, 18.93749999726881228, -4.000000000000001776 ) ) ;
#16583=CARTESIAN_POINT ( 'NONE',  ( 2.780723358947928197E-16, 7.687499998634407028, -4.541265875000002339 ) ) ;
#16587=CARTESIAN_POINT ( 'NONE',  ( -1.656854249492381248, 8.312500000000000000, -4.000000000000001776 ) ) ;
#16589=CARTESIAN_POINT ( 'NONE',  ( 4.541265875000001451, 7.249999998634407916, 1.881053915767124440 ) ) ;
#16601=ORIENTED_EDGE ( 'NONE', *, *, #59841, .T. ) ;
#16652=CARTESIAN_POINT ( 'NONE',  ( -7.347880794884122694E-16, 20.49999999726881583, 4.000000000000001776 ) ) ;
#16663=FACE_OUTER_BOUND ( 'NONE', #4718, .T. ) ;
#16669=CARTESIAN_POINT ( 'NONE',  ( -4.541265875000002339, 13.87499999863440792, -1.881053915767121998 ) ) ;
#16680=CARTESIAN_POINT ( 'NONE',  ( 4.000000000000000888, 10.68749999726881406, 1.656854249492384135 ) ) ;
#16686=CARTESIAN_POINT ( 'NONE',  ( 4.541265875000002339, 12.31249999863440792, 0.000000000000000000 ) ) ;
#16714=CYLINDRICAL_SURFACE ( 'NONE', #39315, 4.000000000000001776 ) ;
#16731=CARTESIAN_POINT ( 'NONE',  ( -1.881053915767121554, 12.74999999863440969, -4.541265875000002339 ) ) ;
#16774=CARTESIAN_POINT ( 'NONE',  ( -4.541265875000002339, 21.93749999863440792, -5.561446717895856393E-16 ) ) ;
#16800=CARTESIAN_POINT ( 'NONE',  ( -3.425306192931087068, 22.00000000000000355, 2.996540939710079954 ) ) ;
#16802=LINE ( 'NONE', #57576, #55845 ) ;
#16821=CARTESIAN_POINT ( 'NONE',  ( 4.541265875000002339, 0.4374999986344068059, 0.000000000000000000 ) ) ;
#16824=( LENGTH_UNIT ( ) NAMED_UNIT ( * ) SI_UNIT ( .MILLI., .METRE. ) );
#16869=ORIENTED_EDGE ( 'NONE', *, *, #64781, .T. ) ;
#16870=EDGE_CURVE ( 'NONE', #41608, #28042, #17892, .T. ) ;
#16882=CARTESIAN_POINT ( 'NONE',  ( -2.828427124746192067, 18.62500000000000000, 2.828427124746190735 ) ) ;
#16894=ORIENTED_EDGE ( 'NONE', *, *, #35904, .F. ) ;
#16921=CARTESIAN_POINT ( 'NONE',  ( -4.541265875000002339, 11.74999999863440792, -1.881053915767121998 ) ) ;
#16962=FACE_OUTER_BOUND ( 'NONE', #33171, .T. ) ;
#16966=CARTESIAN_POINT ( 'NONE',  ( 4.541265875000001451, 9.374999998634407916, 1.881053915767124440 ) ) ;
#16972=CARTESIAN_POINT ( 'NONE',  ( 1.656854249492381914, 6.812500000000000000, 4.000000000000000888 ) ) ;
#16973=CARTESIAN_POINT ( 'NONE',  ( -1.656854249492381248, 21.06249999726881583, -4.000000000000001776 ) ) ;
#16974=CARTESIAN_POINT ( 'NONE',  ( 2.780723358947928197E-16, 13.56249999863440614, -4.541265875000002339 ) ) ;
#17022=DIRECTION ( 'NONE',  ( -1.000000000000000000, -0.000000000000000000, 0.000000000000000000 ) ) ;
#17046=EDGE_CURVE ( 'NONE', #61381, #42656, #52134, .T. ) ;
#17053=CARTESIAN_POINT ( 'NONE',  ( -3.211159895383562723, 13.06249999863440792, 3.211159895383561391 ) ) ;
#17064=CARTESIAN_POINT ( 'NONE',  ( -2.828427124746192067, 9.374999997268814056, 2.828427124746190735 ) ) ;
#17065=CARTESIAN_POINT ( 'NONE',  ( -7.347880794884122694E-16, 17.75000000000000355, 4.000000000000001776 ) ) ;
#17071=CARTESIAN_POINT ( 'NONE',  ( 1.881053915767122664, 10.12499999863440792, 4.541265875000001451 ) ) ;
#17076=ORIENTED_EDGE ( 'NONE', *, *, #72067, .F. ) ;
#17097=CARTESIAN_POINT ( 'NONE',  ( 1.656854249492381914, 1.562499997268813390, 4.000000000000000888 ) ) ;
#17098=DIRECTION ( 'NONE',  ( 1.000000000000000000, 0.000000000000000000, -0.000000000000000000 ) ) ;
#17114=CARTESIAN_POINT ( 'NONE',  ( 4.541265875000002339, 10.49999999863440792, -1.881053915767121554 ) ) ;
#17142=CARTESIAN_POINT ( 'NONE',  ( 4.541265875000001451, 1.374999998634407250, 1.881053915767124440 ) ) ;
#17146=EDGE_CURVE ( 'NONE', #43761, #3011, #4903, .T. ) ;
#17150=CARTESIAN_POINT ( 'NONE',  ( 2.449293598294707893E-16, 0.2500000000000001665, -4.000000000000001776 ) ) ;
#17153=EDGE_CURVE ( 'NONE', #282, #31861, #12595, .T. ) ;
#17158=CARTESIAN_POINT ( 'NONE',  ( 4.541265875000001451, 19.37499999863440792, 1.881053915767124440 ) ) ;
#17165=FACE_OUTER_BOUND ( 'NONE', #62893, .T. ) ;
#17200=CARTESIAN_POINT ( 'NONE',  ( -4.000000000000001776, 11.43750000000000000, -1.656854249492381470 ) ) ;
#17203=CARTESIAN_POINT ( 'NONE',  ( 4.541265875000001451, 21.24999999863440436, 1.881053915767124440 ) ) ;
#17210=CARTESIAN_POINT ( 'NONE',  ( 4.000000000000000888, 15.68749999726881406, 1.656854249492384135 ) ) ;
#17221=CARTESIAN_POINT ( 'NONE',  ( 0.000000000000000000, 0.000000000000000000, -4.000000000000001776 ) ) ;
#17259=CARTESIAN_POINT ( 'NONE',  ( 3.211159895383560947, 2.187499998634407028, 3.211159895383562723 ) ) ;
#17270=SHAPE_DEFINITION_REPRESENTATION ( #16179, #30147 ) ;
#17295=CARTESIAN_POINT ( 'NONE',  ( 2.828427124746190291, 9.875000000000000000, 2.828427124746192067 ) ) ;
#17296=CARTESIAN_POINT ( 'NONE',  ( 2.780723358947928197E-16, 9.562499998634406140, -4.541265875000002339 ) ) ;
#17315=CARTESIAN_POINT ( 'NONE',  ( 0.000000000000000000, 15.99999999999998579, -1.000000000000000000 ) ) ;
#17337=CARTESIAN_POINT ( 'NONE',  ( 1.881053915767121776, 7.624999998634408804, -4.541265875000002339 ) ) ;
#17343=CARTESIAN_POINT ( 'NONE',  ( 4.000000000000000888, 8.937500000000001776, 1.656854249492384135 ) ) ;
#17344=CARTESIAN_POINT ( 'NONE',  ( -7.347880794884122694E-16, 21.49999999726881583, 4.000000000000001776 ) ) ;
#17345=CARTESIAN_POINT ( 'NONE',  ( -1.881053915767121776, 10.62499999863440969, -4.541265875000002339 ) ) ;
#17348=AXIS2_PLACEMENT_3D ( 'NONE', #52944, #13292, #35595 ) ;
#17355=ORIENTED_EDGE ( 'NONE', *, *, #49425, .F. ) ;
#17424=CARTESIAN_POINT ( 'NONE',  ( -3.211159895383562723, 14.06249999863440614, 3.211159895383561391 ) ) ;
#17433=AXIS2_PLACEMENT_3D ( 'NONE', #48165, #20230, #66637 ) ;
#17436=CARTESIAN_POINT ( 'NONE',  ( 4.000000000000001776, 10.74999999726881406, 0.000000000000000000 ) ) ;
#17438=CARTESIAN_POINT ( 'NONE',  ( 3.211159895383561835, 1.437499998634406806, -3.211159895383561835 ) ) ;
#17444=CARTESIAN_POINT ( 'NONE',  ( -3.211159895383561391, 11.68749999863440614, -3.211159895383561835 ) ) ;
#17491=CARTESIAN_POINT ( 'NONE',  ( -4.541265875000002339, 12.87499999863440969, -1.881053915767121998 ) ) ;
#17519=CARTESIAN_POINT ( 'NONE',  ( -1.881053915767121776, 2.749999998634407028, -4.541265875000002339 ) ) ;
#17530=CARTESIAN_POINT ( 'NONE',  ( -2.828427124746190735, 15.37500000000000000, -2.828427124746191623 ) ) ;
#17531=CARTESIAN_POINT ( 'NONE',  ( -1.881053915767124440, 21.12499999863441147, 4.541265875000001451 ) ) ;
#17579=CARTESIAN_POINT ( 'NONE',  ( -1.881053915767124440, 20.99999999863440792, 4.541265875000001451 ) ) ;
#17586=CARTESIAN_POINT ( 'NONE',  ( -7.347880794884122694E-16, 15.49999999726881406, 4.000000000000001776 ) ) ;
#17596=CARTESIAN_POINT ( 'NONE',  ( -4.000000000000001776, 6.249999997268812280, -4.898587196589415787E-16 ) ) ;
#17670=CARTESIAN_POINT ( 'NONE',  ( 3.211159895383560947, 9.187499998634407916, 3.211159895383562723 ) ) ;
#17704=PRODUCT_DEFINITION_FORMATION_WITH_SPECIFIED_SOURCE ( 'ANY', '', #1223, .NOT_KNOWN. ) ;
#17707=EDGE_CURVE ( 'NONE', #61795, #45464, #17983, .T. ) ;
#17712=CARTESIAN_POINT ( 'NONE',  ( 1.881053915767121776, 11.62499999863440969, -4.541265875000002339 ) ) ;
#17715=CARTESIAN_POINT ( 'NONE',  ( 4.000000000000001776, 14.06249999999999822, -1.656854249492381248 ) ) ;
#17717=CARTESIAN_POINT ( 'NONE',  ( 1.881053915767122664, 11.12499999863440969, 4.541265875000001451 ) ) ;
#17732=CARTESIAN_POINT ( 'NONE',  ( -1.656854249492371034, 9.437499997268814056, 4.000000000000013323 ) ) ;
#17747=CLOSED_SHELL ( 'NONE', ( #24296, #63736, #48144, #39313, #954, #72931, #70333, #37115, #17999, #57284, #16308, #34847, #28328, #1056, #26412, #3185, #47867, #20965, #45163, #61930, #54657, #42944, #49772, #13857, #24299, #64488, #20822, #12929, #26228, #13149, #54244, #33519, #12519, #65084, #60109, #46262, #26743, #54374, #22810, #70477, #31108, #53866, #344, #20568, #53917, #60157, #12972, #10196, #11619, #44567, #68075, #40408, #55036, #64689, #27096, #18641 ) ) ;
#17774=( BOUNDED_SURFACE ( )  B_SPLINE_SURFACE ( 1, 2, ( 
 ( #5421, #46890, #18959, #42699, #47254, #41963, #19318, #58597, #8007, #18593, #47616, #35950, #1628, #64619, #70639, #31014, #18224, #2349, #52931, #47989, #71364, #59335, #64245, #29545, #7276, #30283, #53668, #64971, #35221, #25344, #24608, #53304, #41239, #42330, #13280, #23881, #6539, #12915, #65712, #36320, #65348, #58968, #70281, #41604, #58241, #52556, #48358, #1262, #7646, #6903, #13649, #30651, #36688, #895, #1981, #24973, #59699, #71002, #54039, #19690, #12555, #69914, #35583, #29914, #24241, #72117, #54787, #20430, #32910, #3099, #21186, #37053, #43070, #66086, #14396, #15149, #49485, #43831, #43446, #15520, #32146, #14770, #44584, #60804, #55166, #4227, #55542, #26461, #54416, #49863, #61561, #26084, #38560, #9129, #44211, #50232, #67224, #3472, #72504, #8757, #66461, #3852, #73253, #37430, #20813, #60430, #37808, #31768, #49105, #66846, #38181, #26848, #61185, #9515, #32530, #72880, #21558, #9882, #55915, #27215, #14016, #60053, #31390, #8374, #2723, #25711, #48732, #71738, #20053, #28995, #40687, #46343, #63318, #52013, #63689, #52753, #29738, #12016, #1089, #68612, #18048, #35049, #17670, #57685, #5621, #1460, #7102, #41433, #17296, #64445, #35416, #30110, #45972, #58061, #69360, #69733, #40314, #53127, #62949, #6372, #57310, #11274, #29378, #74649, #52385, #720, #58426, #12746, #47076, #351, #35777, #6734, #18419, #51634, #70113, #34306, #58792, #24441, #23704, #22964, #23331, #68987, #46708, #16921, #41063, #64073, #12381, #24066, #39944, #28621, #34679, #11644, #5993, #59522, #64805, #2546, #8948, #7835, #31589, #13833, #70835, #30840, #19510, #25167, #42150, #53861, #42528, #54610, #8573, #65542, #2917, #47449, #71560, #36879, #71191, #36513, #59164, #54985, #60626, #20247, #19147, #43267, #14213, #31960, #24798, #59887, #48184, #48550, #65163, #3292, #41796, #8200, #36143, #13107, #31212, #53495, #54237, #25537, #37251, #66282, #25905, #2173, #14589, #60247, #71935, #30478, #48922, #7473, #37628, #70473, #19882, #1812, #42888, #47812, #65907, #18791, #13474, #67411, #73067, #15709, #22114, #27406, #67036, #72316, #39111, #38370, #15335, #32723, #45138, #61375, #33469, #49299, #55357, #3662, #26662, #50421, #61751, #56101, #55731, #27780, #44397, #27040, #56841, #21373, #38751, #16447, #67785, #10069, #66656, #62115, #73806, #9702, #50793, #33104, #56471, #62479, #4787, #4410, #73435, #21001, #4048, #16077, #10809, #49685, #21743, #72700, #50051, #44027, #44771, #10439, #68150, #39483, #33843, #26278, #20629, #43645, #14963, #38000, #60998, #9324, #32344, #23241, #34586, #6644, #46249, #5902, #35685, #51920, #69268, #70020, #46621, #17579, #45501, #40973, #52662, #17203, #29647, #258, #35328, #41341, #58340, #40597, #63598, #74553, #11552, #69641, #64351, #28528, #11925, #34211, #28902, #57213, #5527 ),
 ( #16821, #39849, #998, #12654, #34957, #57972, #23979, #46987, #5162, #17955, #28156, #62850, #6278, #18326, #63980, #630, #12293, #29284, #52294, #11186, #23611, #51167, #68519, #74176, #51536, #22480, #22865, #45879, #68893, #40222, #63225, #57592, #8113, #70385, #1365, #31118, #2826, #36055, #65450, #13747, #7381, #53034, #53407, #2455, #14124, #54146, #71101, #66192, #43176, #30388, #2083, #65817, #25448, #19794, #18700, #42434, #14496, #70743, #36790, #42801, #1730, #31499, #42063, #19421, #59436, #25075, #13384, #59800, #54520, #41707, #25817, #24710, #71468, #20159, #48463, #13017, #24350, #30753, #53774, #37158, #60160, #58700, #48836, #48092, #8479, #64721, #71842, #59072, #7011, #30020, #47722, #47359, #19061, #65071, #36422, #7748, #49966, #45055, #22029, #60908, #55643, #44682, #4326, #73353, #49211, #21286, #68066, #49592, #44309, #21657, #9231, #10353, #20914, #72980, #38282, #3958, #66944, #67324, #33377, #20535, #4699, #55271, #50331, #73719, #61663, #66563, #31871, #9614, #32634, #56014, #15621, #37535, #27692, #26947, #38661, #43549, #67698, #9982, #26191, #8861, #15248, #60535, #33013, #15995, #61287, #72608, #43935, #54892, #3203, #50701, #3576, #27315, #32253, #39025, #62029, #56378, #72220, #14872, #37911, #26568, #45792, #17114, #40136, #22392, #52573, #28068, #45412, #57509, #74461, #11470, #5815, #33751, #63142, #35237, #34504, #68802, #17865, #5074, #51079, #74093, #12199, #910, #28810, #51828, #58255, #40882, #23896, #57879, #46905, #68428, #174, #63888, #6186, #11838, #29195, #23150, #46163, #16731, #69180, #17491, #39757, #62392, #62759, #40510, #69554, #6556, #52207, #11102, #63514, #29562, #34873, #34125, #56754, #540, #16355, #23522, #46536, #39393, #10719, #57125, #5440, #28442, #51448, #22769, #31033, #42719, #7293, #19706, #64990, #25362, #31407, #48379, #41979, #13299, #64635, #1644, #36705, #54434, #18612, #36337, #24258, #70658, #47271, #70297, #2000, #59352, #59717, #35968, #7663, #18975, #53320, #2742, #41623, #65732, #42349, #65366, #30669, #12571, #24990, #25728, #30301, #54058, #53689, #12932, #24625, #48007, #47636, #58988, #71020, #19337, #2367, #71382, #13665, #14034, #69929, #8025, #37071, #60074, #8393, #6921, #18239, #41254, #64263, #35600, #58615, #29932, #52948, #1281, #43848, #49504, #49881, #72135, #61943, #43088, #15169, #37447, #66105, #9533, #54807, #38199, #66861, #15538, #21575, #27233, #32164, #44601, #38579, #73271, #31787, #50249, #14415, #67614, #10271, #61202, #3118, #55185, #26103, #3491, #33298, #32548, #55558, #20831, #3871, #15911, #72896, #14787, #20072, #61579, #60824, #37827, #26479, #38942, #9147, #55934, #71758, #49123, #20448, #43465, #21204, #26867, #44231, #72523, #67242, #60445, #9898, #56296, #32928, #4245, #4612, #66479, #48749, #8775, #5356 ) ),
 .UNSPECIFIED., .F., .F., .F. ) 
 B_SPLINE_SURFACE_WITH_KNOTS ( ( 2, 2 ),
 ( 3, 2, 2, 2, 2, 2, 2, 2, 2, 2, 2, 2, 2, 2, 2, 2, 2, 2, 2, 2, 2, 2, 2, 2, 2, 2, 2, 2, 2, 2, 2, 2, 2, 2, 2, 2, 2, 2, 2, 2, 2, 2, 2, 2, 2, 2, 2, 2, 2, 2, 2, 2, 2, 2, 2, 2, 2, 2, 2, 2, 2, 2, 2, 2, 2, 2, 2, 2, 2, 2, 2, 2, 2, 2, 2, 2, 2, 2, 2, 2, 2, 2, 2, 2, 2, 2, 2, 2, 2, 2, 2, 2, 2, 2, 2, 2, 2, 2, 2, 2, 2, 2, 2, 2, 2, 2, 2, 2, 2, 2, 2, 2, 2, 2, 2, 2, 2, 2, 2, 2, 2, 2, 2, 2, 2, 2, 2, 2, 2, 2, 2, 2, 2, 2, 2, 2, 2, 2, 2, 2, 2, 2, 2, 2, 2, 2, 2, 2, 2, 2, 2, 2, 2, 2, 2, 2, 2, 2, 2, 2, 2, 2, 2, 2, 2, 2, 2, 2, 2, 2, 2, 2, 2, 2, 2, 2, 3 ),
 ( 0.000000000000000000, 1.000000000000000000 ),
 ( 0.000000000000000000, 0.005681818181818181976, 0.01136363636363636395, 0.01704545454545454419, 0.02272727272727272790, 0.02840909090909090814, 0.03409090909090908839, 0.03977272727272727210, 0.04545454545454545581, 0.05113636363636363952, 0.05681818181818181629, 0.06250000000000000000, 0.06818181818181817677, 0.07386363636363636742, 0.07954545454545454419, 0.08522727272727272096, 0.09090909090909091161, 0.09659090909090908839, 0.1022727272727272790, 0.1079545454545454558, 0.1136363636363636326, 0.1193181818181818232, 0.1250000000000000000, 0.1306818181818181768, 0.1363636363636363535, 0.1420454545454545581, 0.1477272727272727348, 0.1534090909090909116, 0.1590909090909090884, 0.1647727272727272652, 0.1704545454545454419, 0.1761363636363636465, 0.1818181818181818232, 0.1875000000000000000, 0.1931818181818181768, 0.1988636363636363535, 0.2045454545454545581, 0.2102272727272727348, 0.2159090909090909116, 0.2215909090909090884, 0.2272727272727272652, 0.2329545454545454419, 0.2386363636363636465, 0.2443181818181818232, 0.2500000000000000000, 0.2556818181818181768, 0.2613636363636363535, 0.2670454545454545303, 0.2727272727272727071, 0.2784090909090908839, 0.2840909090909091161, 0.2897727272727272929, 0.2954545454545454697, 0.3011363636363636465, 0.3068181818181818232, 0.3125000000000000000, 0.3181818181818181768, 0.3238636363636363535, 0.3295454545454545303, 0.3352272727272727071, 0.3409090909090908839, 0.3465909090909091161, 0.3522727272727272929, 0.3579545454545454697, 0.3636363636363636465, 0.3693181818181818232, 0.3750000000000000000, 0.3806818181818181768, 0.3863636363636363535, 0.3920454545454545303, 0.3977272727272727071, 0.4034090909090908839, 0.4090909090909091161, 0.4147727272727272929, 0.4204545454545454697, 0.4261363636363636465, 0.4318181818181818232, 0.4375000000000000000, 0.4431818181818181768, 0.4488636363636363535, 0.4545454545454545303, 0.4602272727272727071, 0.4659090909090908839, 0.4715909090909091161, 0.4772727272727272929, 0.4829545454545454697, 0.4886363636363636465, 0.4943181818181818232, 0.5000000000000000000, 0.5056818181818182323, 0.5113636363636363535, 0.5170454545454545858, 0.5227272727272727071, 0.5284090909090909394, 0.5340909090909090606, 0.5397727272727272929, 0.5454545454545454142, 0.5511363636363636465, 0.5568181818181817677, 0.5625000000000000000, 0.5681818181818182323, 0.5738636363636363535, 0.5795454545454545858, 0.5852272727272727071, 0.5909090909090909394, 0.5965909090909090606, 0.6022727272727272929, 0.6079545454545454142, 0.6136363636363636465, 0.6193181818181817677, 0.6250000000000000000, 0.6306818181818182323, 0.6363636363636363535, 0.6420454545454545858, 0.6477272727272727071, 0.6534090909090909394, 0.6590909090909090606, 0.6647727272727272929, 0.6704545454545454142, 0.6761363636363636465, 0.6818181818181817677, 0.6875000000000000000, 0.6931818181818182323, 0.6988636363636363535, 0.7045454545454545858, 0.7102272727272727071, 0.7159090909090909394, 0.7215909090909090606, 0.7272727272727272929, 0.7329545454545454142, 0.7386363636363636465, 0.7443181818181817677, 0.7500000000000000000, 0.7556818181818182323, 0.7613636363636363535, 0.7670454545454545858, 0.7727272727272727071, 0.7784090909090909394, 0.7840909090909090606, 0.7897727272727272929, 0.7954545454545454142, 0.8011363636363636465, 0.8068181818181817677, 0.8125000000000000000, 0.8181818181818182323, 0.8238636363636363535, 0.8295454545454545858, 0.8352272727272727071, 0.8409090909090909394, 0.8465909090909090606, 0.8522727272727272929, 0.8579545454545454142, 0.8636363636363636465, 0.8693181818181817677, 0.8750000000000000000, 0.8806818181818182323, 0.8863636363636363535, 0.8920454545454545858, 0.8977272727272727071, 0.9034090909090909394, 0.9090909090909090606, 0.9147727272727272929, 0.9204545454545454142, 0.9261363636363636465, 0.9318181818181817677, 0.9375000000000000000, 0.9431818181818182323, 0.9488636363636363535, 0.9545454545454545858, 0.9602272727272727071, 0.9659090909090909394, 0.9715909090909090606, 0.9772727272727272929, 0.9829545454545454142, 0.9886363636363636465, 0.9943181818181817677, 1.000000000000000000 ),
 .UNSPECIFIED. ) 
 GEOMETRIC_REPRESENTATION_ITEM ( )  RATIONAL_B_SPLINE_SURFACE ( (
 ( 1.000000000000000000, 0.9238795325112867385, 1.000000000000000000, 0.9238795325112867385, 1.000000000000000000, 0.9238795325112867385, 1.000000000000000000, 0.9238795325112867385, 1.000000000000000000, 0.9238795325112867385, 1.000000000000000000, 0.9238795325112867385, 1.000000000000000000, 0.9238795325112867385, 1.000000000000000000, 0.9238795325112867385, 1.000000000000000000, 0.9238795325112867385, 1.000000000000000000, 0.9238795325112867385, 1.000000000000000000, 0.9238795325112867385, 1.000000000000000000, 0.9238795325112867385, 1.000000000000000000, 0.9238795325112867385, 1.000000000000000000, 0.9238795325112867385, 1.000000000000000000, 0.9238795325112867385, 1.000000000000000000, 0.9238795325112867385, 1.000000000000000000, 0.9238795325112867385, 1.000000000000000000, 0.9238795325112867385, 1.000000000000000000, 0.9238795325112867385, 1.000000000000000000, 0.9238795325112867385, 1.000000000000000000, 0.9238795325112867385, 1.000000000000000000, 0.9238795325112867385, 1.000000000000000000, 0.9238795325112867385, 1.000000000000000000, 0.9238795325112867385, 1.000000000000000000, 0.9238795325112867385, 1.000000000000000000, 0.9238795325112867385, 1.000000000000000000, 0.9238795325112867385, 1.000000000000000000, 0.9238795325112867385, 1.000000000000000000, 0.9238795325112867385, 1.000000000000000000, 0.9238795325112867385, 1.000000000000000000, 0.9238795325112867385, 1.000000000000000000, 0.9238795325112867385, 1.000000000000000000, 0.9238795325112867385, 1.000000000000000000, 0.9238795325112867385, 1.000000000000000000, 0.9238795325112867385, 1.000000000000000000, 0.9238795325112867385, 1.000000000000000000, 0.9238795325112867385, 1.000000000000000000, 0.9238795325112867385, 1.000000000000000000, 0.9238795325112867385, 1.000000000000000000, 0.9238795325112867385, 1.000000000000000000, 0.9238795325112867385, 1.000000000000000000, 0.9238795325112867385, 1.000000000000000000, 0.9238795325112867385, 1.000000000000000000, 0.9238795325112867385, 1.000000000000000000, 0.9238795325112867385, 1.000000000000000000, 0.9238795325112867385, 1.000000000000000000, 0.9238795325112867385, 1.000000000000000000, 0.9238795325112867385, 1.000000000000000000, 0.9238795325112867385, 1.000000000000000000, 0.9238795325112867385, 1.000000000000000000, 0.9238795325112867385, 1.000000000000000000, 0.9238795325112867385, 1.000000000000000000, 0.9238795325112867385, 1.000000000000000000, 0.9238795325112867385, 1.000000000000000000, 0.9238795325112867385, 1.000000000000000000, 0.9238795325112867385, 1.000000000000000000, 0.9238795325112867385, 1.000000000000000000, 0.9238795325112867385, 1.000000000000000000, 0.9238795325112867385, 1.000000000000000000, 0.9238795325112867385, 1.000000000000000000, 0.9238795325112867385, 1.000000000000000000, 0.9238795325112867385, 1.000000000000000000, 0.9238795325112867385, 1.000000000000000000, 0.9238795325112867385, 1.000000000000000000, 0.9238795325112867385, 1.000000000000000000, 0.9238795325112867385, 1.000000000000000000, 0.9238795325112867385, 1.000000000000000000, 0.9238795325112867385, 1.000000000000000000, 0.9238795325112867385, 1.000000000000000000, 0.9238795325112867385, 1.000000000000000000, 0.9238795325112867385, 1.000000000000000000, 0.9238795325112867385, 1.000000000000000000, 0.9238795325112867385, 1.000000000000000000, 0.9238795325112867385, 1.000000000000000000, 0.9238795325112867385, 1.000000000000000000, 0.9238795325112867385, 1.000000000000000000, 0.9238795325112867385, 1.000000000000000000, 0.9238795325112867385, 1.000000000000000000, 0.9238795325112867385, 1.000000000000000000, 0.9238795325112867385, 1.000000000000000000, 0.9238795325112867385, 1.000000000000000000, 0.9238795325112867385, 1.000000000000000000, 0.9238795325112867385, 1.000000000000000000, 0.9238795325112867385, 1.000000000000000000, 0.9238795325112867385, 1.000000000000000000, 0.9238795325112867385, 1.000000000000000000, 0.9238795325112867385, 1.000000000000000000, 0.9238795325112867385, 1.000000000000000000, 0.9238795325112867385, 1.000000000000000000, 0.9238795325112867385, 1.000000000000000000, 0.9238795325112867385, 1.000000000000000000, 0.9238795325112867385, 1.000000000000000000, 0.9238795325112867385, 1.000000000000000000, 0.9238795325112867385, 1.000000000000000000, 0.9238795325112867385, 1.000000000000000000, 0.9238795325112867385, 1.000000000000000000, 0.9238795325112867385, 1.000000000000000000, 0.9238795325112867385, 1.000000000000000000, 0.9238795325112867385, 1.000000000000000000, 0.9238795325112867385, 1.000000000000000000, 0.9238795325112867385, 1.000000000000000000, 0.9238795325112867385, 1.000000000000000000, 0.9238795325112867385, 1.000000000000000000, 0.9238795325112867385, 1.000000000000000000, 0.9238795325112867385, 1.000000000000000000, 0.9238795325112867385, 1.000000000000000000, 0.9238795325112867385, 1.000000000000000000, 0.9238795325112867385, 1.000000000000000000, 0.9238795325112867385, 1.000000000000000000, 0.9238795325112867385, 1.000000000000000000, 0.9238795325112867385, 1.000000000000000000, 0.9238795325112867385, 1.000000000000000000, 0.9238795325112867385, 1.000000000000000000, 0.9238795325112867385, 1.000000000000000000, 0.9238795325112867385, 1.000000000000000000, 0.9238795325112867385, 1.000000000000000000, 0.9238795325112867385, 1.000000000000000000, 0.9238795325112867385, 1.000000000000000000, 0.9238795325112867385, 1.000000000000000000, 0.9238795325112867385, 1.000000000000000000, 0.9238795325112867385, 1.000000000000000000, 0.9238795325112867385, 1.000000000000000000, 0.9238795325112867385, 1.000000000000000000, 0.9238795325112867385, 1.000000000000000000, 0.9238795325112867385, 1.000000000000000000, 0.9238795325112867385, 1.000000000000000000, 0.9238795325112867385, 1.000000000000000000, 0.9238795325112867385, 1.000000000000000000, 0.9238795325112867385, 1.000000000000000000, 0.9238795325112867385, 1.000000000000000000, 0.9238795325112867385, 1.000000000000000000, 0.9238795325112867385, 1.000000000000000000, 0.9238795325112867385, 1.000000000000000000, 0.9238795325112867385, 1.000000000000000000, 0.9238795325112867385, 1.000000000000000000, 0.9238795325112867385, 1.000000000000000000, 0.9238795325112867385, 1.000000000000000000, 0.9238795325112867385, 1.000000000000000000, 0.9238795325112867385, 1.000000000000000000, 0.9238795325112867385, 1.000000000000000000, 0.9238795325112867385, 1.000000000000000000, 0.9238795325112867385, 1.000000000000000000, 0.9238795325112867385, 1.000000000000000000, 0.9238795325112867385, 1.000000000000000000, 0.9238795325112867385, 1.000000000000000000, 0.9238795325112867385, 1.000000000000000000, 0.9238795325112867385, 1.000000000000000000, 0.9238795325112867385, 1.000000000000000000, 0.9238795325112867385, 1.000000000000000000, 0.9238795325112867385, 1.000000000000000000, 0.9238795325112867385, 1.000000000000000000, 0.9238795325112867385, 1.000000000000000000, 0.9238795325112867385, 1.000000000000000000, 0.9238795325112867385, 1.000000000000000000, 0.9238795325112867385, 1.000000000000000000, 0.9238795325112867385, 1.000000000000000000, 0.9238795325112867385, 1.000000000000000000, 0.9238795325112867385, 1.000000000000000000, 0.9238795325112867385, 1.000000000000000000, 0.9238795325112867385, 1.000000000000000000, 0.9238795325112867385, 1.000000000000000000, 0.9238795325112867385, 1.000000000000000000, 0.9238795325112867385, 1.000000000000000000, 0.9238795325112867385, 1.000000000000000000, 0.9238795325112867385, 1.000000000000000000, 0.9238795325112867385, 1.000000000000000000, 0.9238795325112867385, 1.000000000000000000, 0.9238795325112867385, 1.000000000000000000, 0.9238795325112867385, 1.000000000000000000, 0.9238795325112867385, 1.000000000000000000, 0.9238795325112867385, 1.000000000000000000, 0.9238795325112867385, 1.000000000000000000, 0.9238795325112867385, 1.000000000000000000, 0.9238795325112867385, 1.000000000000000000, 0.9238795325112867385, 1.000000000000000000, 0.9238795325112867385, 1.000000000000000000),
 ( 1.000000000000000000, 0.9238795325112867385, 1.000000000000000000, 0.9238795325112867385, 1.000000000000000000, 0.9238795325112867385, 1.000000000000000000, 0.9238795325112867385, 1.000000000000000000, 0.9238795325112867385, 1.000000000000000000, 0.9238795325112867385, 1.000000000000000000, 0.9238795325112867385, 1.000000000000000000, 0.9238795325112867385, 1.000000000000000000, 0.9238795325112867385, 1.000000000000000000, 0.9238795325112867385, 1.000000000000000000, 0.9238795325112867385, 1.000000000000000000, 0.9238795325112867385, 1.000000000000000000, 0.9238795325112867385, 1.000000000000000000, 0.9238795325112867385, 1.000000000000000000, 0.9238795325112867385, 1.000000000000000000, 0.9238795325112867385, 1.000000000000000000, 0.9238795325112867385, 1.000000000000000000, 0.9238795325112867385, 1.000000000000000000, 0.9238795325112867385, 1.000000000000000000, 0.9238795325112867385, 1.000000000000000000, 0.9238795325112867385, 1.000000000000000000, 0.9238795325112867385, 1.000000000000000000, 0.9238795325112867385, 1.000000000000000000, 0.9238795325112867385, 1.000000000000000000, 0.9238795325112867385, 1.000000000000000000, 0.9238795325112867385, 1.000000000000000000, 0.9238795325112867385, 1.000000000000000000, 0.9238795325112867385, 1.000000000000000000, 0.9238795325112867385, 1.000000000000000000, 0.9238795325112867385, 1.000000000000000000, 0.9238795325112867385, 1.000000000000000000, 0.9238795325112867385, 1.000000000000000000, 0.9238795325112867385, 1.000000000000000000, 0.9238795325112867385, 1.000000000000000000, 0.9238795325112867385, 1.000000000000000000, 0.9238795325112867385, 1.000000000000000000, 0.9238795325112867385, 1.000000000000000000, 0.9238795325112867385, 1.000000000000000000, 0.9238795325112867385, 1.000000000000000000, 0.9238795325112867385, 1.000000000000000000, 0.9238795325112867385, 1.000000000000000000, 0.9238795325112867385, 1.000000000000000000, 0.9238795325112867385, 1.000000000000000000, 0.9238795325112867385, 1.000000000000000000, 0.9238795325112867385, 1.000000000000000000, 0.9238795325112867385, 1.000000000000000000, 0.9238795325112867385, 1.000000000000000000, 0.9238795325112867385, 1.000000000000000000, 0.9238795325112867385, 1.000000000000000000, 0.9238795325112867385, 1.000000000000000000, 0.9238795325112867385, 1.000000000000000000, 0.9238795325112867385, 1.000000000000000000, 0.9238795325112867385, 1.000000000000000000, 0.9238795325112867385, 1.000000000000000000, 0.9238795325112867385, 1.000000000000000000, 0.9238795325112867385, 1.000000000000000000, 0.9238795325112867385, 1.000000000000000000, 0.9238795325112867385, 1.000000000000000000, 0.9238795325112867385, 1.000000000000000000, 0.9238795325112867385, 1.000000000000000000, 0.9238795325112867385, 1.000000000000000000, 0.9238795325112867385, 1.000000000000000000, 0.9238795325112867385, 1.000000000000000000, 0.9238795325112867385, 1.000000000000000000, 0.9238795325112867385, 1.000000000000000000, 0.9238795325112867385, 1.000000000000000000, 0.9238795325112867385, 1.000000000000000000, 0.9238795325112867385, 1.000000000000000000, 0.9238795325112867385, 1.000000000000000000, 0.9238795325112867385, 1.000000000000000000, 0.9238795325112867385, 1.000000000000000000, 0.9238795325112867385, 1.000000000000000000, 0.9238795325112867385, 1.000000000000000000, 0.9238795325112867385, 1.000000000000000000, 0.9238795325112867385, 1.000000000000000000, 0.9238795325112867385, 1.000000000000000000, 0.9238795325112867385, 1.000000000000000000, 0.9238795325112867385, 1.000000000000000000, 0.9238795325112867385, 1.000000000000000000, 0.9238795325112867385, 1.000000000000000000, 0.9238795325112867385, 1.000000000000000000, 0.9238795325112867385, 1.000000000000000000, 0.9238795325112867385, 1.000000000000000000, 0.9238795325112867385, 1.000000000000000000, 0.9238795325112867385, 1.000000000000000000, 0.9238795325112867385, 1.000000000000000000, 0.9238795325112867385, 1.000000000000000000, 0.9238795325112867385, 1.000000000000000000, 0.9238795325112867385, 1.000000000000000000, 0.9238795325112867385, 1.000000000000000000, 0.9238795325112867385, 1.000000000000000000, 0.9238795325112867385, 1.000000000000000000, 0.9238795325112867385, 1.000000000000000000, 0.9238795325112867385, 1.000000000000000000, 0.9238795325112867385, 1.000000000000000000, 0.9238795325112867385, 1.000000000000000000, 0.9238795325112867385, 1.000000000000000000, 0.9238795325112867385, 1.000000000000000000, 0.9238795325112867385, 1.000000000000000000, 0.9238795325112867385, 1.000000000000000000, 0.9238795325112867385, 1.000000000000000000, 0.9238795325112867385, 1.000000000000000000, 0.9238795325112867385, 1.000000000000000000, 0.9238795325112867385, 1.000000000000000000, 0.9238795325112867385, 1.000000000000000000, 0.9238795325112867385, 1.000000000000000000, 0.9238795325112867385, 1.000000000000000000, 0.9238795325112867385, 1.000000000000000000, 0.9238795325112867385, 1.000000000000000000, 0.9238795325112867385, 1.000000000000000000, 0.9238795325112867385, 1.000000000000000000, 0.9238795325112867385, 1.000000000000000000, 0.9238795325112867385, 1.000000000000000000, 0.9238795325112867385, 1.000000000000000000, 0.9238795325112867385, 1.000000000000000000, 0.9238795325112867385, 1.000000000000000000, 0.9238795325112867385, 1.000000000000000000, 0.9238795325112867385, 1.000000000000000000, 0.9238795325112867385, 1.000000000000000000, 0.9238795325112867385, 1.000000000000000000, 0.9238795325112867385, 1.000000000000000000, 0.9238795325112867385, 1.000000000000000000, 0.9238795325112867385, 1.000000000000000000, 0.9238795325112867385, 1.000000000000000000, 0.9238795325112867385, 1.000000000000000000, 0.9238795325112867385, 1.000000000000000000, 0.9238795325112867385, 1.000000000000000000, 0.9238795325112867385, 1.000000000000000000, 0.9238795325112867385, 1.000000000000000000, 0.9238795325112867385, 1.000000000000000000, 0.9238795325112867385, 1.000000000000000000, 0.9238795325112867385, 1.000000000000000000, 0.9238795325112867385, 1.000000000000000000, 0.9238795325112867385, 1.000000000000000000, 0.9238795325112867385, 1.000000000000000000, 0.9238795325112867385, 1.000000000000000000, 0.9238795325112867385, 1.000000000000000000, 0.9238795325112867385, 1.000000000000000000, 0.9238795325112867385, 1.000000000000000000, 0.9238795325112867385, 1.000000000000000000, 0.9238795325112867385, 1.000000000000000000, 0.9238795325112867385, 1.000000000000000000, 0.9238795325112867385, 1.000000000000000000, 0.9238795325112867385, 1.000000000000000000, 0.9238795325112867385, 1.000000000000000000, 0.9238795325112867385, 1.000000000000000000, 0.9238795325112867385, 1.000000000000000000, 0.9238795325112867385, 1.000000000000000000, 0.9238795325112867385, 1.000000000000000000, 0.9238795325112867385, 1.000000000000000000, 0.9238795325112867385, 1.000000000000000000, 0.9238795325112867385, 1.000000000000000000, 0.9238795325112867385, 1.000000000000000000, 0.9238795325112867385, 1.000000000000000000, 0.9238795325112867385, 1.000000000000000000, 0.9238795325112867385, 1.000000000000000000, 0.9238795325112867385, 1.000000000000000000, 0.9238795325112867385, 1.000000000000000000, 0.9238795325112867385, 1.000000000000000000, 0.9238795325112867385, 1.000000000000000000, 0.9238795325112867385, 1.000000000000000000, 0.9238795325112867385, 1.000000000000000000, 0.9238795325112867385, 1.000000000000000000, 0.9238795325112867385, 1.000000000000000000, 0.9238795325112867385, 1.000000000000000000, 0.9238795325112867385, 1.000000000000000000, 0.9238795325112867385, 1.000000000000000000, 0.9238795325112867385, 1.000000000000000000, 0.9238795325112867385, 1.000000000000000000, 0.9238795325112867385, 1.000000000000000000, 0.9238795325112867385, 1.000000000000000000, 0.9238795325112867385, 1.000000000000000000, 0.9238795325112867385, 1.000000000000000000, 0.9238795325112867385, 1.000000000000000000, 0.9238795325112867385, 1.000000000000000000, 0.9238795325112867385, 1.000000000000000000) ) ) 
 REPRESENTATION_ITEM ( '' )  SURFACE ( )  );
#17802=CARTESIAN_POINT ( 'NONE',  ( 1.881053915767121998, 11.62499999863440792, -4.541265875000002339 ) ) ;
#17811=CARTESIAN_POINT ( 'NONE',  ( 2.828427124746190291, 0.8750000000000002220, 2.828427124746192067 ) ) ;
#17812=CARTESIAN_POINT ( 'NONE',  ( -2.828427124746190735, 12.12499999726881406, -2.828427124746191623 ) ) ;
#17822=CARTESIAN_POINT ( 'NONE',  ( -1.881053915767121554, 10.62499999863440792, -4.541265875000002339 ) ) ;
#17823=CARTESIAN_POINT ( 'NONE',  ( -2.828427124746192067, 18.37499999726881583, 2.828427124746190735 ) ) ;
#17865=CARTESIAN_POINT ( 'NONE',  ( 4.541265875000002339, 11.43749999863440614, 0.000000000000000000 ) ) ;
#17892=( BOUNDED_CURVE ( )  B_SPLINE_CURVE ( 2, ( #31414, #9540, #3877, #20453, #54441, #55564, #15175, #43095, #49887 ),
 .UNSPECIFIED., .F., .F. ) 
 B_SPLINE_CURVE_WITH_KNOTS ( ( 3, 2, 2, 2, 3 ),
 ( 0.5113636363636363535, 0.5170454545454545858, 0.5227272727272727071, 0.5284090909090909394, 0.5340909090909090606 ),
 .UNSPECIFIED. ) 
 CURVE ( )  GEOMETRIC_REPRESENTATION_ITEM ( )  RATIONAL_B_SPLINE_CURVE ( ( 1.000000000000000000, 0.9238795325112867385, 1.000000000000000000, 0.9238795325112867385, 1.000000000000000000, 0.9238795325112867385, 1.000000000000000000, 0.9238795325112867385, 1.000000000000000000 ) ) 
 REPRESENTATION_ITEM ( '' )  );
#17896=CARTESIAN_POINT ( 'NONE',  ( 4.541265875000002339, 2.437499998634407028, 0.000000000000000000 ) ) ;
#17907=CARTESIAN_POINT ( 'NONE',  ( 3.211159895383561835, 20.56249999863440436, -3.211159895383561835 ) ) ;
#17955=CARTESIAN_POINT ( 'NONE',  ( -4.541265875000003227, 0.9999999986344068059, 1.881053915767121110 ) ) ;
#17971=CYLINDRICAL_SURFACE ( 'NONE', #1084, 4.000000000000001776 ) ;
#17983=LINE ( 'NONE', #658, #65202 ) ;
#17999=ADVANCED_FACE ( 'NONE', ( #16663 ), #21220, .T. ) ;
#18010=( BOUNDED_CURVE ( )  B_SPLINE_CURVE ( 2, ( #56474, #50796, #45504, #68522, #58343, #70388, #23982, #6647, #18329 ),
 .UNSPECIFIED., .F., .F. ) 
 B_SPLINE_CURVE_WITH_KNOTS ( ( 3, 2, 2, 2, 3 ),
 ( 0.05681818181818182323, 0.06250000000000000000, 0.06818181818181817677, 0.07386363636363636742, 0.07954545454545454419 ),
 .UNSPECIFIED. ) 
 CURVE ( )  GEOMETRIC_REPRESENTATION_ITEM ( )  RATIONAL_B_SPLINE_CURVE ( ( 0.9999999999999998890, 0.9238795325112868495, 1.000000000000000000, 0.9238795325112867385, 1.000000000000000000, 0.9238795325112867385, 1.000000000000000000, 0.9238795325112867385, 1.000000000000000000 ) ) 
 REPRESENTATION_ITEM ( '' )  );
#18013=ORIENTED_EDGE ( 'NONE', *, *, #40922, .T. ) ;
#18014=CARTESIAN_POINT ( 'NONE',  ( 1.656854249492381914, 2.562499997268814056, 4.000000000000000888 ) ) ;
#18025=( BOUNDED_CURVE ( )  B_SPLINE_CURVE ( 2, ( #4281, #27273, #61985, #50289, #73310, #10308, #56335, #4655, #70796 ),
 .UNSPECIFIED., .F., .F. ) 
 B_SPLINE_CURVE_WITH_KNOTS ( ( 3, 2, 2, 2, 3 ),
 ( 0.5340909090909090606, 0.5397727272727272929, 0.5454545454545454142, 0.5511363636363637575, 0.5568181818181818787 ),
 .UNSPECIFIED. ) 
 CURVE ( )  GEOMETRIC_REPRESENTATION_ITEM ( )  RATIONAL_B_SPLINE_CURVE ( ( 1.000000000000000000, 0.9238795325112867385, 1.000000000000000000, 0.9238795325112867385, 1.000000000000000000, 0.9238795325112867385, 1.000000000000000000, 0.9238795325112852952, 1.000000000000001554 ) ) 
 REPRESENTATION_ITEM ( '' )  );
#18048=CARTESIAN_POINT ( 'NONE',  ( -8.342170076843785083E-16, 9.062499998634407916, 4.541265875000002339 ) ) ;
#18072=CARTESIAN_POINT ( 'NONE',  ( 2.828427124746191623, 4.125000000000000000, -2.828427124746191623 ) ) ;
#18092=EDGE_CURVE ( 'NONE', #62884, #61795, #63713, .T. ) ;
#18094=CARTESIAN_POINT ( 'NONE',  ( -1.656854249492381248, 11.31249999999999822, -4.000000000000001776 ) ) ;
#18096=CARTESIAN_POINT ( 'NONE',  ( -4.541265875000002339, 10.74999999863440969, -1.881053915767121998 ) ) ;
#18104=CARTESIAN_POINT ( 'NONE',  ( 1.656854249492381248, 6.937499997268813168, -4.000000000000001776 ) ) ;
#18162=CARTESIAN_POINT ( 'NONE',  ( 1.656854249492381914, 14.56249999726881583, 4.000000000000000888 ) ) ;
#18177=CARTESIAN_POINT ( 'NONE',  ( 2.780723358947928197E-16, 17.68749999863440792, -4.541265875000002339 ) ) ;
#18186=CARTESIAN_POINT ( 'NONE',  ( 4.000000000000000888, 1.937500000000000222, 1.656854249492384135 ) ) ;
#18187=CARTESIAN_POINT ( 'NONE',  ( 4.000000000000001776, 12.81249999726881406, -1.656854249492381248 ) ) ;
#18196=CARTESIAN_POINT ( 'NONE',  ( 4.541265875000001451, 16.24999999863440436, 1.881053915767124440 ) ) ;
#18224=CARTESIAN_POINT ( 'NONE',  ( 4.541265875000002339, 1.312499998634406584, 0.000000000000000000 ) ) ;
#18239=CARTESIAN_POINT ( 'NONE',  ( -4.541265875000002339, 17.93749999863440792, -5.561446717895856393E-16 ) ) ;
#18254=ORIENTED_EDGE ( 'NONE', *, *, #58896, .T. ) ;
#18257=CARTESIAN_POINT ( 'NONE',  ( -4.000000000000001776, 17.50000000000000000, -4.898587196589415787E-16 ) ) ;
#18266=CARTESIAN_POINT ( 'NONE',  ( 4.541265875000002339, 5.499999998634407028, -1.881053915767121776 ) ) ;
#18274=APPLICATION_CONTEXT ( 'automotive_design' ) ;
#18279=CARTESIAN_POINT ( 'NONE',  ( -7.347880794884122694E-16, 2.499999997268813168, 4.000000000000001776 ) ) ;
#18292=FACE_OUTER_BOUND ( 'NONE', #14058, .T. ) ;
#18314=CARTESIAN_POINT ( 'NONE',  ( 0.000000000000000000, 0.000000000000000000, 0.000000000000000000 ) ) ;
#18326=CARTESIAN_POINT ( 'NONE',  ( 1.881053915767122664, 1.249999998634407028, 4.541265875000001451 ) ) ;
#18329=CARTESIAN_POINT ( 'NONE',  ( -7.347880794884122694E-16, 1.750000000000000222, 4.000000000000001776 ) ) ;
#18419=CARTESIAN_POINT ( 'NONE',  ( -8.342170076843785083E-16, 11.06249999863440792, 4.541265875000002339 ) ) ;
#18425=ORIENTED_EDGE ( 'NONE', *, *, #68470, .F. ) ;
#18463=CARTESIAN_POINT ( 'NONE',  ( 2.828427124746190291, 10.87500000000000178, 2.828427124746192067 ) ) ;
#18465=CARTESIAN_POINT ( 'NONE',  ( -1.881053915767124440, 10.99999999863440969, 4.541265875000001451 ) ) ;
#18474=ORIENTED_EDGE ( 'NONE', *, *, #255, .F. ) ;
#18513=EDGE_CURVE ( 'NONE', #57615, #11773, #37533, .T. ) ;
#18530=EDGE_LOOP ( 'NONE', ( #48855, #69847, #6252, #40946 ) ) ;
#18535=CARTESIAN_POINT ( 'NONE',  ( -4.000000000000001776, 16.18749999726881228, -1.656854249492381470 ) ) ;
#18537=FACE_OUTER_BOUND ( 'NONE', #43330, .T. ) ;
#18547=CARTESIAN_POINT ( 'NONE',  ( -4.541265875000002339, 16.87499999863440436, -1.881053915767121998 ) ) ;
#18552=CARTESIAN_POINT ( 'NONE',  ( 2.780723358947928197E-16, 1.687499998634406806, -4.541265875000002339 ) ) ;
#18557=CARTESIAN_POINT ( 'NONE',  ( 2.828427124746191623, 12.87499999726881406, -2.828427124746191623 ) ) ;
#18565=CARTESIAN_POINT ( 'NONE',  ( -1.881053915767124440, 14.99999999863440969, 4.541265875000001451 ) ) ;
#18566=CARTESIAN_POINT ( 'NONE',  ( 2.828427124746191623, 12.12500000000000000, -2.828427124746191623 ) ) ;
#18586=CARTESIAN_POINT ( 'NONE',  ( 4.000000000000001776, 8.000000000000000000, 0.000000000000000000 ) ) ;
#18593=CARTESIAN_POINT ( 'NONE',  ( -4.541265875000003227, 0.8749999986344069169, 1.881053915767121110 ) ) ;
#18596=CARTESIAN_POINT ( 'NONE',  ( 2.828427124746190291, 4.875000000000000000, 2.828427124746192067 ) ) ;
#18612=CARTESIAN_POINT ( 'NONE',  ( 3.211159895383560947, 15.31249999863440792, 3.211159895383562723 ) ) ;
#18639=CARTESIAN_POINT ( 'NONE',  ( 1.881053915767122664, 4.249999998634407028, 4.541265875000001451 ) ) ;
#18641=ADVANCED_FACE ( 'NONE', ( #16962 ), #53163, .T. ) ;
#18650=CARTESIAN_POINT ( 'NONE',  ( 2.828427124746191623, 1.874999997268813390, -2.828427124746191623 ) ) ;
#18656=CARTESIAN_POINT ( 'NONE',  ( -3.211159895383562723, 1.937499998634406806, 3.211159895383561391 ) ) ;
#18678=CARTESIAN_POINT ( 'NONE',  ( -2.828427124746192067, 17.37499999726881583, 2.828427124746190735 ) ) ;
#18700=CARTESIAN_POINT ( 'NONE',  ( -3.211159895383561391, 3.812499998634407028, -3.211159895383561835 ) ) ;
#18720=ORIENTED_EDGE ( 'NONE', *, *, #643, .F. ) ;
#18736=CARTESIAN_POINT ( 'NONE',  ( -0.01139559756449873805, 21.99999999999999645, 4.447709176919010687 ) ) ;
#18758=CARTESIAN_POINT ( 'NONE',  ( -1.388913554731741051, 22.00000000000001776, -3.856217111854652657 ) ) ;
#18762=CARTESIAN_POINT ( 'NONE',  ( -4.000000000000001776, 15.18749999726881406, -1.656854249492381470 ) ) ;
#18764=ORIENTED_EDGE ( 'NONE', *, *, #17707, .T. ) ;
#18791=CARTESIAN_POINT ( 'NONE',  ( 4.541265875000001451, 16.24999999863440436, 1.881053915767124440 ) ) ;
#18804=CARTESIAN_POINT ( 'NONE',  ( -7.347880794884122694E-16, 8.499999997268814056, 4.000000000000001776 ) ) ;
#18805=CARTESIAN_POINT ( 'NONE',  ( -4.000000000000001776, 13.24999999726881406, -4.898587196589415787E-16 ) ) ;
#18832=CARTESIAN_POINT ( 'NONE',  ( 1.656854249492381914, 12.81250000000000000, 4.000000000000000888 ) ) ;
#18834=CARTESIAN_POINT ( 'NONE',  ( 3.211159895383560947, 17.18749999863440792, 3.211159895383562723 ) ) ;
#18900=CARTESIAN_POINT ( 'NONE',  ( -4.000000000000001776, 16.24999999726881228, -4.898587196589415787E-16 ) ) ;
#18911=CARTESIAN_POINT ( 'NONE',  ( 2.780723358947928197E-16, 18.68749999863440436, -4.541265875000002339 ) ) ;
#18915=CARTESIAN_POINT ( 'NONE',  ( 2.780723358947928197E-16, 0.6874999986344068059, -4.541265875000002339 ) ) ;
#18921=CARTESIAN_POINT ( 'NONE',  ( 4.000000000000000888, 0.9375000000000001110, 1.656854249492384135 ) ) ;
#18922=CARTESIAN_POINT ( 'NONE',  ( -4.000000000000001776, 13.18749999726881583, -1.656854249492381470 ) ) ;
#18931=CARTESIAN_POINT ( 'NONE',  ( -4.541265875000002339, 12.74999999863440969, -1.881053915767121998 ) ) ;
#18953=CARTESIAN_POINT ( 'NONE',  ( -7.347880794884122694E-16, 3.499999997268812724, 4.000000000000001776 ) ) ;
#18959=CARTESIAN_POINT ( 'NONE',  ( 3.211159895383561835, 0.4374999986344066949, -3.211159895383561835 ) ) ;
#18971=CYLINDRICAL_SURFACE ( 'NONE', #17348, 4.000000000000001776 ) ;
#18975=CARTESIAN_POINT ( 'NONE',  ( -4.541265875000003227, 15.99999999863440614, 1.881053915767121110 ) ) ;
#18977=CARTESIAN_POINT ( 'NONE',  ( 2.828427124746191623, 10.87499999726881406, -2.828427124746191623 ) ) ;
#18999=CARTESIAN_POINT ( 'NONE',  ( 4.541265875000002339, 6.437499998634407028, 0.000000000000000000 ) ) ;
#19010=CARTESIAN_POINT ( 'NONE',  ( 4.000000000000001776, 3.749999997268813168, 0.000000000000000000 ) ) ;
#19017=CARTESIAN_POINT ( 'NONE',  ( -3.211159895383561391, 0.6874999986344068059, -3.211159895383561835 ) ) ;
#19041=DIRECTION ( 'NONE',  ( 0.000000000000000000, 0.000000000000000000, -1.000000000000000000 ) ) ;
#19046=DIRECTION ( 'NONE',  ( 0.000000000000000000, 0.000000000000000000, -1.000000000000000000 ) ) ;
#19061=CARTESIAN_POINT ( 'NONE',  ( -8.342170076843785083E-16, 6.187499998634407028, 4.541265875000002339 ) ) ;
#19089=ORIENTED_EDGE ( 'NONE', *, *, #35833, .F. ) ;
#19103=CARTESIAN_POINT ( 'NONE',  ( 1.881053915767121776, 13.62499999863440792, -4.541265875000002339 ) ) ;
#19104=EDGE_LOOP ( 'NONE', ( #25883, #20659, #6396, #2046 ) ) ;
#19114=CARTESIAN_POINT ( 'NONE',  ( -7.347880794884122694E-16, 19.75000000000000000, 4.000000000000001776 ) ) ;
#19119=CARTESIAN_POINT ( 'NONE',  ( -2.828427124746190735, 15.12499999726881406, -2.828427124746191623 ) ) ;
#19120=ORIENTED_EDGE ( 'NONE', *, *, #25130, .T. ) ;
#19147=CARTESIAN_POINT ( 'NONE',  ( -8.342170076843785083E-16, 14.06249999863440614, 4.541265875000002339 ) ) ;
#19180=CARTESIAN_POINT ( 'NONE',  ( 4.000000000000001776, 21.74999999726881583, 0.000000000000000000 ) ) ;
#19194=CARTESIAN_POINT ( 'NONE',  ( -4.000000000000002665, 13.56250000000000000, 1.656854249492380804 ) ) ;
#19195=( BOUNDED_CURVE ( )  B_SPLINE_CURVE ( 2, ( #67701, #55275, #49596, #9985, #72612, #43939, #33754, #73356, #9235 ),
 .UNSPECIFIED., .F., .F. ) 
 B_SPLINE_CURVE_WITH_KNOTS ( ( 3, 2, 2, 2, 3 ),
 ( 0.03409090909090908839, 0.03977272727272727210, 0.04545454545454545581, 0.05113636363636364646, 0.05681818181818182323 ),
 .UNSPECIFIED. ) 
 CURVE ( )  GEOMETRIC_REPRESENTATION_ITEM ( )  RATIONAL_B_SPLINE_CURVE ( ( 1.000000000000000000, 0.9238795325112867385, 1.000000000000000000, 0.9238795325112867385, 1.000000000000000000, 0.9238795325112867385, 1.000000000000000000, 0.9238795325112866275, 1.000000000000000000 ) ) 
 REPRESENTATION_ITEM ( '' )  );
#19196=CARTESIAN_POINT ( 'NONE',  ( -1.881053915767124440, 13.99999999863440792, 4.541265875000001451 ) ) ;
#19203=CARTESIAN_POINT ( 'NONE',  ( 4.000000000000001776, 6.749999997268813168, 0.000000000000000000 ) ) ;
#19210=ORIENTED_EDGE ( 'NONE', *, *, #1678, .F. ) ;
#19221=LINE ( 'NONE', #29815, #47039 ) ;
#19238=CARTESIAN_POINT ( 'NONE',  ( -1.656854249492381248, 8.062499997268814056, -4.000000000000001776 ) ) ;
#19248=AXIS2_PLACEMENT_3D ( 'NONE', #68318, #68687, #50963 ) ;
#19268=DIRECTION ( 'NONE',  ( -0.000000000000000000, -1.000000000000000000, -0.000000000000000000 ) ) ;
#19273=CARTESIAN_POINT ( 'NONE',  ( -4.541265875000003227, 16.99999999863440436, 1.881053915767121110 ) ) ;
#19282=CARTESIAN_POINT ( 'NONE',  ( 2.449293598294707893E-16, 13.99999999726881406, -4.000000000000001776 ) ) ;
#19283=CARTESIAN_POINT ( 'NONE',  ( -4.541265875000002339, 4.749999998634407028, -1.881053915767121998 ) ) ;
#19290=CARTESIAN_POINT ( 'NONE',  ( -4.541265875000003227, 14.87499999863441147, 1.881053915767121110 ) ) ;
#19295=ORIENTED_EDGE ( 'NONE', *, *, #32090, .T. ) ;
#19318=CARTESIAN_POINT ( 'NONE',  ( -3.211159895383561391, 0.6874999986344068059, -3.211159895383561835 ) ) ;
#19337=CARTESIAN_POINT ( 'NONE',  ( 1.881053915767122664, 17.24999999863440792, 4.541265875000001451 ) ) ;
#19360=CARTESIAN_POINT ( 'NONE',  ( 4.541265875000002339, 3.499999998634407028, -1.881053915767121776 ) ) ;
#19370=CARTESIAN_POINT ( 'NONE',  ( -1.656854249492381248, 2.062499997268813612, -4.000000000000001776 ) ) ;
#19376=CARTESIAN_POINT ( 'NONE',  ( 2.780723358947928197E-16, 3.562499998634407028, -4.541265875000002339 ) ) ;
#19398=CYLINDRICAL_SURFACE ( 'NONE', #19827, 4.000000000000001776 ) ;
#19401=CARTESIAN_POINT ( 'NONE',  ( 0.000000000000000000, 0.000000000000000000, -4.000000000000001776 ) ) ;
#19421=CARTESIAN_POINT ( 'NONE',  ( 4.541265875000001451, 4.374999998634407028, 1.881053915767124440 ) ) ;
#19454=CARTESIAN_POINT ( 'NONE',  ( 4.000000000000000888, 20.68749999726881583, 1.656854249492384135 ) ) ;
#19468=CARTESIAN_POINT ( 'NONE',  ( -8.342170076843785083E-16, 11.18749999863440792, 4.541265875000002339 ) ) ;
#19484=CARTESIAN_POINT ( 'NONE',  ( -7.347880794884122694E-16, 11.75000000000000000, 4.000000000000001776 ) ) ;
#19494=DIRECTION ( 'NONE',  ( 0.000000000000000000, 0.000000000000000000, -1.000000000000000000 ) ) ;
#19510=CARTESIAN_POINT ( 'NONE',  ( -3.211159895383562723, 12.93749999863440792, 3.211159895383561391 ) ) ;
#19528=CARTESIAN_POINT ( 'NONE',  ( 0.000000000000000000, 0.000000000000000000, 0.000000000000000000 ) ) ;
#19532=VECTOR ( 'NONE', #69607, 1000.000000000000000 ) ;
#19559=CARTESIAN_POINT ( 'NONE',  ( -7.347880794884122694E-16, 17.75000000000000355, 4.000000000000001776 ) ) ;
#19560=CARTESIAN_POINT ( 'NONE',  ( -1.881053915767124440, 14.99999999863440969, 4.541265875000001451 ) ) ;
#19567=DIRECTION ( 'NONE',  ( -0.000000000000000000, -1.000000000000000000, -0.000000000000000000 ) ) ;
#19573=EDGE_LOOP ( 'NONE', ( #6858, #67285, #39936, #8360 ) ) ;
#19589=CARTESIAN_POINT ( 'NONE',  ( 0.000000000000000000, 0.000000000000000000, 0.000000000000000000 ) ) ;
#19594=CARTESIAN_POINT ( 'NONE',  ( -1.656854249492405895, 12.31250000000000178, -3.999999999999976463 ) ) ;
#19606=CARTESIAN_POINT ( 'NONE',  ( 2.449293598294707893E-16, 7.999999997268813168, -4.000000000000001776 ) ) ;
#19611=CARTESIAN_POINT ( 'NONE',  ( 0.000000000000000000, 0.000000000000000000, -4.000000000000001776 ) ) ;
#19639=EDGE_CURVE ( 'NONE', #6173, #5243, #72961, .T. ) ;
#19641=CARTESIAN_POINT ( 'NONE',  ( -4.541265875000002339, 15.93749999863440436, -5.561446717895856393E-16 ) ) ;
#19645=CARTESIAN_POINT ( 'NONE',  ( -1.881053915767124440, 3.124999998634407472, 4.541265875000001451 ) ) ;
#19651=CARTESIAN_POINT ( 'NONE',  ( -4.000000000000001776, 2.500000000000000000, -4.898587196589415787E-16 ) ) ;
#19652=CARTESIAN_POINT ( 'NONE',  ( -1.656854249492383691, 14.43749999726881406, 4.000000000000000888 ) ) ;
#19653=CARTESIAN_POINT ( 'NONE',  ( 4.541265875000001451, 2.249999998634407028, 1.881053915767124440 ) ) ;
#19659=CARTESIAN_POINT ( 'NONE',  ( 2.780723358947928197E-16, 15.56249999863440614, -4.541265875000002339 ) ) ;
#19680=CARTESIAN_POINT ( 'NONE',  ( -2.828427124746192067, 5.625000000000000000, 2.828427124746190735 ) ) ;
#19690=CARTESIAN_POINT ( 'NONE',  ( -1.881053915767124440, 3.999999998634406140, 4.541265875000001451 ) ) ;
#19693=ORIENTED_EDGE ( 'NONE', *, *, #23459, .F. ) ;
#19697=CARTESIAN_POINT ( 'NONE',  ( 2.828427124746191623, 19.87499999726881228, -2.828427124746191623 ) ) ;
#19706=CARTESIAN_POINT ( 'NONE',  ( 1.881053915767121776, 14.62499999863440969, -4.541265875000002339 ) ) ;
#19733=CARTESIAN_POINT ( 'NONE',  ( 1.881053915767122664, 3.249999998634407472, 4.541265875000001451 ) ) ;
#19745=CARTESIAN_POINT ( 'NONE',  ( 2.828427124746190291, 8.875000000000001776, 2.828427124746192067 ) ) ;
#19746=CARTESIAN_POINT ( 'NONE',  ( -4.000000000000001776, 4.249999997268813168, -4.898587196589415787E-16 ) ) ;
#19751=CARTESIAN_POINT ( 'NONE',  ( 4.541265875000002339, 3.374999998634406584, -1.881053915767121554 ) ) ;
#19755=ORIENTED_EDGE ( 'NONE', *, *, #18513, .F. ) ;
#19772=CARTESIAN_POINT ( 'NONE',  ( -2.828427124746190735, 17.12499999726881583, -2.828427124746191623 ) ) ;
#19794=CARTESIAN_POINT ( 'NONE',  ( -1.881053915767121554, 3.749999998634407028, -4.541265875000002339 ) ) ;
#19801=CIRCLE ( 'NONE', #42843, 8.000000000000003553 ) ;
#19827=AXIS2_PLACEMENT_3D ( 'NONE', #2434, #25427, #19041 ) ;
#19837=CARTESIAN_POINT ( 'NONE',  ( -1.881053915767124440, 11.12499999863440792, 4.541265875000001451 ) ) ;
#19854=CARTESIAN_POINT ( 'NONE',  ( -2.644300734200176084, 21.99999999999999289, -3.253854384680795242 ) ) ;
#19860=CARTESIAN_POINT ( 'NONE',  ( -2.828427124746190735, 2.124999997268813168, -2.828427124746191623 ) ) ;
#19861=CARTESIAN_POINT ( 'NONE',  ( -2.828427124746192067, 9.374999997268814056, 2.828427124746190735 ) ) ;
#19881=DIRECTION ( 'NONE',  ( -0.000000000000000000, -1.000000000000000000, -0.000000000000000000 ) ) ;
#19882=CARTESIAN_POINT ( 'NONE',  ( -3.211159895383562723, 15.93749999863440436, 3.211159895383561391 ) ) ;
#19900=CIRCLE ( 'NONE', #37960, 4.000000000000000000 ) ;
#19927=CARTESIAN_POINT ( 'NONE',  ( -4.000000000000001776, 16.50000000000000000, -4.898587196589415787E-16 ) ) ;
#19928=CARTESIAN_POINT ( 'NONE',  ( 1.881053915767122664, 16.12499999863440436, 4.541265875000001451 ) ) ;
#19942=AXIS2_PLACEMENT_3D ( 'NONE', #40558, #221, #6604 ) ;
#19970=CARTESIAN_POINT ( 'NONE',  ( 4.898587196589415787E-16, 0.000000000000000000, 4.000000000000001776 ) ) ;
#19972=CARTESIAN_POINT ( 'NONE',  ( -2.828427124746192067, 6.625000000000000000, 2.828427124746190735 ) ) ;
#19996=CARTESIAN_POINT ( 'NONE',  ( 2.449293598294707893E-16, 8.250000000000000000, -4.000000000000001776 ) ) ;
#20011=CARTESIAN_POINT ( 'NONE',  ( 2.780723358947928197E-16, 4.687499998634407028, -4.541265875000002339 ) ) ;
#20018=CARTESIAN_POINT ( 'NONE',  ( 1.656854249492381248, 2.187500000000000444, -4.000000000000001776 ) ) ;
#20019=CARTESIAN_POINT ( 'NONE',  ( -4.000000000000001776, 19.24999999726881228, -4.898587196589415787E-16 ) ) ;
#20020=CARTESIAN_POINT ( 'NONE',  ( 2.780723358947928197E-16, 3.562499998634407028, -4.541265875000002339 ) ) ;
#20026=CARTESIAN_POINT ( 'NONE',  ( -3.211159895383562723, 18.93749999863440436, 3.211159895383561391 ) ) ;
#20046=CARTESIAN_POINT ( 'NONE',  ( 2.449293598294707893E-16, 0.9999999972688131678, -4.000000000000001776 ) ) ;
#20053=CARTESIAN_POINT ( 'NONE',  ( 4.541265875000002339, 8.312499998634407916, 0.000000000000000000 ) ) ;
#20072=CARTESIAN_POINT ( 'NONE',  ( -3.211159895383561391, 20.81249999863440436, -3.211159895383561835 ) ) ;
#20098=CARTESIAN_POINT ( 'NONE',  ( 2.780723358947928197E-16, 10.68749999863440792, -4.541265875000002339 ) ) ;
#20113=CARTESIAN_POINT ( 'NONE',  ( 4.000000000000000888, 5.687499997268812280, 1.656854249492384135 ) ) ;
#20118=CARTESIAN_POINT ( 'NONE',  ( 1.881053915767121776, 4.499999998634407028, -4.541265875000002339 ) ) ;
#20123=CARTESIAN_POINT ( 'NONE',  ( -2.828427124746192067, 21.62500000000000355, 2.828427124746190735 ) ) ;
#20146=FACE_OUTER_BOUND ( 'NONE', #8167, .T. ) ;
#20159=CARTESIAN_POINT ( 'NONE',  ( -4.541265875000003227, 4.999999998634406140, 1.881053915767121110 ) ) ;
#20178=( BOUNDED_CURVE ( )  B_SPLINE_CURVE ( 2, ( #14832, #15583, #27278, #67284, #9578, #71805, #20123, #20493, #15212 ),
 .UNSPECIFIED., .F., .F. ) 
 B_SPLINE_CURVE_WITH_KNOTS ( ( 3, 2, 2, 2, 3 ),
 ( 0.9659090909090909394, 0.9715909090909090606, 0.9772727272727272929, 0.9829545454545454142, 0.9886363636363636465 ),
 .UNSPECIFIED. ) 
 CURVE ( )  GEOMETRIC_REPRESENTATION_ITEM ( )  RATIONAL_B_SPLINE_CURVE ( ( 1.000000000000000000, 0.9238795325112867385, 1.000000000000000000, 0.9238795325112867385, 1.000000000000000000, 0.9238795325112867385, 1.000000000000000000, 0.9238795325112867385, 1.000000000000000000 ) ) 
 REPRESENTATION_ITEM ( '' )  );
#20188=CARTESIAN_POINT ( 'NONE',  ( 0.000000000000000000, 0.000000000000000000, -4.000000000000001776 ) ) ;
#20203=CARTESIAN_POINT ( 'NONE',  ( 1.881053915767122664, 12.24999999863440969, 4.541265875000001451 ) ) ;
#20214=CARTESIAN_POINT ( 'NONE',  ( 1.656854249492381914, 19.81250000000000000, 4.000000000000000888 ) ) ;
#20230=DIRECTION ( 'NONE',  ( -0.000000000000000000, -1.000000000000000000, -0.000000000000000000 ) ) ;
#20247=CARTESIAN_POINT ( 'NONE',  ( -1.881053915767124440, 13.99999999863440792, 4.541265875000001451 ) ) ;
#20280=CARTESIAN_POINT ( 'NONE',  ( -4.000000000000002665, 19.56250000000000000, 1.656854249492380582 ) ) ;
#20297=CARTESIAN_POINT ( 'NONE',  ( 2.828427124746190291, 15.87500000000000000, 2.828427124746192067 ) ) ;
#20298=CARTESIAN_POINT ( 'NONE',  ( -1.881053915767121776, 14.62499999863440969, -4.541265875000002339 ) ) ;
#20349=DIRECTION ( 'NONE',  ( -0.000000000000000000, -1.000000000000000000, -0.000000000000000000 ) ) ;
#20353=CARTESIAN_POINT ( 'NONE',  ( -7.347880794884122694E-16, 5.499999997268813168, 4.000000000000001776 ) ) ;
#20381=CARTESIAN_POINT ( 'NONE',  ( -1.881053915767121776, 20.74999999863440436, -4.541265875000002339 ) ) ;
#20384=CARTESIAN_POINT ( 'NONE',  ( -1.881053915767124440, 4.124999998634407028, 4.541265875000001451 ) ) ;
#20393=CARTESIAN_POINT ( 'NONE',  ( -1.656854249492381248, 3.312500000000000000, -4.000000000000001776 ) ) ;
#20394=CARTESIAN_POINT ( 'NONE',  ( 2.828427124746190291, 16.62499999726881583, 2.828427124746192067 ) ) ;
#20395=CARTESIAN_POINT ( 'NONE',  ( 1.881053915767122664, 4.124999998634407028, 4.541265875000001451 ) ) ;
#20401=CARTESIAN_POINT ( 'NONE',  ( 3.211159895383560947, 19.18749999863440436, 3.211159895383562723 ) ) ;
#20430=CARTESIAN_POINT ( 'NONE',  ( 1.881053915767121776, 4.499999998634407028, -4.541265875000002339 ) ) ;
#20448=CARTESIAN_POINT ( 'NONE',  ( 4.541265875000002339, 21.43749999863440792, 0.000000000000000000 ) ) ;
#20453=CARTESIAN_POINT ( 'NONE',  ( -4.000000000000001776, 12.18749999726881406, -1.656854249492381470 ) ) ;
#20468=CARTESIAN_POINT ( 'NONE',  ( 3.211159895383561835, 10.56249999863440792, -3.211159895383561835 ) ) ;
#20469=ORIENTED_EDGE ( 'NONE', *, *, #16870, .T. ) ;
#20480=CARTESIAN_POINT ( 'NONE',  ( -7.347880794884122694E-16, 7.499999997268813168, 4.000000000000001776 ) ) ;
#20486=CARTESIAN_POINT ( 'NONE',  ( 3.211159895383561835, 7.437499998634407028, -3.211159895383561835 ) ) ;
#20491=ORIENTED_EDGE ( 'NONE', *, *, #44850, .F. ) ;
#20493=CARTESIAN_POINT ( 'NONE',  ( -1.656854249492383468, 21.68750000000000355, 4.000000000000000888 ) ) ;
#20496=DIRECTION ( 'NONE',  ( 0.000000000000000000, 0.000000000000000000, -1.000000000000000000 ) ) ;
#20529=CARTESIAN_POINT ( 'NONE',  ( 4.898587196589415787E-16, 0.000000000000000000, 4.000000000000001776 ) ) ;
#20535=CARTESIAN_POINT ( 'NONE',  ( -4.541265875000002339, 7.874999998634407028, -1.881053915767121998 ) ) ;
#20541=ORIENTED_EDGE ( 'NONE', *, *, #33953, .F. ) ;
#20567=LINE ( 'NONE', #20188, #4296 ) ;
#20568=ADVANCED_FACE ( 'NONE', ( #28495 ), #68118, .T. ) ;
#20583=CARTESIAN_POINT ( 'NONE',  ( 4.541265875000001451, 15.37499999863440969, 1.881053915767124440 ) ) ;
#20589=EDGE_LOOP ( 'NONE', ( #31363, #40735, #13, #57205 ) ) ;
#20621=DIRECTION ( 'NONE',  ( -0.000000000000000000, -1.000000000000000000, -0.000000000000000000 ) ) ;
#20629=CARTESIAN_POINT ( 'NONE',  ( -3.211159895383562723, 19.93749999863440436, 3.211159895383561391 ) ) ;
#20651=CARTESIAN_POINT ( 'NONE',  ( 4.000000000000000888, 14.93750000000000178, 1.656854249492384135 ) ) ;
#20659=ORIENTED_EDGE ( 'NONE', *, *, #17046, .T. ) ;
#20661=CARTESIAN_POINT ( 'NONE',  ( 1.656854249492381914, 3.562499997268812724, 4.000000000000000888 ) ) ;
#20678=CARTESIAN_POINT ( 'NONE',  ( -1.656854249492383691, 16.68750000000000355, 4.000000000000000888 ) ) ;
#20679=CARTESIAN_POINT ( 'NONE',  ( 2.780723358947928197E-16, 19.56249999863440436, -4.541265875000002339 ) ) ;
#20762=CARTESIAN_POINT ( 'NONE',  ( 3.211159895383561835, 20.56249999863440436, -3.211159895383561835 ) ) ;
#20765=CARTESIAN_POINT ( 'NONE',  ( 1.881053915767122664, 4.249999998634406140, 4.541265875000001451 ) ) ;
#20772=CARTESIAN_POINT ( 'NONE',  ( 1.656854249492381248, 4.187500000000000000, -4.000000000000001776 ) ) ;
#20773=CARTESIAN_POINT ( 'NONE',  ( -4.000000000000002665, 16.31249999726881228, 1.656854249492380804 ) ) ;
#20774=CARTESIAN_POINT ( 'NONE',  ( 3.211159895383560947, 4.187499998634407028, 3.211159895383562723 ) ) ;
#20780=CARTESIAN_POINT ( 'NONE',  ( 3.211159895383560947, 17.18749999863440792, 3.211159895383562723 ) ) ;
#20793=VECTOR ( 'NONE', #52140, 1000.000000000000000 ) ;
#20794=EDGE_CURVE ( 'NONE', #43772, #13303, #58666, .T. ) ;
#20803=DIRECTION ( 'NONE',  ( -0.000000000000000000, -1.000000000000000000, -0.000000000000000000 ) ) ;
#20813=CARTESIAN_POINT ( 'NONE',  ( -4.541265875000002339, 6.812499998634407028, -5.561446717895856393E-16 ) ) ;
#20822=ADVANCED_FACE ( 'NONE', ( #18292 ), #12621, .T. ) ;
#20831=CARTESIAN_POINT ( 'NONE',  ( 4.541265875000002339, 20.49999999863440436, -1.881053915767121554 ) ) ;
#20853=CARTESIAN_POINT ( 'NONE',  ( 2.780723358947928197E-16, 8.687499998634407916, -4.541265875000002339 ) ) ;
#20863=CARTESIAN_POINT ( 'NONE',  ( 1.656854249492381248, 5.937499997268813168, -4.000000000000001776 ) ) ;
#20869=CARTESIAN_POINT ( 'NONE',  ( 3.211159895383560947, 5.187499998634407028, 3.211159895383562723 ) ) ;
#20914=CARTESIAN_POINT ( 'NONE',  ( 4.541265875000002339, 7.437499998634407028, 0.000000000000000000 ) ) ;
#20919=EDGE_LOOP ( 'NONE', ( #50690, #57906, #32409, #72159 ) ) ;
#20957=CARTESIAN_POINT ( 'NONE',  ( -3.211159895383561391, 15.81249999863440436, -3.211159895383561835 ) ) ;
#20964=ORIENTED_EDGE ( 'NONE', *, *, #35755, .F. ) ;
#20965=ADVANCED_FACE ( 'NONE', ( #32215 ), #72573, .T. ) ;
#21001=CARTESIAN_POINT ( 'NONE',  ( -1.881053915767124440, 18.99999999863440436, 4.541265875000001451 ) ) ;
#21041=CARTESIAN_POINT ( 'NONE',  ( -2.828427124746192067, 20.62500000000000000, 2.828427124746190735 ) ) ;
#21054=EDGE_CURVE ( 'NONE', #9782, #23983, #49822, .T. ) ;
#21055=CARTESIAN_POINT ( 'NONE',  ( 2.828427124746191623, 15.12500000000000000, -2.828427124746191623 ) ) ;
#21056=CARTESIAN_POINT ( 'NONE',  ( -4.541265875000003227, 18.87499999863441147, 1.881053915767121110 ) ) ;
#21070=ORIENTED_EDGE ( 'NONE', *, *, #5757, .T. ) ;
#21136=CARTESIAN_POINT ( 'NONE',  ( -4.541265875000003227, 18.99999999863440436, 1.881053915767121110 ) ) ;
#21139=CARTESIAN_POINT ( 'NONE',  ( 4.541265875000001451, 2.374999998634407028, 1.881053915767124440 ) ) ;
#21147=CARTESIAN_POINT ( 'NONE',  ( 4.000000000000001776, 6.062500000000000000, -1.656854249492381248 ) ) ;
#21148=CARTESIAN_POINT ( 'NONE',  ( -4.000000000000001776, 19.18749999726881228, -1.656854249492381470 ) ) ;
#21149=CARTESIAN_POINT ( 'NONE',  ( 1.881053915767121998, 6.499999998634407916, -4.541265875000002339 ) ) ;
#21154=CARTESIAN_POINT ( 'NONE',  ( 4.541265875000002339, 18.31249999863440792, 0.000000000000000000 ) ) ;
#21170=VERTEX_POINT ( 'NONE', #15960 ) ;
#21186=CARTESIAN_POINT ( 'NONE',  ( -3.211159895383561391, 4.687499998634407028, -3.211159895383561835 ) ) ;
#21204=CARTESIAN_POINT ( 'NONE',  ( 3.211159895383561835, 21.56249999863440792, -3.211159895383561835 ) ) ;
#21220=CYLINDRICAL_SURFACE ( 'NONE', #7379, 4.000000000000001776 ) ;
#21227=CARTESIAN_POINT ( 'NONE',  ( -8.342170076843785083E-16, 9.187499998634407916, 4.541265875000002339 ) ) ;
#21237=CARTESIAN_POINT ( 'NONE',  ( 1.656854249492381914, 5.562499997268813168, 4.000000000000000888 ) ) ;
#21245=CARTESIAN_POINT ( 'NONE',  ( -4.541265875000003227, 6.874999998634407916, 1.881053915767121110 ) ) ;
#21286=CARTESIAN_POINT ( 'NONE',  ( -4.541265875000003227, 6.999999998634407916, 1.881053915767121110 ) ) ;
#21334=CARTESIAN_POINT ( 'NONE',  ( 1.881053915767121776, 17.62499999863440436, -4.541265875000002339 ) ) ;
#21373=CARTESIAN_POINT ( 'NONE',  ( -1.881053915767124440, 17.99999999863440436, 4.541265875000001451 ) ) ;
#21397=CARTESIAN_POINT ( 'NONE',  ( 2.828427124746191623, 15.12500000000000000, -2.828427124746191623 ) ) ;
#21428=CARTESIAN_POINT ( 'NONE',  ( -1.656854249492381248, 18.31249999999999645, -4.000000000000001776 ) ) ;
#21429=CARTESIAN_POINT ( 'NONE',  ( 4.541265875000001451, 19.24999999863440436, 1.881053915767124440 ) ) ;
#21451=CARTESIAN_POINT ( 'NONE',  ( 1.656854249492381914, 13.81250000000000000, 4.000000000000000888 ) ) ;
#21510=CARTESIAN_POINT ( 'NONE',  ( -4.541265875000002339, 20.87499999863440792, -1.881053915767121998 ) ) ;
#21513=CARTESIAN_POINT ( 'NONE',  ( 3.211159895383560947, 8.312499998634407916, 3.211159895383562723 ) ) ;
#21519=EDGE_CURVE ( 'NONE', #6173, #8238, #59676, .T. ) ;
#21521=CARTESIAN_POINT ( 'NONE',  ( 1.656854249492381248, 7.187500000000000000, -4.000000000000001776 ) ) ;
#21522=CARTESIAN_POINT ( 'NONE',  ( 4.000000000000001776, 19.81249999726881583, -1.656854249492381248 ) ) ;
#21523=CARTESIAN_POINT ( 'NONE',  ( -8.342170076843785083E-16, 6.062499998634407028, 4.541265875000002339 ) ) ;
#21528=CARTESIAN_POINT ( 'NONE',  ( -4.541265875000003227, 16.87499999863440436, 1.881053915767121110 ) ) ;
#21552=CARTESIAN_POINT ( 'NONE',  ( 2.449293598294707893E-16, 9.999999997268814056, -4.000000000000001776 ) ) ;
#21558=CARTESIAN_POINT ( 'NONE',  ( 2.780723358947928197E-16, 7.562499998634407028, -4.541265875000002339 ) ) ;
#21575=CARTESIAN_POINT ( 'NONE',  ( 3.211159895383560947, 19.31249999863440436, 3.211159895383562723 ) ) ;
#21585=CARTESIAN_POINT ( 'NONE',  ( -7.347880794884122694E-16, 3.750000000000000000, 4.000000000000001776 ) ) ;
#21596=CARTESIAN_POINT ( 'NONE',  ( -4.541265875000003227, 8.999999998634407916, 1.881053915767121110 ) ) ;
#21607=CARTESIAN_POINT ( 'NONE',  ( 2.828427124746191623, 7.874999997268813168, -2.828427124746191623 ) ) ;
#21613=CARTESIAN_POINT ( 'NONE',  ( 4.541265875000002339, 6.374999998634407028, -1.881053915767121554 ) ) ;
#21657=CARTESIAN_POINT ( 'NONE',  ( 1.881053915767122664, 7.249999998634408804, 4.541265875000001451 ) ) ;
#21699=CARTESIAN_POINT ( 'NONE',  ( 3.211159895383561835, 15.56249999863440614, -3.211159895383561835 ) ) ;
#21737=CARTESIAN_POINT ( 'NONE',  ( 4.000000000000001776, 2.000000000000000000, 0.000000000000000000 ) ) ;
#21743=CARTESIAN_POINT ( 'NONE',  ( 4.541265875000002339, 19.31249999863440436, 0.000000000000000000 ) ) ;
#21791=CARTESIAN_POINT ( 'NONE',  ( 2.449293598294707893E-16, 21.25000000000000000, -4.000000000000001776 ) ) ;
#21792=CARTESIAN_POINT ( 'NONE',  ( 1.881053915767121998, 20.49999999863440436, -4.541265875000002339 ) ) ;
#21836=CARTESIAN_POINT ( 'NONE',  ( 2.828427124746190291, 16.87500000000000000, 2.828427124746192067 ) ) ;
#21862=FACE_OUTER_BOUND ( 'NONE', #57963, .T. ) ;
#21881=CARTESIAN_POINT ( 'NONE',  ( 1.881053915767122664, 6.249999998634407916, 4.541265875000001451 ) ) ;
#21886=CARTESIAN_POINT ( 'NONE',  ( 2.828427124746190291, 8.875000000000001776, 2.828427124746192067 ) ) ;
#21887=CARTESIAN_POINT ( 'NONE',  ( 1.656854249492381914, 22.56249999726881583, 4.000000000000000888 ) ) ;
#21888=CARTESIAN_POINT ( 'NONE',  ( -3.211159895383562723, 6.937499998634407028, 3.211159895383561391 ) ) ;
#21894=CARTESIAN_POINT ( 'NONE',  ( 3.211159895383561835, 20.43749999863440436, -3.211159895383561835 ) ) ;
#21898=EDGE_CURVE ( 'NONE', #33515, #10305, #42105, .T. ) ;
#21940=AXIS2_PLACEMENT_3D ( 'NONE', #10087, #33125, #10827 ) ;
#21968=CARTESIAN_POINT ( 'NONE',  ( 1.881053915767121998, 13.62499999863440792, -4.541265875000002339 ) ) ;
#21978=CARTESIAN_POINT ( 'NONE',  ( 4.000000000000000888, 9.687499997268815832, 1.656854249492384135 ) ) ;
#21988=CARTESIAN_POINT ( 'NONE',  ( -4.541265875000003227, 8.874999998634407916, 1.881053915767121110 ) ) ;
#21989=CARTESIAN_POINT ( 'NONE',  ( 4.000000000000001776, 1.806524977843537691E-16, 0.000000000000000000 ) ) ;
#22029=CARTESIAN_POINT ( 'NONE',  ( 3.211159895383561835, 6.562499998634407028, -3.211159895383561835 ) ) ;
#22032=CARTESIAN_POINT ( 'NONE',  ( -1.656854249492381248, 5.062499997268813168, -4.000000000000001776 ) ) ;
#22055=CARTESIAN_POINT ( 'NONE',  ( -4.000000000000001776, 4.437500000000001776, -1.656854249492381470 ) ) ;
#22069=CARTESIAN_POINT ( 'NONE',  ( -1.881053915767121554, 14.74999999863440969, -4.541265875000002339 ) ) ;
#22114=CARTESIAN_POINT ( 'NONE',  ( 2.780723358947928197E-16, 16.56249999863440436, -4.541265875000002339 ) ) ;
#22120=CARTESIAN_POINT ( 'NONE',  ( 4.000000000000001776, 15.74999999726881406, 0.000000000000000000 ) ) ;
#22167=CARTESIAN_POINT ( 'NONE',  ( -2.828427124746192067, 20.62500000000000000, 2.828427124746190735 ) ) ;
#22168=CARTESIAN_POINT ( 'NONE',  ( 4.541265875000002339, 18.31249999863440792, 0.000000000000000000 ) ) ;
#22182=EDGE_LOOP ( 'NONE', ( #47322, #63893, #1045, #39839 ) ) ;
#22202=CARTESIAN_POINT ( 'NONE',  ( -7.347880794884122694E-16, 16.49999999726881228, 4.000000000000001776 ) ) ;
#22243=ORIENTED_EDGE ( 'NONE', *, *, #73874, .T. ) ;
#22246=CARTESIAN_POINT ( 'NONE',  ( -4.541265875000002339, 7.874999998634407028, -1.881053915767121998 ) ) ;
#22252=CARTESIAN_POINT ( 'NONE',  ( -4.000000000000002665, 6.562500000000000000, 1.656854249492380804 ) ) ;
#22254=CARTESIAN_POINT ( 'NONE',  ( -4.541265875000003227, 5.874999998634406140, 1.881053915767121110 ) ) ;
#22263=CARTESIAN_POINT ( 'NONE',  ( -3.211159895383561391, 21.68749999863440792, -3.211159895383561835 ) ) ;
#22269=ORIENTED_EDGE ( 'NONE', *, *, #50459, .T. ) ;
#22328=VERTEX_POINT ( 'NONE', #5140 ) ;
#22330=CARTESIAN_POINT ( 'NONE',  ( -4.541265875000003227, 11.99999999863440792, 1.881053915767121110 ) ) ;
#22340=CARTESIAN_POINT ( 'NONE',  ( 2.828427124746190291, 9.624999997268814056, 2.828427124746192067 ) ) ;
#22347=CARTESIAN_POINT ( 'NONE',  ( -3.211159895383561391, 10.68749999863440792, -3.211159895383561835 ) ) ;
#22392=CARTESIAN_POINT ( 'NONE',  ( 1.881053915767121776, 10.62499999863440792, -4.541265875000002339 ) ) ;
#22435=CARTESIAN_POINT ( 'NONE',  ( -2.828427124746192067, 15.62500000000000000, 2.828427124746190735 ) ) ;
#22436=CARTESIAN_POINT ( 'NONE',  ( 1.881053915767121776, 18.62499999863440792, -4.541265875000002339 ) ) ;
#22480=CARTESIAN_POINT ( 'NONE',  ( -4.541265875000003227, 1.999999998634407250, 1.881053915767121110 ) ) ;
#22488=CARTESIAN_POINT ( 'NONE',  ( 2.449293598294707893E-16, 18.99999999726881228, -4.000000000000001776 ) ) ;
#22539=CARTESIAN_POINT ( 'NONE',  ( 4.000000000000001776, 19.00000000000000000, 0.000000000000000000 ) ) ;
#22576=CARTESIAN_POINT ( 'NONE',  ( 4.000000000000000888, 17.68749999726881583, 1.656854249492384135 ) ) ;
#22584=VECTOR ( 'NONE', #36698, 1000.000000000000000 ) ;
#22603=ORIENTED_EDGE ( 'NONE', *, *, #36731, .F. ) ;
#22622=CARTESIAN_POINT ( 'NONE',  ( 2.780723358947928197E-16, 6.687499998634407028, -4.541265875000002339 ) ) ;
#22626=CARTESIAN_POINT ( 'NONE',  ( -7.347880794884122694E-16, 6.750000000000000000, 4.000000000000001776 ) ) ;
#22628=CARTESIAN_POINT ( 'NONE',  ( -3.211159895383562723, 7.937499998634407028, 3.211159895383561391 ) ) ;
#22670=CARTESIAN_POINT ( 'NONE',  ( 2.828427124746190291, 11.62499999726881406, 2.828427124746192067 ) ) ;
#22709=CARTESIAN_POINT ( 'NONE',  ( -3.211159895383562723, 12.06249999863440614, 3.211159895383561391 ) ) ;
#22720=CARTESIAN_POINT ( 'NONE',  ( 1.656854249492381248, 8.937499997268814056, -4.000000000000001776 ) ) ;
#22722=CARTESIAN_POINT ( 'NONE',  ( 2.828427124746191623, 18.12500000000000000, -2.828427124746191623 ) ) ;
#22724=CYLINDRICAL_SURFACE ( 'NONE', #53922, 4.000000000000001776 ) ;
#22727=CARTESIAN_POINT ( 'NONE',  ( -8.342170076843785083E-16, 10.06249999863440614, 4.541265875000002339 ) ) ;
#22728=CARTESIAN_POINT ( 'NONE',  ( -4.000000000000001776, 18.24999999726881583, -4.898587196589415787E-16 ) ) ;
#22741=ORIENTED_EDGE ( 'NONE', *, *, #47564, .T. ) ;
#22769=CARTESIAN_POINT ( 'NONE',  ( 4.541265875000001451, 14.37499999863440969, 1.881053915767124440 ) ) ;
#22780=CARTESIAN_POINT ( 'NONE',  ( 1.656854249492381914, 6.812500000000000000, 4.000000000000000888 ) ) ;
#22810=ADVANCED_FACE ( 'NONE', ( #43524 ), #8837, .T. ) ;
#22815=CARTESIAN_POINT ( 'NONE',  ( -3.211159895383561391, 19.81249999863440436, -3.211159895383561835 ) ) ;
#22835=ORIENTED_EDGE ( 'NONE', *, *, #1502, .F. ) ;
#22865=CARTESIAN_POINT ( 'NONE',  ( -3.211159895383562723, 2.062499998634407028, 3.211159895383561391 ) ) ;
#22872=DIRECTION ( 'NONE',  ( -0.000000000000000000, -1.000000000000000000, -0.000000000000000000 ) ) ;
#22880=VECTOR ( 'NONE', #23968, 1000.000000000000000 ) ;
#22893=CARTESIAN_POINT ( 'NONE',  ( 2.828427124746190291, 5.875000000000000000, 2.828427124746192067 ) ) ;
#22908=ORIENTED_EDGE ( 'NONE', *, *, #66528, .F. ) ;
#22922=VERTEX_POINT ( 'NONE', #32228 ) ;
#22923=CARTESIAN_POINT ( 'NONE',  ( 2.449293598294707893E-16, 20.25000000000000000, -4.000000000000001776 ) ) ;
#22924=CARTESIAN_POINT ( 'NONE',  ( 1.656854249492381248, 2.937499997268813612, -4.000000000000001776 ) ) ;
#22940=ORIENTED_EDGE ( 'NONE', *, *, #21898, .F. ) ;
#22941=( BOUNDED_CURVE ( )  B_SPLINE_CURVE ( 2, ( #2567, #7490, #54629, #53512, #48201, #59907, #1831, #2938, #47832 ),
 .UNSPECIFIED., .F., .F. ) 
 B_SPLINE_CURVE_WITH_KNOTS ( ( 3, 2, 2, 2, 3 ),
 ( 0.5795454545454545858, 0.5852272727272727071, 0.5909090909090909394, 0.5965909090909090606, 0.6022727272727272929 ),
 .UNSPECIFIED. ) 
 CURVE ( )  GEOMETRIC_REPRESENTATION_ITEM ( )  RATIONAL_B_SPLINE_CURVE ( ( 1.000000000000000000, 0.9238795325112867385, 1.000000000000000000, 0.9238795325112867385, 1.000000000000000000, 0.9238795325112867385, 1.000000000000000000, 0.9238795325112867385, 1.000000000000000000 ) ) 
 REPRESENTATION_ITEM ( '' )  );
#22962=CARTESIAN_POINT ( 'NONE',  ( 1.656854249492381914, 16.56249999726881228, 4.000000000000000888 ) ) ;
#22964=CARTESIAN_POINT ( 'NONE',  ( 1.881053915767121776, 11.49999999863440792, -4.541265875000002339 ) ) ;
#23007=CARTESIAN_POINT ( 'NONE',  ( 1.881053915767121776, 9.624999998634404363, -4.541265875000002339 ) ) ;
#23012=CARTESIAN_POINT ( 'NONE',  ( -1.656854249492383691, 7.687500000000000000, 4.000000000000000888 ) ) ;
#23013=CARTESIAN_POINT ( 'NONE',  ( -7.347880794884122694E-16, 22.49999999726881583, 4.000000000000001776 ) ) ;
#23014=CARTESIAN_POINT ( 'NONE',  ( 2.780723358947928197E-16, 12.56249999863440792, -4.541265875000002339 ) ) ;
#23023=CARTESIAN_POINT ( 'NONE',  ( 3.211159895383560947, 22.18749999863440792, 3.211159895383562723 ) ) ;
#23073=CARTESIAN_POINT ( 'NONE',  ( -2.828427124746190735, 20.12499999726881228, -2.828427124746191623 ) ) ;
#23088=CARTESIAN_POINT ( 'NONE',  ( -1.881053915767121776, 12.74999999863440969, -4.541265875000002339 ) ) ;
#23099=CARTESIAN_POINT ( 'NONE',  ( -2.828427124746190735, 10.12499999726881406, -2.828427124746191623 ) ) ;
#23100=CARTESIAN_POINT ( 'NONE',  ( 3.211159895383561835, 0.4374999986344066949, -3.211159895383561835 ) ) ;
#23106=CARTESIAN_POINT ( 'NONE',  ( 1.881053915767121776, 9.499999998634406140, -4.541265875000002339 ) ) ;
#23107=CARTESIAN_POINT ( 'NONE',  ( -4.000000000000001776, 10.24999999726881406, -4.898587196589415787E-16 ) ) ;
#23136=PLANE ( 'NONE',  #73199 ) ;
#23150=CARTESIAN_POINT ( 'NONE',  ( 1.881053915767121776, 12.62499999863441147, -4.541265875000002339 ) ) ;
#23153=CARTESIAN_POINT ( 'NONE',  ( -4.000000000000002665, 4.312499997268813168, 1.656854249492380582 ) ) ;
#23180=CARTESIAN_POINT ( 'NONE',  ( 1.881053915767121998, 2.624999998634407028, -4.541265875000002339 ) ) ;
#23189=AXIS2_PLACEMENT_3D ( 'NONE', #46825, #28458, #39772 ) ;
#23194=CARTESIAN_POINT ( 'NONE',  ( 4.541265875000001451, 20.37499999863441147, 1.881053915767124440 ) ) ;
#23223=CARTESIAN_POINT ( 'NONE',  ( 2.449293598294707893E-16, 3.250000000000000444, -4.000000000000001776 ) ) ;
#23227=CYLINDRICAL_SURFACE ( 'NONE', #60116, 4.000000000000001776 ) ;
#23241=CARTESIAN_POINT ( 'NONE',  ( 4.541265875000002339, 20.37499999863441147, -1.881053915767121554 ) ) ;
#23245=CARTESIAN_POINT ( 'NONE',  ( 2.449293598294707893E-16, 5.999999997268813168, -4.000000000000001776 ) ) ;
#23248=CARTESIAN_POINT ( 'NONE',  ( -2.828427124746190735, 19.12499999726881228, -2.828427124746191623 ) ) ;
#23266=CARTESIAN_POINT ( 'NONE',  ( 2.449293598294707893E-16, 6.250000000000000000, -4.000000000000001776 ) ) ;
#23287=CIRCLE ( 'NONE', #65441, 8.000000000000003553 ) ;
#23296=CARTESIAN_POINT ( 'NONE',  ( 4.000000000000001776, 2.749999997268813168, 0.000000000000000000 ) ) ;
#23330=CARTESIAN_POINT ( 'NONE',  ( 4.000000000000001776, 10.00000000000000000, 0.000000000000000000 ) ) ;
#23331=CARTESIAN_POINT ( 'NONE',  ( 2.780723358947928197E-16, 11.56249999863440614, -4.541265875000002339 ) ) ;
#23359=CARTESIAN_POINT ( 'NONE',  ( 1.656854249492406783, 18.56249999726881583, 3.999999999999976019 ) ) ;
#23375=CARTESIAN_POINT ( 'NONE',  ( 4.541265875000002339, 13.43749999863440792, 0.000000000000000000 ) ) ;
#23378=CARTESIAN_POINT ( 'NONE',  ( 2.828427124746190291, 13.87500000000000000, 2.828427124746192067 ) ) ;
#23379=CARTESIAN_POINT ( 'NONE',  ( 4.000000000000000888, 21.68749999726881583, 1.656854249492384135 ) ) ;
#23380=CARTESIAN_POINT ( 'NONE',  ( 4.541265875000002339, 13.31249999863440792, 0.000000000000000000 ) ) ;
#23390=CARTESIAN_POINT ( 'NONE',  ( 4.541265875000002339, 20.37499999863441147, -1.881053915767121554 ) ) ;
#23445=CARTESIAN_POINT ( 'NONE',  ( -1.656854249492381248, 16.06249999726881228, -4.000000000000001776 ) ) ;
#23459=EDGE_CURVE ( 'NONE', #48578, #34152, #31540, .T. ) ;
#23460=CARTESIAN_POINT ( 'NONE',  ( 3.211159895383560947, 12.31249999863440792, 3.211159895383562723 ) ) ;
#23461=VERTEX_POINT ( 'NONE', #54778 ) ;
#23471=CARTESIAN_POINT ( 'NONE',  ( -1.656854249492381248, 12.06249999726881228, -4.000000000000001776 ) ) ;
#23472=CARTESIAN_POINT ( 'NONE',  ( -4.541265875000002339, 1.749999998634406584, -1.881053915767121998 ) ) ;
#23477=CARTESIAN_POINT ( 'NONE',  ( 3.211159895383560947, 12.18749999863440614, 3.211159895383562723 ) ) ;
#23478=CARTESIAN_POINT ( 'NONE',  ( -2.828427124746190735, 18.12499999726881583, -2.828427124746191623 ) ) ;
#23499=LINE ( 'NONE', #46885, #51177 ) ;
#23511=VECTOR ( 'NONE', #65463, 1000.000000000000000 ) ;
#23522=CARTESIAN_POINT ( 'NONE',  ( -4.541265875000002339, 13.87499999863440969, -1.881053915767121998 ) ) ;
#23534=EDGE_CURVE ( 'NONE', #1512, #13147, #36679, .T. ) ;
#23550=CARTESIAN_POINT ( 'NONE',  ( -8.342170076843785083E-16, 2.187499998634407028, 4.541265875000002339 ) ) ;
#23562=CARTESIAN_POINT ( 'NONE',  ( -1.881053915767121554, 18.74999999863440436, -4.541265875000002339 ) ) ;
#23575=VERTEX_POINT ( 'NONE', #50968 ) ;
#23611=CARTESIAN_POINT ( 'NONE',  ( 2.780723358947928197E-16, 1.687499998634406806, -4.541265875000002339 ) ) ;
#23619=CARTESIAN_POINT ( 'NONE',  ( 0.000000000000000000, 0.000000000000000000, 0.000000000000000000 ) ) ;
#23653=CARTESIAN_POINT ( 'NONE',  ( 3.901180567966413104, 22.00000000000000355, 1.216512768759604235 ) ) ;
#23670=ORIENTED_EDGE ( 'NONE', *, *, #29834, .T. ) ;
#23693=CARTESIAN_POINT ( 'NONE',  ( 4.000000000000000888, 18.93750000000000000, 1.656854249492384135 ) ) ;
#23704=CARTESIAN_POINT ( 'NONE',  ( 3.211159895383561835, 11.43749999863440614, -3.211159895383561835 ) ) ;
#23721=( BOUNDED_CURVE ( )  B_SPLINE_CURVE ( 2, ( #65023, #2402, #19745, #64304, #13696, #71418, #42752, #69970, #36741 ),
 .UNSPECIFIED., .F., .F. ) 
 B_SPLINE_CURVE_WITH_KNOTS ( ( 3, 2, 2, 2, 3 ),
 ( 0.3977272727272727626, 0.4034090909090909394, 0.4090909090909091717, 0.4147727272727272929, 0.4204545454545454697 ),
 .UNSPECIFIED. ) 
 CURVE ( )  GEOMETRIC_REPRESENTATION_ITEM ( )  RATIONAL_B_SPLINE_CURVE ( ( 0.9999999999999992228, 0.9238795325112875156, 1.000000000000000000, 0.9238795325112867385, 1.000000000000000000, 0.9238795325112867385, 1.000000000000000000, 0.9238795325112867385, 1.000000000000000000 ) ) 
 REPRESENTATION_ITEM ( '' )  );
#23730=CARTESIAN_POINT ( 'NONE',  ( 4.000000000000001776, 4.062500000000000000, -1.656854249492381248 ) ) ;
#23738=CYLINDRICAL_SURFACE ( 'NONE', #40871, 4.000000000000001776 ) ;
#23752=CARTESIAN_POINT ( 'NONE',  ( 2.828427124746190291, 12.87500000000000178, 2.828427124746192067 ) ) ;
#23754=CARTESIAN_POINT ( 'NONE',  ( -4.541265875000002339, 12.81249999863440792, -5.561446717895856393E-16 ) ) ;
#23800=ORIENTED_EDGE ( 'NONE', *, *, #17153, .T. ) ;
#23817=ORIENTED_EDGE ( 'NONE', *, *, #36731, .T. ) ;
#23835=CARTESIAN_POINT ( 'NONE',  ( 1.881053915767122664, 17.24999999863440792, 4.541265875000001451 ) ) ;
#23839=CARTESIAN_POINT ( 'NONE',  ( -4.541265875000002339, 1.874999998634406806, -1.881053915767121998 ) ) ;
#23842=VECTOR ( 'NONE', #71490, 1000.000000000000000 ) ;
#23844=CARTESIAN_POINT ( 'NONE',  ( -1.656854249492381248, 1.312500000000000444, -4.000000000000001776 ) ) ;
#23845=CARTESIAN_POINT ( 'NONE',  ( -4.000000000000001776, 14.18749999726881406, -1.656854249492381470 ) ) ;
#23851=SHAPE_REPRESENTATION_RELATIONSHIP ( 'NONE' , 'NONE' ,  #30147, #13835 ) ;
#23853=CARTESIAN_POINT ( 'NONE',  ( 1.881053915767122664, 16.12499999863440792, 4.541265875000001451 ) ) ;
#23881=CARTESIAN_POINT ( 'NONE',  ( 1.881053915767121776, 2.499999998634407028, -4.541265875000002339 ) ) ;
#23882=CARTESIAN_POINT ( 'NONE',  ( 2.828427124746190291, 1.624999997268813390, 2.828427124746192067 ) ) ;
#23892=CARTESIAN_POINT ( 'NONE',  ( 0.000000000000000000, 0.000000000000000000, -4.000000000000001776 ) ) ;
#23896=CARTESIAN_POINT ( 'NONE',  ( -3.211159895383562723, 12.06249999863440614, 3.211159895383561391 ) ) ;
#23913=CARTESIAN_POINT ( 'NONE',  ( 2.449293598294707893E-16, 7.250000000000000000, -4.000000000000001776 ) ) ;
#23922=CARTESIAN_POINT ( 'NONE',  ( -4.541265875000002339, 2.874999998634407028, -1.881053915767121998 ) ) ;
#23932=CARTESIAN_POINT ( 'NONE',  ( -1.656854249492381248, 3.062499997268814056, -4.000000000000001776 ) ) ;
#23941=EDGE_CURVE ( 'NONE', #56214, #30314, #52942, .T. ) ;
#23968=DIRECTION ( 'NONE',  ( -0.000000000000000000, -1.000000000000000000, -0.000000000000000000 ) ) ;
#23976=CARTESIAN_POINT ( 'NONE',  ( -2.828427124746190735, 11.37500000000000000, -2.828427124746191623 ) ) ;
#23979=CARTESIAN_POINT ( 'NONE',  ( -3.211159895383561391, 0.8124999986344069169, -3.211159895383561835 ) ) ;
#23982=CARTESIAN_POINT ( 'NONE',  ( -2.828427124746192067, 1.625000000000000444, 2.828427124746190735 ) ) ;
#23983=VERTEX_POINT ( 'NONE', #32921 ) ;
#24038=CARTESIAN_POINT ( 'NONE',  ( -4.384251028818017204, 22.00000000000000711, 1.062498824860025781 ) ) ;
#24066=CARTESIAN_POINT ( 'NONE',  ( -1.881053915767124440, 11.99999999863440969, 4.541265875000001451 ) ) ;
#24107=AXIS2_PLACEMENT_3D ( 'NONE', #25536, #19881, #67035 ) ;
#24109=CARTESIAN_POINT ( 'NONE',  ( -2.828427124746190735, 10.37500000000000000, -2.828427124746191623 ) ) ;
#24111=CARTESIAN_POINT ( 'NONE',  ( 3.211159895383561835, 10.43749999863440792, -3.211159895383561835 ) ) ;
#24194=CARTESIAN_POINT ( 'NONE',  ( -1.881053915767124440, 15.12499999863440792, 4.541265875000001451 ) ) ;
#24198=CARTESIAN_POINT ( 'NONE',  ( 4.541265875000002339, 1.437499998634406806, 0.000000000000000000 ) ) ;
#24203=CARTESIAN_POINT ( 'NONE',  ( 2.828427124746191623, 1.125000000000000444, -2.828427124746191623 ) ) ;
#24204=CARTESIAN_POINT ( 'NONE',  ( -2.828427124746192067, 15.37499999726881406, 2.828427124746190735 ) ) ;
#24205=CARTESIAN_POINT ( 'NONE',  ( -4.541265875000002339, 0.8124999986344066949, -5.561446717895856393E-16 ) ) ;
#24209=VECTOR ( 'NONE', #61760, 1000.000000000000000 ) ;
#24213=CARTESIAN_POINT ( 'NONE',  ( -8.342170076843785083E-16, 14.06249999863440614, 4.541265875000002339 ) ) ;
#24241=CARTESIAN_POINT ( 'NONE',  ( 4.541265875000002339, 4.312499998634407028, 0.000000000000000000 ) ) ;
#24244=CARTESIAN_POINT ( 'NONE',  ( 2.828427124746191623, 5.125000000000000000, -2.828427124746191623 ) ) ;
#24258=CARTESIAN_POINT ( 'NONE',  ( 4.541265875000002339, 15.43749999863440614, 0.000000000000000000 ) ) ;
#24278=CARTESIAN_POINT ( 'NONE',  ( -4.000000000000002665, 17.56250000000000000, 1.656854249492380582 ) ) ;
#24287=CARTESIAN_POINT ( 'NONE',  ( -3.211159895383562723, 6.062499998634407028, 3.211159895383561391 ) ) ;
#24296=ADVANCED_FACE ( 'NONE', ( #73263 ), #10633, .T. ) ;
#24299=ADVANCED_FACE ( 'NONE', ( #56666 ), #34040, .T. ) ;
#24301=CARTESIAN_POINT ( 'NONE',  ( 1.656854249492381248, 2.937499997268813612, -4.000000000000001776 ) ) ;
#24306=CARTESIAN_POINT ( 'NONE',  ( 3.211159895383560947, 3.187499998634407028, 3.211159895383562723 ) ) ;
#24327=DIRECTION ( 'NONE',  ( 0.000000000000000000, 0.000000000000000000, -1.000000000000000000 ) ) ;
#24342=B_SPLINE_CURVE_WITH_KNOTS ( 'NONE', 3,
 ( #73418, #62097, #4392, #16800, #50404, #56449, #27760, #73786 ),
 .UNSPECIFIED., .F., .F.,
 ( 4, 2, 2, 4 ),
 ( 0.000000000000000000, 0.001793316283962787623, 0.002689974425944181326, 0.003586632567925575246 ),
 .UNSPECIFIED. ) ;
#24350=CARTESIAN_POINT ( 'NONE',  ( -8.342170076843785083E-16, 5.187499998634407028, 4.541265875000002339 ) ) ;
#24356=CARTESIAN_POINT ( 'NONE',  ( -1.656854249492383468, 19.43749999726880873, 4.000000000000000888 ) ) ;
#24384=ORIENTED_EDGE ( 'NONE', *, *, #73977, .T. ) ;
#24413=CARTESIAN_POINT ( 'NONE',  ( -4.436061581686053579, 22.00000000000000000, 0.5394833180921509985 ) ) ;
#24441=CARTESIAN_POINT ( 'NONE',  ( 4.541265875000002339, 11.37499999863440969, -1.881053915767121554 ) ) ;
#24486=CARTESIAN_POINT ( 'NONE',  ( -4.000000000000001776, 11.50000000000000000, -4.898587196589415787E-16 ) ) ;
#24489=CARTESIAN_POINT ( 'NONE',  ( 4.541265875000001451, 13.24999999863440969, 1.881053915767124440 ) ) ;
#24511=CARTESIAN_POINT ( 'NONE',  ( -4.000000000000001776, 0.5000000000000002220, -4.898587196589415787E-16 ) ) ;
#24545=AXIS2_PLACEMENT_3D ( 'NONE', #15289, #66609, #37579 ) ;
#24553=CARTESIAN_POINT ( 'NONE',  ( -1.656854249492381248, 3.312500000000000000, -4.000000000000001776 ) ) ;
#24565=CARTESIAN_POINT ( 'NONE',  ( 4.541265875000001451, 18.37499999863441147, 1.881053915767124440 ) ) ;
#24576=CARTESIAN_POINT ( 'NONE',  ( -2.828427124746190735, 14.12499999726881406, -2.828427124746191623 ) ) ;
#24577=CARTESIAN_POINT ( 'NONE',  ( 4.541265875000002339, 1.312499998634406584, 0.000000000000000000 ) ) ;
#24584=CARTESIAN_POINT ( 'NONE',  ( 1.881053915767121776, 15.49999999863440792, -4.541265875000002339 ) ) ;
#24608=CARTESIAN_POINT ( 'NONE',  ( 3.211159895383560947, 2.187499998634407028, 3.211159895383562723 ) ) ;
#24625=CARTESIAN_POINT ( 'NONE',  ( -4.541265875000002339, 16.93749999863440436, -5.561446717895856393E-16 ) ) ;
#24627=CARTESIAN_POINT ( 'NONE',  ( 2.828427124746190291, 10.62499999726881406, 2.828427124746192067 ) ) ;
#24650=CARTESIAN_POINT ( 'NONE',  ( 1.881053915767122664, 5.249999998634407028, 4.541265875000001451 ) ) ;
#24661=CARTESIAN_POINT ( 'NONE',  ( 2.828427124746190291, 2.624999997268812724, 2.828427124746192067 ) ) ;
#24666=CARTESIAN_POINT ( 'NONE',  ( 2.780723358947928197E-16, 0.5624999986344066949, -4.541265875000002339 ) ) ;
#24687=CARTESIAN_POINT ( 'NONE',  ( -1.656854249492383468, 17.43749999726881583, 4.000000000000000888 ) ) ;
#24710=CARTESIAN_POINT ( 'NONE',  ( -4.541265875000002339, 4.874999998634407916, -1.881053915767121998 ) ) ;
#24735=CARTESIAN_POINT ( 'NONE',  ( -2.828427124746192067, 9.625000000000000000, 2.828427124746190735 ) ) ;
#24747=DIRECTION ( 'NONE',  ( -0.000000000000000000, -1.000000000000000000, -0.000000000000000000 ) ) ;
#24757=CARTESIAN_POINT ( 'NONE',  ( 2.780723358947928197E-16, 10.68749999863440792, -4.541265875000002339 ) ) ;
#24786=CARTESIAN_POINT ( 'NONE',  ( 2.828427124746191623, 19.12500000000000000, -2.828427124746191623 ) ) ;
#24789=EDGE_CURVE ( 'NONE', #57749, #11511, #72801, .T. ) ;
#24798=CARTESIAN_POINT ( 'NONE',  ( 4.541265875000002339, 14.31249999863440792, 0.000000000000000000 ) ) ;
#24814=CARTESIAN_POINT ( 'NONE',  ( -2.828427124746192067, 13.37499999726881406, 2.828427124746190735 ) ) ;
#24818=( BOUNDED_CURVE ( )  B_SPLINE_CURVE ( 2, ( #27075, #60279, #67071, #44061, #44431, #14623, #26698, #49718, #66317 ),
 .UNSPECIFIED., .F., .F. ) 
 B_SPLINE_CURVE_WITH_KNOTS ( ( 3, 2, 2, 2, 3 ),
 ( 0.4659090909090909394, 0.4715909090909091717, 0.4772727272727272929, 0.4829545454545454697, 0.4886363636363636465 ),
 .UNSPECIFIED. ) 
 CURVE ( )  GEOMETRIC_REPRESENTATION_ITEM ( )  RATIONAL_B_SPLINE_CURVE ( ( 0.9999999999999992228, 0.9238795325112875156, 1.000000000000000000, 0.9238795325112867385, 1.000000000000000000, 0.9238795325112867385, 1.000000000000000000, 0.9238795325112867385, 1.000000000000000000 ) ) 
 REPRESENTATION_ITEM ( '' )  );
#24837=CARTESIAN_POINT ( 'NONE',  ( -7.347880794884122694E-16, 19.75000000000000000, 4.000000000000001776 ) ) ;
#24841=CARTESIAN_POINT ( 'NONE',  ( 4.000000000000001776, 13.00000000000000178, 0.000000000000000000 ) ) ;
#24843=CARTESIAN_POINT ( 'NONE',  ( 3.211159895383561835, 17.43749999863440792, -3.211159895383561835 ) ) ;
#24866=CARTESIAN_POINT ( 'NONE',  ( -4.000000000000002665, 0.5625000000000003331, 1.656854249492380582 ) ) ;
#24908=CARTESIAN_POINT ( 'NONE',  ( 1.656854249492381248, 7.187500000000000000, -4.000000000000001776 ) ) ;
#24917=ORIENTED_EDGE ( 'NONE', *, *, #63245, .T. ) ;
#24924=CARTESIAN_POINT ( 'NONE',  ( -8.342170076843785083E-16, 15.18749999863440792, 4.541265875000002339 ) ) ;
#24926=ORIENTED_EDGE ( 'NONE', *, *, #55653, .F. ) ;
#24928=CARTESIAN_POINT ( 'NONE',  ( -4.541265875000002339, 1.937499998634406806, -5.561446717895856393E-16 ) ) ;
#24934=CARTESIAN_POINT ( 'NONE',  ( -1.656854249492383691, 0.6875000000000003331, 4.000000000000000888 ) ) ;
#24935=CARTESIAN_POINT ( 'NONE',  ( -4.000000000000002665, 12.31249999726881406, 1.656854249492380804 ) ) ;
#24936=CARTESIAN_POINT ( 'NONE',  ( -4.541265875000002339, 4.812499998634407028, -5.561446717895856393E-16 ) ) ;
#24944=CARTESIAN_POINT ( 'NONE',  ( -1.881053915767124440, 12.99999999863440969, 4.541265875000001451 ) ) ;
#24954=CARTESIAN_POINT ( 'NONE',  ( 4.898587196589415787E-16, 0.000000000000000000, 4.000000000000001776 ) ) ;
#24973=CARTESIAN_POINT ( 'NONE',  ( -4.541265875000002339, 3.749999998634407028, -1.881053915767121998 ) ) ;
#24990=CARTESIAN_POINT ( 'NONE',  ( 3.211159895383561835, 16.56249999863440436, -3.211159895383561835 ) ) ;
#25012=CARTESIAN_POINT ( 'NONE',  ( -3.211159895383562723, 3.062499998634407028, 3.211159895383561391 ) ) ;
#25023=CARTESIAN_POINT ( 'NONE',  ( -3.211159895383562723, 22.06249999863440792, 3.211159895383561391 ) ) ;
#25029=CARTESIAN_POINT ( 'NONE',  ( -4.541265875000002339, 3.812499998634407028, -5.561446717895856393E-16 ) ) ;
#25046=VERTEX_POINT ( 'NONE', #73912 ) ;
#25075=CARTESIAN_POINT ( 'NONE',  ( 4.541265875000002339, 4.499999998634407028, -1.881053915767121554 ) ) ;
#25107=VERTEX_POINT ( 'NONE', #10915 ) ;
#25120=CARTESIAN_POINT ( 'NONE',  ( 3.211159895383560947, 11.31249999863440792, 3.211159895383562723 ) ) ;
#25130=EDGE_CURVE ( 'NONE', #34152, #6173, #15661, .T. ) ;
#25134=DIRECTION ( 'NONE',  ( 0.000000000000000000, 0.000000000000000000, 1.000000000000000000 ) ) ;
#25167=CARTESIAN_POINT ( 'NONE',  ( -1.881053915767124440, 12.99999999863440969, 4.541265875000001451 ) ) ;
#25215=CARTESIAN_POINT ( 'NONE',  ( 1.656854249492381248, 16.18750000000000355, -4.000000000000001776 ) ) ;
#25216=CARTESIAN_POINT ( 'NONE',  ( 4.541265875000002339, 15.31249999863440614, 0.000000000000000000 ) ) ;
#25225=CARTESIAN_POINT ( 'NONE',  ( 2.828427124746191623, 6.874999997268813168, -2.828427124746191623 ) ) ;
#25246=FACE_OUTER_BOUND ( 'NONE', #67750, .T. ) ;
#25295=CARTESIAN_POINT ( 'NONE',  ( 1.881053915767121998, 15.62499999863440614, -4.541265875000002339 ) ) ;
#25299=CARTESIAN_POINT ( 'NONE',  ( 3.211159895383560947, 4.312499998634407028, 3.211159895383562723 ) ) ;
#25306=CARTESIAN_POINT ( 'NONE',  ( 2.828427124746191623, 3.125000000000000000, -2.828427124746191623 ) ) ;
#25307=CARTESIAN_POINT ( 'NONE',  ( 4.000000000000000888, 13.68749999726881406, 1.656854249492384135 ) ) ;
#25308=CARTESIAN_POINT ( 'NONE',  ( -3.211159895383561391, 5.687499998634407028, -3.211159895383561835 ) ) ;
#25313=CARTESIAN_POINT ( 'NONE',  ( 1.881053915767121776, 14.49999999863440969, -4.541265875000002339 ) ) ;
#25337=CARTESIAN_POINT ( 'NONE',  ( -4.000000000000002665, 3.312499997268814056, 1.656854249492380582 ) ) ;
#25344=CARTESIAN_POINT ( 'NONE',  ( 1.881053915767122664, 2.124999998634406584, 4.541265875000001451 ) ) ;
#25358=VECTOR ( 'NONE', #2906, 1000.000000000000000 ) ;
#25362=CARTESIAN_POINT ( 'NONE',  ( -1.881053915767121554, 14.74999999863440969, -4.541265875000002339 ) ) ;
#25367=( BOUNDED_CURVE ( )  B_SPLINE_CURVE ( 2, ( #65568, #20661, #49717, #38031, #38405, #37660, #54268, #37284, #71964 ),
 .UNSPECIFIED., .F., .F. ) 
 B_SPLINE_CURVE_WITH_KNOTS ( ( 3, 2, 2, 2, 3 ),
 ( 0.1250000000000000000, 0.1306818181818181768, 0.1363636363636363535, 0.1420454545454545581, 0.1477272727272727348 ),
 .UNSPECIFIED. ) 
 CURVE ( )  GEOMETRIC_REPRESENTATION_ITEM ( )  RATIONAL_B_SPLINE_CURVE ( ( 1.000000000000000000, 0.9238795325112867385, 1.000000000000000000, 0.9238795325112867385, 1.000000000000000000, 0.9238795325112867385, 1.000000000000000000, 0.9238795325112867385, 1.000000000000000000 ) ) 
 REPRESENTATION_ITEM ( '' )  );
#25386=CARTESIAN_POINT ( 'NONE',  ( 2.780723358947928197E-16, 6.687499998634407028, -4.541265875000002339 ) ) ;
#25399=CARTESIAN_POINT ( 'NONE',  ( -2.828427124746190735, 4.124999997268813168, -2.828427124746191623 ) ) ;
#25406=CARTESIAN_POINT ( 'NONE',  ( -8.342170076843785083E-16, 3.062499998634406584, 4.541265875000002339 ) ) ;
#25427=DIRECTION ( 'NONE',  ( -0.000000000000000000, -1.000000000000000000, -0.000000000000000000 ) ) ;
#25448=CARTESIAN_POINT ( 'NONE',  ( 2.780723358947928197E-16, 3.687499998634407472, -4.541265875000002339 ) ) ;
#25462=LINE ( 'NONE', #8495, #16407 ) ;
#25469=ORIENTED_EDGE ( 'NONE', *, *, #21054, .T. ) ;
#25494=CARTESIAN_POINT ( 'NONE',  ( -4.541265875000003227, 11.99999999863440969, 1.881053915767121110 ) ) ;
#25500=AXIS2_PLACEMENT_3D ( 'NONE', #6408, #51671, #46009 ) ;
#25506=SPHERICAL_SURFACE ( 'NONE', #36642, 10.00000000000001243 ) ;
#25536=CARTESIAN_POINT ( 'NONE',  ( 0.000000000000000000, 0.000000000000000000, 0.000000000000000000 ) ) ;
#25537=CARTESIAN_POINT ( 'NONE',  ( 1.881053915767122664, 15.12499999863441147, 4.541265875000001451 ) ) ;
#25548=VERTEX_POINT ( 'NONE', #41367 ) ;
#25587=CARTESIAN_POINT ( 'NONE',  ( -4.000000000000001776, 16.43750000000000355, -1.656854249492381470 ) ) ;
#25588=CARTESIAN_POINT ( 'NONE',  ( -3.211159895383561391, 15.68749999863440436, -3.211159895383561835 ) ) ;
#25627=CARTESIAN_POINT ( 'NONE',  ( -4.000000000000001776, 6.500000000000000888, -4.898587196589415787E-16 ) ) ;
#25632=CARTESIAN_POINT ( 'NONE',  ( -1.656854249492381248, 14.31250000000000000, -4.000000000000001776 ) ) ;
#25648=EDGE_CURVE ( 'NONE', #23461, #3011, #15641, .T. ) ;
#25665=CARTESIAN_POINT ( 'NONE',  ( -4.541265875000002339, 21.87499999863441147, -1.881053915767121998 ) ) ;
#25668=CARTESIAN_POINT ( 'NONE',  ( -4.541265875000002339, 4.937499998634407916, -5.561446717895856393E-16 ) ) ;
#25674=CARTESIAN_POINT ( 'NONE',  ( -4.000000000000002665, 5.562500000000000000, 1.656854249492380804 ) ) ;
#25675=CARTESIAN_POINT ( 'NONE',  ( -7.347880794884122694E-16, 18.49999999726881583, 4.000000000000001776 ) ) ;
#25676=CARTESIAN_POINT ( 'NONE',  ( -4.541265875000002339, 2.749999998634407028, -1.881053915767121998 ) ) ;
#25683=CARTESIAN_POINT ( 'NONE',  ( 4.541265875000002339, 20.31249999863440436, 0.000000000000000000 ) ) ;
#25697=ORIENTED_EDGE ( 'NONE', *, *, #69485, .F. ) ;
#25711=CARTESIAN_POINT ( 'NONE',  ( 1.881053915767122664, 8.124999998634407916, 4.541265875000001451 ) ) ;
#25728=CARTESIAN_POINT ( 'NONE',  ( 1.881053915767121776, 16.62499999863440436, -4.541265875000002339 ) ) ;
#25754=CARTESIAN_POINT ( 'NONE',  ( 2.780723358947928197E-16, 9.687499998634406140, -4.541265875000002339 ) ) ;
#25766=CARTESIAN_POINT ( 'NONE',  ( -4.000000000000001776, 8.187499997268812280, -1.656854249492381470 ) ) ;
#25770=CARTESIAN_POINT ( 'NONE',  ( -4.541265875000003227, 0.8749999986344069169, 1.881053915767121110 ) ) ;
#25817=CARTESIAN_POINT ( 'NONE',  ( -3.211159895383561391, 4.812499998634407028, -3.211159895383561835 ) ) ;
#25849=CARTESIAN_POINT ( 'NONE',  ( 1.672363534939973917, 21.99999999999999289, 4.002810566133208958 ) ) ;
#25858=CARTESIAN_POINT ( 'NONE',  ( 4.541265875000002339, 10.49999999863440792, -1.881053915767121554 ) ) ;
#25876=CARTESIAN_POINT ( 'NONE',  ( -1.656854249492381248, 15.06249999726881406, -4.000000000000001776 ) ) ;
#25883=ORIENTED_EDGE ( 'NONE', *, *, #53722, .F. ) ;
#25897=( BOUNDED_CURVE ( )  B_SPLINE_CURVE ( 2, ( #40669, #333, #46692, #74630, #5973, #57666, #63297, #33918, #45953 ),
 .UNSPECIFIED., .F., .F. ) 
 B_SPLINE_CURVE_WITH_KNOTS ( ( 3, 2, 2, 2, 3 ),
 ( 0.9431818181818182323, 0.9488636363636363535, 0.9545454545454545858, 0.9602272727272727071, 0.9659090909090909394 ),
 .UNSPECIFIED. ) 
 CURVE ( )  GEOMETRIC_REPRESENTATION_ITEM ( )  RATIONAL_B_SPLINE_CURVE ( ( 1.000000000000000000, 0.9238795325112867385, 1.000000000000000000, 0.9238795325112867385, 1.000000000000000000, 0.9238795325112867385, 1.000000000000000000, 0.9238795325112867385, 1.000000000000000000 ) ) 
 REPRESENTATION_ITEM ( '' )  );
#25905=CARTESIAN_POINT ( 'NONE',  ( 4.541265875000002339, 15.31249999863440614, 0.000000000000000000 ) ) ;
#25951=CARTESIAN_POINT ( 'NONE',  ( -4.000000000000002665, 15.56250000000000000, 1.656854249492380804 ) ) ;
#25952=CARTESIAN_POINT ( 'NONE',  ( 3.211159895383560947, 16.18749999863440436, 3.211159895383562723 ) ) ;
#25981=CARTESIAN_POINT ( 'NONE',  ( 4.000000000000001776, 5.812499997268813168, -1.656854249492381248 ) ) ;
#25993=VERTEX_POINT ( 'NONE', #23913 ) ;
#26019=CARTESIAN_POINT ( 'NONE',  ( 1.656854249492381914, 21.81250000000000355, 4.000000000000000888 ) ) ;
#26027=ORIENTED_EDGE ( 'NONE', *, *, #73977, .F. ) ;
#26037=CARTESIAN_POINT ( 'NONE',  ( 1.881053915767121776, 3.624999998634407028, -4.541265875000002339 ) ) ;
#26044=CARTESIAN_POINT ( 'NONE',  ( -2.828427124746190735, 4.375000000000000000, -2.828427124746191623 ) ) ;
#26045=CARTESIAN_POINT ( 'NONE',  ( -2.828427124746190735, 20.12499999726881228, -2.828427124746191623 ) ) ;
#26046=CARTESIAN_POINT ( 'NONE',  ( 4.541265875000001451, 3.249999998634407472, 1.881053915767124440 ) ) ;
#26052=CARTESIAN_POINT ( 'NONE',  ( 3.211159895383561835, 18.43749999863440436, -3.211159895383561835 ) ) ;
#26055=ORIENTED_EDGE ( 'NONE', *, *, #58642, .T. ) ;
#26084=CARTESIAN_POINT ( 'NONE',  ( -1.881053915767124440, 5.999999998634407028, 4.541265875000001451 ) ) ;
#26103=CARTESIAN_POINT ( 'NONE',  ( -8.342170076843785083E-16, 20.18749999863440436, 4.541265875000002339 ) ) ;
#26124=ORIENTED_EDGE ( 'NONE', *, *, #12451, .T. ) ;
#26126=CARTESIAN_POINT ( 'NONE',  ( 3.211159895383560947, 10.31249999863440792, 3.211159895383562723 ) ) ;
#26140=CARTESIAN_POINT ( 'NONE',  ( 4.000000000000000888, 6.687499997268813168, 1.656854249492384135 ) ) ;
#26146=CARTESIAN_POINT ( 'NONE',  ( -8.342170076843785083E-16, 5.062499998634407028, 4.541265875000002339 ) ) ;
#26148=CARTESIAN_POINT ( 'NONE',  ( -1.656854249492381248, 13.31250000000000000, -4.000000000000001776 ) ) ;
#26191=CARTESIAN_POINT ( 'NONE',  ( -3.211159895383562723, 9.062499998634407916, 3.211159895383561391 ) ) ;
#26218=ORIENTED_EDGE ( 'NONE', *, *, #46301, .F. ) ;
#26228=ADVANCED_FACE ( 'NONE', ( #29029 ), #6767, .T. ) ;
#26235=CARTESIAN_POINT ( 'NONE',  ( -3.211159895383561391, 14.81249999863440792, -3.211159895383561835 ) ) ;
#26278=CARTESIAN_POINT ( 'NONE',  ( -4.541265875000003227, 19.87499999863440792, 1.881053915767121110 ) ) ;
#26312=CARTESIAN_POINT ( 'NONE',  ( -4.000000000000001776, 19.43750000000000000, -1.656854249492381470 ) ) ;
#26329=CARTESIAN_POINT ( 'NONE',  ( 4.000000000000001776, 15.06249999999999822, -1.656854249492381248 ) ) ;
#26330=CARTESIAN_POINT ( 'NONE',  ( 1.881053915767122664, 17.12499999863440436, 4.541265875000001451 ) ) ;
#26360=CARTESIAN_POINT ( 'NONE',  ( 4.000000000000001776, 5.749999997268813168, 0.000000000000000000 ) ) ;
#26381=CARTESIAN_POINT ( 'NONE',  ( 2.449293598294707893E-16, 10.99999999726881406, -4.000000000000001776 ) ) ;
#26407=CARTESIAN_POINT ( 'NONE',  ( -4.541265875000003227, 19.99999999863440436, 1.881053915767121110 ) ) ;
#26410=CARTESIAN_POINT ( 'NONE',  ( -4.541265875000002339, 3.874999998634407028, -1.881053915767121998 ) ) ;
#26412=ADVANCED_FACE ( 'NONE', ( #754 ), #23738, .T. ) ;
#26420=CARTESIAN_POINT ( 'NONE',  ( 2.828427124746190291, 4.875000000000000000, 2.828427124746192067 ) ) ;
#26421=CARTESIAN_POINT ( 'NONE',  ( 1.656854249492381248, 19.93749999726881228, -4.000000000000001776 ) ) ;
#26422=CARTESIAN_POINT ( 'NONE',  ( 4.541265875000002339, 5.374999998634407028, -1.881053915767121776 ) ) ;
#26428=CARTESIAN_POINT ( 'NONE',  ( -8.342170076843785083E-16, 17.06249999863440792, 4.541265875000002339 ) ) ;
#26432=( BOUNDED_CURVE ( )  B_SPLINE_CURVE ( 2, ( #43455, #15158, #38189, #61193, #3108, #55549, #19697, #60813, #31776 ),
 .UNSPECIFIED., .F., .F. ) 
 B_SPLINE_CURVE_WITH_KNOTS ( ( 3, 2, 2, 2, 3 ),
 ( 0.8522727272727272929, 0.8579545454545454142, 0.8636363636363636465, 0.8693181818181817677, 0.8750000000000000000 ),
 .UNSPECIFIED. ) 
 CURVE ( )  GEOMETRIC_REPRESENTATION_ITEM ( )  RATIONAL_B_SPLINE_CURVE ( ( 1.000000000000000000, 0.9238795325112867385, 1.000000000000000000, 0.9238795325112867385, 1.000000000000000000, 0.9238795325112867385, 1.000000000000000000, 0.9238795325112867385, 1.000000000000000000 ) ) 
 REPRESENTATION_ITEM ( '' )  );
#26439=CARTESIAN_POINT ( 'NONE',  ( -4.000000000000002665, 21.31249999726881228, 1.656854249492380582 ) ) ;
#26450=CARTESIAN_POINT ( 'NONE',  ( -4.000000000000001776, 5.437500000000001776, -1.656854249492381470 ) ) ;
#26457=( BOUNDED_CURVE ( )  B_SPLINE_CURVE ( 2, ( #19114, #20214, #54949, #42119, #2512, #65508, #13441, #3258, #72280 ),
 .UNSPECIFIED., .F., .F. ) 
 B_SPLINE_CURVE_WITH_KNOTS ( ( 3, 2, 2, 2, 3 ),
 ( 0.8977272727272727071, 0.9034090909090909394, 0.9090909090909091717, 0.9147727272727274039, 0.9204545454545455252 ),
 .UNSPECIFIED. ) 
 CURVE ( )  GEOMETRIC_REPRESENTATION_ITEM ( )  RATIONAL_B_SPLINE_CURVE ( ( 1.000000000000000000, 0.9238795325112867385, 1.000000000000000000, 0.9238795325112867385, 1.000000000000000000, 0.9238795325112867385, 1.000000000000000000, 0.9238795325112852952, 1.000000000000001554 ) ) 
 REPRESENTATION_ITEM ( '' )  );
#26461=CARTESIAN_POINT ( 'NONE',  ( -4.541265875000002339, 5.749999998634407028, -1.881053915767121998 ) ) ;
#26479=CARTESIAN_POINT ( 'NONE',  ( -3.211159895383562723, 21.06249999863440792, 3.211159895383561391 ) ) ;
#26503=CARTESIAN_POINT ( 'NONE',  ( 4.541265875000002339, 7.499999998634407916, -1.881053915767121776 ) ) ;
#26514=CARTESIAN_POINT ( 'NONE',  ( -2.828427124746190735, 7.124999997268813168, -2.828427124746191623 ) ) ;
#26522=CARTESIAN_POINT ( 'NONE',  ( 4.541265875000002339, 8.312499998634407916, 0.000000000000000000 ) ) ;
#26568=CARTESIAN_POINT ( 'NONE',  ( 4.541265875000001451, 10.37499999863440792, 1.881053915767124440 ) ) ;
#26572=CARTESIAN_POINT ( 'NONE',  ( -7.347880794884122694E-16, 14.49999999726881406, 4.000000000000001776 ) ) ;
#26616=CARTESIAN_POINT ( 'NONE',  ( 4.541265875000002339, 16.43749999863440436, 0.000000000000000000 ) ) ;
#26630=CARTESIAN_POINT ( 'NONE',  ( -7.240284387734133737E-08, 22.00000000000001066, -4.000000000000000888 ) ) ;
#26662=CARTESIAN_POINT ( 'NONE',  ( 3.211159895383561835, 17.43749999863440792, -3.211159895383561835 ) ) ;
#26668=FACE_OUTER_BOUND ( 'NONE', #34634, .T. ) ;
#26672=AXIS2_PLACEMENT_3D ( 'NONE', #44597, #49499, #38937 ) ;
#26684=EDGE_CURVE ( 'NONE', #7966, #61381, #41235, .T. ) ;
#26696=DIRECTION ( 'NONE',  ( 0.000000000000000000, 0.000000000000000000, -1.000000000000000000 ) ) ;
#26698=CARTESIAN_POINT ( 'NONE',  ( -2.828427124746192067, 11.37499999726881406, 2.828427124746190735 ) ) ;
#26715=CARTESIAN_POINT ( 'NONE',  ( 4.000000000000001776, 16.00000000000000000, 0.000000000000000000 ) ) ;
#26716=CARTESIAN_POINT ( 'NONE',  ( 3.211159895383560947, 20.18749999863440436, 3.211159895383562723 ) ) ;
#26743=ADVANCED_FACE ( 'NONE', ( #38602 ), #31438, .T. ) ;
#26799=CARTESIAN_POINT ( 'NONE',  ( 4.541265875000001451, 20.37499999863441147, 1.881053915767124440 ) ) ;
#26802=CARTESIAN_POINT ( 'NONE',  ( 1.881053915767122664, 5.249999998634406140, 4.541265875000001451 ) ) ;
#26809=CARTESIAN_POINT ( 'NONE',  ( 4.000000000000001776, 4.000000000000000000, 0.000000000000000000 ) ) ;
#26810=CARTESIAN_POINT ( 'NONE',  ( 1.656854249492381914, 18.56249999726882294, 4.000000000000000888 ) ) ;
#26811=CARTESIAN_POINT ( 'NONE',  ( -1.881053915767124440, 6.999999998634407916, 4.541265875000001451 ) ) ;
#26817=CARTESIAN_POINT ( 'NONE',  ( 2.780723358947928197E-16, 16.56249999863440436, -4.541265875000002339 ) ) ;
#26833=ORIENTED_EDGE ( 'NONE', *, *, #51043, .F. ) ;
#26848=CARTESIAN_POINT ( 'NONE',  ( 4.541265875000001451, 7.249999998634408804, 1.881053915767124440 ) ) ;
#26867=CARTESIAN_POINT ( 'NONE',  ( 1.881053915767121776, 21.62499999863441502, -4.541265875000002339 ) ) ;
#26885=ORIENTED_EDGE ( 'NONE', *, *, #15669, .T. ) ;
#26887=CARTESIAN_POINT ( 'NONE',  ( -1.881053915767124440, 7.124999998634407916, 4.541265875000001451 ) ) ;
#26899=CARTESIAN_POINT ( 'NONE',  ( -4.000000000000002665, 6.312499997268812280, 1.656854249492380804 ) ) ;
#26905=CARTESIAN_POINT ( 'NONE',  ( 4.541265875000001451, 5.249999998634406140, 1.881053915767124440 ) ) ;
#26947=CARTESIAN_POINT ( 'NONE',  ( -1.881053915767121554, 8.749999998634406140, -4.541265875000002339 ) ) ;
#26956=CARTESIAN_POINT ( 'NONE',  ( 0.000000000000000000, 0.000000000000000000, 0.000000000000000000 ) ) ;
#26993=CARTESIAN_POINT ( 'NONE',  ( 1.881053915767121776, 15.62499999863440614, -4.541265875000002339 ) ) ;
#27033=CARTESIAN_POINT ( 'NONE',  ( 1.656854249492381914, 1.812500000000000222, 4.000000000000000888 ) ) ;
#27040=CARTESIAN_POINT ( 'NONE',  ( -4.541265875000003227, 17.87499999863441147, 1.881053915767121110 ) ) ;
#27074=CARTESIAN_POINT ( 'NONE',  ( 1.656854249492381248, 0.9374999972688131678, -4.000000000000001776 ) ) ;
#27075=CARTESIAN_POINT ( 'NONE',  ( 2.449293598294707893E-16, 10.99999999726881406, -4.000000000000001776 ) ) ;
#27090=CARTESIAN_POINT ( 'NONE',  ( -1.656854249492383691, 18.68750000000000000, 4.000000000000000888 ) ) ;
#27091=CARTESIAN_POINT ( 'NONE',  ( -3.211159895383561391, 20.68749999863440436, -3.211159895383561835 ) ) ;
#27094=EDGE_LOOP ( 'NONE', ( #73119, #23670, #2460, #62610 ) ) ;
#27096=ADVANCED_FACE ( 'NONE', ( #64206 ), #56678, .F. ) ;
#27166=CARTESIAN_POINT ( 'NONE',  ( -4.541265875000002339, 19.93749999863440436, -5.561446717895856393E-16 ) ) ;
#27169=CARTESIAN_POINT ( 'NONE',  ( 1.881053915767121776, 8.624999998634406140, -4.541265875000002339 ) ) ;
#27177=CARTESIAN_POINT ( 'NONE',  ( 2.449293598294707893E-16, 9.250000000000000000, -4.000000000000001776 ) ) ;
#27178=CARTESIAN_POINT ( 'NONE',  ( 1.656854249492381914, 19.56249999726881228, 4.000000000000000888 ) ) ;
#27179=CARTESIAN_POINT ( 'NONE',  ( -8.342170076843785083E-16, 9.062499998634407916, 4.541265875000002339 ) ) ;
#27185=CARTESIAN_POINT ( 'NONE',  ( 4.541265875000001451, 20.24999999863440436, 1.881053915767124440 ) ) ;
#27215=CARTESIAN_POINT ( 'NONE',  ( -4.541265875000002339, 7.749999998634407916, -1.881053915767121998 ) ) ;
#27233=CARTESIAN_POINT ( 'NONE',  ( 4.541265875000001451, 19.37499999863440792, 1.881053915767124440 ) ) ;
#27256=CARTESIAN_POINT ( 'NONE',  ( -3.211159895383562723, 10.06249999863440614, 3.211159895383561391 ) ) ;
#27265=CARTESIAN_POINT ( 'NONE',  ( 1.656854249492381914, 4.562499997268812280, 4.000000000000000888 ) ) ;
#27273=CARTESIAN_POINT ( 'NONE',  ( 1.656854249492381914, 12.56249999726881406, 4.000000000000000888 ) ) ;
#27275=CARTESIAN_POINT ( 'NONE',  ( 4.541265875000002339, 4.374999998634407028, -1.881053915767121554 ) ) ;
#27278=CARTESIAN_POINT ( 'NONE',  ( -2.828427124746190735, 21.37500000000000000, -2.828427124746191623 ) ) ;
#27315=CARTESIAN_POINT ( 'NONE',  ( -4.541265875000002339, 9.874999998634404363, -1.881053915767121998 ) ) ;
#27318=CARTESIAN_POINT ( 'NONE',  ( -2.828427124746192067, 5.374999997268813168, 2.828427124746190735 ) ) ;
#27332=FACE_OUTER_BOUND ( 'NONE', #6379, .T. ) ;
#27336=CARTESIAN_POINT ( 'NONE',  ( 4.898587196589415787E-16, 0.000000000000000000, 4.000000000000001776 ) ) ;
#27360=CARTESIAN_POINT ( 'NONE',  ( -4.541265875000003227, 16.99999999863440792, 1.881053915767121110 ) ) ;
#27406=CARTESIAN_POINT ( 'NONE',  ( -1.881053915767121554, 16.62499999863440436, -4.541265875000002339 ) ) ;
#27435=CARTESIAN_POINT ( 'NONE',  ( -1.656854249492381248, 1.062499997268813168, -4.000000000000001776 ) ) ;
#27456=CARTESIAN_POINT ( 'NONE',  ( 2.828427124746190291, 21.87500000000000355, 2.828427124746192067 ) ) ;
#27457=CARTESIAN_POINT ( 'NONE',  ( 3.211159895383560947, 19.18749999863440436, 3.211159895383562723 ) ) ;
#27493=CARTESIAN_POINT ( 'NONE',  ( 1.656854249492381248, 17.93749999726881583, -4.000000000000001776 ) ) ;
#27526=DIRECTION ( 'NONE',  ( 0.000000000000000000, 0.000000000000000000, -1.000000000000000000 ) ) ;
#27543=CARTESIAN_POINT ( 'NONE',  ( -4.541265875000003227, 8.999999998634406140, 1.881053915767121110 ) ) ;
#27550=CARTESIAN_POINT ( 'NONE',  ( -4.000000000000001776, 8.437500000000000000, -1.656854249492381470 ) ) ;
#27551=CARTESIAN_POINT ( 'NONE',  ( 4.000000000000001776, 21.74999999726881583, 0.000000000000000000 ) ) ;
#27552=CARTESIAN_POINT ( 'NONE',  ( 3.211159895383561835, 7.437499998634407028, -3.211159895383561835 ) ) ;
#27633=CARTESIAN_POINT ( 'NONE',  ( 3.211159895383561835, 11.56249999863440614, -3.211159895383561835 ) ) ;
#27643=CARTESIAN_POINT ( 'NONE',  ( -1.656854249492383691, 9.437499997268815832, 4.000000000000000888 ) ) ;
#27649=CARTESIAN_POINT ( 'NONE',  ( -3.211159895383562723, 9.937499998634406140, 3.211159895383561391 ) ) ;
#27657=CARTESIAN_POINT ( 'NONE',  ( -1.656854249492383468, 18.68750000000000000, 4.000000000000000888 ) ) ;
#27667=VERTEX_POINT ( 'NONE', #20353 ) ;
#27692=CARTESIAN_POINT ( 'NONE',  ( 2.780723358947928197E-16, 8.687499998634407916, -4.541265875000002339 ) ) ;
#27722=DIRECTION ( 'NONE',  ( -0.000000000000000000, -1.000000000000000000, -0.000000000000000000 ) ) ;
#27735=CARTESIAN_POINT ( 'NONE',  ( 1.656854249492381914, 2.812500000000000000, 4.000000000000000888 ) ) ;
#27736=CARTESIAN_POINT ( 'NONE',  ( 4.541265875000002339, 15.49999999863440792, -1.881053915767121554 ) ) ;
#27745=DIRECTION ( 'NONE',  ( 0.000000000000000000, 0.000000000000000000, -1.000000000000000000 ) ) ;
#27760=CARTESIAN_POINT ( 'NONE',  ( -4.081160451454018734, 22.00000000000000000, 2.014106693209854804 ) ) ;
#27773=EDGE_CURVE ( 'NONE', #57934, #55774, #9510, .T. ) ;
#27780=CARTESIAN_POINT ( 'NONE',  ( -4.541265875000002339, 17.74999999863440792, -1.881053915767121998 ) ) ;
#27784=CARTESIAN_POINT ( 'NONE',  ( 2.449293598294707893E-16, 20.25000000000000000, -4.000000000000001776 ) ) ;
#27805=VECTOR ( 'NONE', #14951, 1000.000000000000000 ) ;
#27806=ORIENTED_EDGE ( 'NONE', *, *, #28356, .F. ) ;
#27822=B_SPLINE_CURVE_WITH_KNOTS ( 'NONE', 3,
 ( #29322, #41380, #52332, #23653, #64392, #30058, #53070, #64754, #47757, #70781, #71504, #14530, #25849, #31533, #37570, #36458, #13421, #18736, #60194, #59472, #3236, #36824 ),
 .UNSPECIFIED., .F., .F.,
 ( 4, 2, 2, 2, 2, 2, 2, 2, 2, 2, 4 ),
 ( 8.588689904434031851E-20, 0.001045978366599488755, 0.001568967549899233024, 0.002091956733198977510, 0.003137935099798465181, 0.004183913466397953286, 0.005229891832997441391, 0.005752881016297185443, 0.006275870199596930363, 0.007321848566196421070, 0.008367826932795910042 ),
 .UNSPECIFIED. ) ;
#27839=CARTESIAN_POINT ( 'NONE',  ( 4.000000000000000888, 18.93749999999999645, 1.656854249492384135 ) ) ;
#27840=CARTESIAN_POINT ( 'NONE',  ( -1.881053915767124440, 19.99999999863440436, 4.541265875000001451 ) ) ;
#27854=VERTEX_POINT ( 'NONE', #32829 ) ;
#27878=CARTESIAN_POINT ( 'NONE',  ( 1.656854249492381248, 17.18750000000000000, -4.000000000000001776 ) ) ;
#27881=CARTESIAN_POINT ( 'NONE',  ( 2.449293598294707893E-16, 1.250000000000000222, -4.000000000000001776 ) ) ;
#27924=CARTESIAN_POINT ( 'NONE',  ( 4.541265875000002339, 7.437499998634407028, 0.000000000000000000 ) ) ;
#27930=CARTESIAN_POINT ( 'NONE',  ( -2.828427124746192067, 8.625000000000000000, 2.828427124746190735 ) ) ;
#27931=CARTESIAN_POINT ( 'NONE',  ( 2.828427124746190291, 21.62499999726881583, 2.828427124746192067 ) ) ;
#27932=CARTESIAN_POINT ( 'NONE',  ( -4.541265875000002339, 9.749999998634404363, -1.881053915767121998 ) ) ;
#27940=CARTESIAN_POINT ( 'NONE',  ( -1.656854249492383468, 10.68750000000000000, 4.000000000000000888 ) ) ;
#27983=DIRECTION ( 'NONE',  ( 0.000000000000000000, 0.000000000000000000, -1.000000000000000000 ) ) ;
#28010=CARTESIAN_POINT ( 'NONE',  ( -1.881053915767121776, 11.74999999863440792, -4.541265875000002339 ) ) ;
#28020=CARTESIAN_POINT ( 'NONE',  ( -7.347880794884122694E-16, 11.49999999726881406, 4.000000000000001776 ) ) ;
#28028=CARTESIAN_POINT ( 'NONE',  ( 3.211159895383561835, 11.43749999863440614, -3.211159895383561835 ) ) ;
#28029=CARTESIAN_POINT ( 'NONE',  ( -1.656854249492381248, 18.06249999726881938, -4.000000000000001776 ) ) ;
#28032=CARTESIAN_POINT ( 'NONE',  ( 2.449293598294707893E-16, 20.99999999726881583, -4.000000000000001776 ) ) ;
#28042=VERTEX_POINT ( 'NONE', #64463 ) ;
#28068=CARTESIAN_POINT ( 'NONE',  ( -1.881053915767121554, 10.74999999863440969, -4.541265875000002339 ) ) ;
#28108=CARTESIAN_POINT ( 'NONE',  ( -3.211159895383562723, 19.06249999863440436, 3.211159895383561391 ) ) ;
#28156=CARTESIAN_POINT ( 'NONE',  ( -3.211159895383562723, 1.062499998634406806, 3.211159895383561391 ) ) ;
#28163=CARTESIAN_POINT ( 'NONE',  ( -8.000000000000003553, 22.99999999999999645, 1.000000000000000000 ) ) ;
#28165=DIRECTION ( 'NONE',  ( -0.000000000000000000, -1.000000000000000000, -0.000000000000000000 ) ) ;
#28211=CARTESIAN_POINT ( 'NONE',  ( -4.000000000000001776, 21.43750000000000000, -1.656854249492381470 ) ) ;
#28212=CARTESIAN_POINT ( 'NONE',  ( 2.828427124746190291, 2.624999997268812724, 2.828427124746192067 ) ) ;
#28216=CARTESIAN_POINT ( 'NONE',  ( -7.347880794884122694E-16, 4.499999997268813168, 4.000000000000001776 ) ) ;
#28243=ORIENTED_EDGE ( 'NONE', *, *, #32388, .F. ) ;
#28283=CARTESIAN_POINT ( 'NONE',  ( -7.347880794884122694E-16, 18.49999999726881583, 4.000000000000001776 ) ) ;
#28295=EDGE_CURVE ( 'NONE', #7053, #57749, #22941, .T. ) ;
#28296=CARTESIAN_POINT ( 'NONE',  ( -1.881053915767121554, 7.749999998634407916, -4.541265875000002339 ) ) ;
#28300=CARTESIAN_POINT ( 'NONE',  ( -2.828427124746192067, 7.625000000000000000, 2.828427124746190735 ) ) ;
#28302=CARTESIAN_POINT ( 'NONE',  ( 2.780723358947928197E-16, 6.562499998634407028, -4.541265875000002339 ) ) ;
#28327=DIRECTION ( 'NONE',  ( -0.000000000000000000, -1.000000000000000000, -0.000000000000000000 ) ) ;
#28328=ADVANCED_FACE ( 'NONE', ( #48570 ), #71580, .T. ) ;
#28356=EDGE_CURVE ( 'NONE', #60340, #31431, #37936, .T. ) ;
#28379=CARTESIAN_POINT ( 'NONE',  ( 1.881053915767122664, 13.24999999863440969, 4.541265875000001451 ) ) ;
#28390=CARTESIAN_POINT ( 'NONE',  ( -4.000000000000001776, 11.18749999726881406, -1.656854249492381470 ) ) ;
#28399=CARTESIAN_POINT ( 'NONE',  ( -3.211159895383561391, 9.687499998634406140, -3.211159895383561835 ) ) ;
#28400=CARTESIAN_POINT ( 'NONE',  ( 4.000000000000000888, 15.93750000000000000, 1.656854249492384135 ) ) ;
#28427=CARTESIAN_POINT ( 'NONE',  ( -7.347880794884122694E-16, 1.499999997268813168, 4.000000000000001776 ) ) ;
#28442=CARTESIAN_POINT ( 'NONE',  ( 1.881053915767122664, 14.24999999863440969, 4.541265875000001451 ) ) ;
#28458=DIRECTION ( 'NONE',  ( -0.000000000000000000, -1.000000000000000000, -0.000000000000000000 ) ) ;
#28485=CARTESIAN_POINT ( 'NONE',  ( -1.881053915767124440, 19.12499999863441147, 4.541265875000001451 ) ) ;
#28495=FACE_OUTER_BOUND ( 'NONE', #68078, .T. ) ;
#28523=CYLINDRICAL_SURFACE ( 'NONE', #48225, 4.000000000000001776 ) ;
#28528=CARTESIAN_POINT ( 'NONE',  ( -1.881053915767124440, 21.99999999863440792, 4.541265875000001451 ) ) ;
#28534=ORIENTED_EDGE ( 'NONE', *, *, #757, .T. ) ;
#28535=CARTESIAN_POINT ( 'NONE',  ( -1.656854249492381248, 19.06249999726881228, -4.000000000000001776 ) ) ;
#28556=CARTESIAN_POINT ( 'NONE',  ( 2.449293598294707893E-16, 9.999999997268814056, -4.000000000000001776 ) ) ;
#28563=CARTESIAN_POINT ( 'NONE',  ( -4.000000000000001776, 2.500000000000000000, -4.898587196589415787E-16 ) ) ;
#28585=CARTESIAN_POINT ( 'NONE',  ( 4.000000000000001776, 20.06250000000000355, -1.656854249492381248 ) ) ;
#28586=CARTESIAN_POINT ( 'NONE',  ( 4.000000000000001776, 2.812499997268813612, -1.656854249492381248 ) ) ;
#28599=ORIENTED_EDGE ( 'NONE', *, *, #29834, .F. ) ;
#28621=CARTESIAN_POINT ( 'NONE',  ( 1.881053915767122664, 12.12499999863440969, 4.541265875000001451 ) ) ;
#28660=CARTESIAN_POINT ( 'NONE',  ( 3.211159895383561835, 8.562499998634407916, -3.211159895383561835 ) ) ;
#28666=CARTESIAN_POINT ( 'NONE',  ( 1.656854249492381248, 8.187500000000000000, -4.000000000000001776 ) ) ;
#28668=CARTESIAN_POINT ( 'NONE',  ( -4.541265875000002339, 13.74999999863440969, -1.881053915767121998 ) ) ;
#28677=CARTESIAN_POINT ( 'NONE',  ( -4.541265875000002339, 21.81249999863440792, -5.561446717895856393E-16 ) ) ;
#28680=VERTEX_POINT ( 'NONE', #40619 ) ;
#28730=CARTESIAN_POINT ( 'NONE',  ( -4.000000000000001776, 20.24999999726881228, -4.898587196589415787E-16 ) ) ;
#28738=VERTEX_POINT ( 'NONE', #56865 ) ;
#28747=CARTESIAN_POINT ( 'NONE',  ( 4.541265875000002339, 11.49999999863440969, -1.881053915767121776 ) ) ;
#28760=CARTESIAN_POINT ( 'NONE',  ( -1.656854249492381248, 9.062499997268815832, -4.000000000000001776 ) ) ;
#28762=DIRECTION ( 'NONE',  ( -0.000000000000000000, -1.000000000000000000, -0.000000000000000000 ) ) ;
#28765=CARTESIAN_POINT ( 'NONE',  ( 1.881053915767121776, 10.49999999863440792, -4.541265875000002339 ) ) ;
#28770=DIRECTION ( 'NONE',  ( -0.000000000000000000, -1.000000000000000000, -0.000000000000000000 ) ) ;
#28790=CARTESIAN_POINT ( 'NONE',  ( 0.000000000000000000, 0.000000000000000000, 0.000000000000000000 ) ) ;
#28798=ORIENTED_EDGE ( 'NONE', *, *, #35904, .T. ) ;
#28810=CARTESIAN_POINT ( 'NONE',  ( -3.211159895383561391, 11.81249999863440614, -3.211159895383561835 ) ) ;
#28813=CARTESIAN_POINT ( 'NONE',  ( 4.000000000000001776, 7.812499997268812280, -1.656854249492381248 ) ) ;
#28826=CARTESIAN_POINT ( 'NONE',  ( 2.449293598294707893E-16, 15.25000000000000000, -4.000000000000001776 ) ) ;
#28853=CARTESIAN_POINT ( 'NONE',  ( 2.449293598294707893E-16, 3.250000000000000444, -4.000000000000001776 ) ) ;
#28854=CARTESIAN_POINT ( 'NONE',  ( -8.342170076843785083E-16, 18.18749999863440792, 4.541265875000002339 ) ) ;
#28896=CARTESIAN_POINT ( 'NONE',  ( 0.000000000000000000, 0.000000000000000000, 0.000000000000000000 ) ) ;
#28902=CARTESIAN_POINT ( 'NONE',  ( 3.211159895383560947, 22.18749999863440792, 3.211159895383562723 ) ) ;
#28913=CARTESIAN_POINT ( 'NONE',  ( 0.000000000000000000, 0.000000000000000000, -4.000000000000001776 ) ) ;
#28922=CARTESIAN_POINT ( 'NONE',  ( -7.347880794884122694E-16, 8.750000000000000000, 4.000000000000001776 ) ) ;
#28923=LINE ( 'NONE', #17221, #68961 ) ;
#28928=VERTEX_POINT ( 'NONE', #54913 ) ;
#28931=CARTESIAN_POINT ( 'NONE',  ( 1.656854249492394349, 9.562499997268814056, 3.999999999999988898 ) ) ;
#28993=CARTESIAN_POINT ( 'NONE',  ( 4.000000000000001776, 16.74999999726881583, 0.000000000000000000 ) ) ;
#28995=CARTESIAN_POINT ( 'NONE',  ( 4.541265875000002339, 8.374999998634406140, -1.881053915767121554 ) ) ;
#29029=FACE_OUTER_BOUND ( 'NONE', #18530, .T. ) ;
#29039=CARTESIAN_POINT ( 'NONE',  ( 4.541265875000002339, 11.49999999863440792, -1.881053915767121554 ) ) ;
#29043=CARTESIAN_POINT ( 'NONE',  ( -7.347880794884122694E-16, 13.75000000000000000, 4.000000000000001776 ) ) ;
#29044=CARTESIAN_POINT ( 'NONE',  ( -4.000000000000002665, 21.31249999726881228, 1.656854249492380804 ) ) ;
#29045=CARTESIAN_POINT ( 'NONE',  ( -1.881053915767124440, 12.99999999863440969, 4.541265875000001451 ) ) ;
#29057=CARTESIAN_POINT ( 'NONE',  ( 3.211159895383560947, 21.18749999863440792, 3.211159895383562723 ) ) ;
#29060=EDGE_LOOP ( 'NONE', ( #24926, #56113, #68899, #44461 ) ) ;
#29074=LINE ( 'NONE', #57012, #30182 ) ;
#29115=CARTESIAN_POINT ( 'NONE',  ( -7.347880794884122694E-16, 16.49999999726881228, 4.000000000000001776 ) ) ;
#29129=CARTESIAN_POINT ( 'NONE',  ( 1.881053915767121998, 12.62499999863441147, -4.541265875000002339 ) ) ;
#29140=CARTESIAN_POINT ( 'NONE',  ( 4.000000000000001776, 9.812499997268812280, -1.656854249492381248 ) ) ;
#29147=CARTESIAN_POINT ( 'NONE',  ( 4.541265875000002339, 9.312499998634407916, 0.000000000000000000 ) ) ;
#29151=VERTEX_POINT ( 'NONE', #63530 ) ;
#29195=CARTESIAN_POINT ( 'NONE',  ( 3.211159895383561835, 12.56249999863440792, -3.211159895383561835 ) ) ;
#29221=CARTESIAN_POINT ( 'NONE',  ( 3.211159895383561835, 0.5624999986344069169, -3.211159895383561835 ) ) ;
#29234=CARTESIAN_POINT ( 'NONE',  ( 1.881053915767122664, 20.24999999863440436, 4.541265875000001451 ) ) ;
#29235=UNCERTAINTY_MEASURE_WITH_UNIT (LENGTH_MEASURE( 1.000000000000000082E-05 ), #30986, 'distance_accuracy_value', 'NONE');
#29284=CARTESIAN_POINT ( 'NONE',  ( 4.541265875000002339, 1.499999998634407028, -1.881053915767121554 ) ) ;
#29301=DIRECTION ( 'NONE',  ( -0.000000000000000000, -1.000000000000000000, -0.000000000000000000 ) ) ;
#29311=CARTESIAN_POINT ( 'NONE',  ( -7.347880794884122694E-16, 9.499999997268814056, 4.000000000000001776 ) ) ;
#29317=ORIENTED_EDGE ( 'NONE', *, *, #38391, .F. ) ;
#29322=CARTESIAN_POINT ( 'NONE',  ( 4.000000000000002665, 22.00000000000000000, 0.000000000000000000 ) ) ;
#29378=CARTESIAN_POINT ( 'NONE',  ( 3.211159895383561835, 10.43749999863440792, -3.211159895383561835 ) ) ;
#29384=ORIENTED_EDGE ( 'NONE', *, *, #24789, .T. ) ;
#29420=CARTESIAN_POINT ( 'NONE',  ( -4.000000000000001776, 10.43750000000000000, -1.656854249492381470 ) ) ;
#29422=CARTESIAN_POINT ( 'NONE',  ( 1.881053915767121998, 11.49999999863440969, -4.541265875000002339 ) ) ;
#29433=ORIENTED_EDGE ( 'NONE', *, *, #68834, .T. ) ;
#29498=UNCERTAINTY_MEASURE_WITH_UNIT (LENGTH_MEASURE( 1.000000000000000082E-05 ), #16824, 'distance_accuracy_value', 'NONE');
#29502=CARTESIAN_POINT ( 'NONE',  ( 3.211159895383560947, 16.31249999863440436, 3.211159895383562723 ) ) ;
#29512=CARTESIAN_POINT ( 'NONE',  ( 4.000000000000001776, 12.74999999726881406, 0.000000000000000000 ) ) ;
#29514=ORIENTED_EDGE ( 'NONE', *, *, #48312, .F. ) ;
#29515=CYLINDRICAL_SURFACE ( 'NONE', #722, 4.000000000000001776 ) ;
#29519=CARTESIAN_POINT ( 'NONE',  ( -3.211159895383562723, 12.93749999863440792, 3.211159895383561391 ) ) ;
#29545=CARTESIAN_POINT ( 'NONE',  ( -4.541265875000002339, 1.749999998634406584, -1.881053915767121998 ) ) ;
#29546=CARTESIAN_POINT ( 'NONE',  ( 2.828427124746191623, 1.874999997268813390, -2.828427124746191623 ) ) ;
#29555=CARTESIAN_POINT ( 'NONE',  ( 0.000000000000000000, 0.000000000000000000, -4.000000000000001776 ) ) ;
#29562=CARTESIAN_POINT ( 'NONE',  ( 4.541265875000002339, 13.49999999863440969, -1.881053915767121554 ) ) ;
#29589=CARTESIAN_POINT ( 'NONE',  ( 4.541265875000002339, 1.437499998634406806, 0.000000000000000000 ) ) ;
#29591=EDGE_CURVE ( 'NONE', #282, #59211, #14110, .T. ) ;
#29601=CARTESIAN_POINT ( 'NONE',  ( 3.211159895383561835, 21.56249999863440792, -3.211159895383561835 ) ) ;
#29647=CARTESIAN_POINT ( 'NONE',  ( 4.541265875000002339, 21.31249999863440792, 0.000000000000000000 ) ) ;
#29664=CARTESIAN_POINT ( 'NONE',  ( -1.656854249492383468, 6.437499997268813168, 4.000000000000000888 ) ) ;
#29674=CARTESIAN_POINT ( 'NONE',  ( 1.656854249492381248, 9.937499997268814056, -4.000000000000001776 ) ) ;
#29738=CARTESIAN_POINT ( 'NONE',  ( -4.541265875000002339, 8.812499998634407916, -5.561446717895856393E-16 ) ) ;
#29780=PRODUCT_DEFINITION ( 'UNKNOWN', '', #17704, #38522 ) ;
#29786=CARTESIAN_POINT ( 'NONE',  ( 2.449293598294707893E-16, 10.25000000000000000, -4.000000000000001776 ) ) ;
#29789=CARTESIAN_POINT ( 'NONE',  ( -8.342170076843785083E-16, 10.06249999863440614, 4.541265875000002339 ) ) ;
#29796=CYLINDRICAL_SURFACE ( 'NONE', #3286, 4.000000000000001776 ) ;
#29815=CARTESIAN_POINT ( 'NONE',  ( 4.898587196589415787E-16, 0.000000000000000000, 4.000000000000001776 ) ) ;
#29834=EDGE_CURVE ( 'NONE', #66256, #10305, #63777, .T. ) ;
#29865=CARTESIAN_POINT ( 'NONE',  ( -4.000000000000001776, 8.500000000000000000, -4.898587196589415787E-16 ) ) ;
#29869=CARTESIAN_POINT ( 'NONE',  ( 4.541265875000002339, 15.49999999863440614, -1.881053915767121776 ) ) ;
#29879=CARTESIAN_POINT ( 'NONE',  ( -4.000000000000001776, 15.18749999726881406, -1.656854249492381470 ) ) ;
#29888=CARTESIAN_POINT ( 'NONE',  ( -4.541265875000002339, 14.74999999863440969, -1.881053915767121998 ) ) ;
#29914=CARTESIAN_POINT ( 'NONE',  ( 4.541265875000001451, 4.249999998634406140, 1.881053915767124440 ) ) ;
#29915=CARTESIAN_POINT ( 'NONE',  ( 0.000000000000000000, 0.000000000000000000, 0.000000000000000000 ) ) ;
#29917=CARTESIAN_POINT ( 'NONE',  ( 4.000000000000001776, 5.062500000000000888, -1.656854249492381248 ) ) ;
#29918=VERTEX_POINT ( 'NONE', #13921 ) ;
#29932=CARTESIAN_POINT ( 'NONE',  ( 1.881053915767122664, 18.24999999863440792, 4.541265875000001451 ) ) ;
#29959=CARTESIAN_POINT ( 'NONE',  ( -1.881053915767121776, 3.749999998634407028, -4.541265875000002339 ) ) ;
#29968=CARTESIAN_POINT ( 'NONE',  ( 4.000000000000001776, 0.8124999972688135008, -1.656854249492381248 ) ) ;
#29974=CARTESIAN_POINT ( 'NONE',  ( -3.211159895383561391, 3.687499998634407028, -3.211159895383561835 ) ) ;
#29978=ORIENTED_EDGE ( 'NONE', *, *, #70378, .F. ) ;
#29992=EDGE_CURVE ( 'NONE', #2415, #7053, #58214, .T. ) ;
#30020=CARTESIAN_POINT ( 'NONE',  ( -4.541265875000003227, 5.999999998634407028, 1.881053915767121110 ) ) ;
#30058=CARTESIAN_POINT ( 'NONE',  ( 3.746198271157959336, 21.99999999999999289, 1.721400972335161761 ) ) ;
#30110=CARTESIAN_POINT ( 'NONE',  ( -4.541265875000002339, 9.749999998634406140, -1.881053915767121998 ) ) ;
#30141=CARTESIAN_POINT ( 'NONE',  ( 4.000000000000001776, 21.81249999726881583, -1.656854249492381248 ) ) ;
#30147=SHAPE_REPRESENTATION ( 'screw', ( #57354 ), #58583 ) ;
#30152=CARTESIAN_POINT ( 'NONE',  ( -4.000000000000001776, 12.50000000000000000, -4.898587196589415787E-16 ) ) ;
#30154=CARTESIAN_POINT ( 'NONE',  ( -3.211159895383561391, 11.68749999863440614, -3.211159895383561835 ) ) ;
#30182=VECTOR ( 'NONE', #28327, 1000.000000000000000 ) ;
#30191=DIRECTION ( 'NONE',  ( -0.000000000000000000, -1.000000000000000000, -0.000000000000000000 ) ) ;
#30231=CARTESIAN_POINT ( 'NONE',  ( -1.656854249492381248, 8.312500000000000000, -4.000000000000001776 ) ) ;
#30235=CARTESIAN_POINT ( 'NONE',  ( -8.342170076843785083E-16, 16.18749999863440436, 4.541265875000002339 ) ) ;
#30244=CARTESIAN_POINT ( 'NONE',  ( -2.828427124746190735, 16.12499999726881228, -2.828427124746191623 ) ) ;
#30256=CARTESIAN_POINT ( 'NONE',  ( -1.881053915767121554, 13.62499999863440792, -4.541265875000002339 ) ) ;
#30257=CARTESIAN_POINT ( 'NONE',  ( 1.656854249492356157, 12.18749999999999645, -4.000000000000026645 ) ) ;
#30283=CARTESIAN_POINT ( 'NONE',  ( -4.541265875000003227, 1.874999998634406806, 1.881053915767121110 ) ) ;
#30301=CARTESIAN_POINT ( 'NONE',  ( 2.780723358947928197E-16, 16.68749999863440436, -4.541265875000002339 ) ) ;
#30314=VERTEX_POINT ( 'NONE', #9983 ) ;
#30325=CARTESIAN_POINT ( 'NONE',  ( 2.780723358947928197E-16, 4.687499998634407028, -4.541265875000002339 ) ) ;
#30336=CARTESIAN_POINT ( 'NONE',  ( -8.342170076843785083E-16, 22.18749999863440792, 4.541265875000002339 ) ) ;
#30343=CARTESIAN_POINT ( 'NONE',  ( 4.541265875000001451, 4.249999998634406140, 1.881053915767124440 ) ) ;
#30388=CARTESIAN_POINT ( 'NONE',  ( 4.541265875000002339, 3.499999998634407028, -1.881053915767121554 ) ) ;
#30402=CARTESIAN_POINT ( 'NONE',  ( -4.195582579073398932, 22.00000000000000355, 1.737867247408543925 ) ) ;
#30425=LINE ( 'NONE', #1766, #34264 ) ;
#30434=CARTESIAN_POINT ( 'NONE',  ( -3.211159895383561391, 11.81249999863440614, -3.211159895383561835 ) ) ;
#30478=CARTESIAN_POINT ( 'NONE',  ( -1.881053915767121554, 15.62499999863440614, -4.541265875000002339 ) ) ;
#30505=LINE ( 'NONE', #64475, #68602 ) ;
#30522=CARTESIAN_POINT ( 'NONE',  ( -4.000000000000001776, 13.43749999999999822, -1.656854249492381470 ) ) ;
#30524=CARTESIAN_POINT ( 'NONE',  ( -8.342170076843785083E-16, 17.06249999863440792, 4.541265875000002339 ) ) ;
#30531=( BOUNDED_CURVE ( )  B_SPLINE_CURVE ( 2, ( #8345, #52901, #31361, #64219, #70255, #12526, #18566, #30257, #53276 ),
 .UNSPECIFIED., .F., .F. ) 
 B_SPLINE_CURVE_WITH_KNOTS ( ( 3, 2, 2, 2, 3 ),
 ( 0.5340909090909090606, 0.5397727272727272929, 0.5454545454545454142, 0.5511363636363637575, 0.5568181818181818787 ),
 .UNSPECIFIED. ) 
 CURVE ( )  GEOMETRIC_REPRESENTATION_ITEM ( )  RATIONAL_B_SPLINE_CURVE ( ( 1.000000000000000000, 0.9238795325112867385, 1.000000000000000000, 0.9238795325112867385, 1.000000000000000000, 0.9238795325112867385, 1.000000000000000000, 0.9238795325112852952, 1.000000000000001554 ) ) 
 REPRESENTATION_ITEM ( '' )  );
#30561=CARTESIAN_POINT ( 'NONE',  ( -4.000000000000001776, 12.50000000000000000, -4.898587196589415787E-16 ) ) ;
#30567=ORIENTED_EDGE ( 'NONE', *, *, #21519, .F. ) ;
#30601=CARTESIAN_POINT ( 'NONE',  ( 2.780723358947928197E-16, 15.68749999863440436, -4.541265875000002339 ) ) ;
#30606=CARTESIAN_POINT ( 'NONE',  ( -8.342170076843785083E-16, 1.187499998634406806, 4.541265875000002339 ) ) ;
#30613=CARTESIAN_POINT ( 'NONE',  ( -4.000000000000001776, 16.18749999726881228, -1.656854249492381470 ) ) ;
#30614=CARTESIAN_POINT ( 'NONE',  ( 3.211159895383560947, 2.187499998634407028, 3.211159895383562723 ) ) ;
#30622=CARTESIAN_POINT ( 'NONE',  ( -1.881053915767124440, 13.99999999863440792, 4.541265875000001451 ) ) ;
#30634=EDGE_CURVE ( 'NONE', #21170, #39246, #53801, .T. ) ;
#30651=CARTESIAN_POINT ( 'NONE',  ( 1.881053915767121776, 3.499999998634407028, -4.541265875000002339 ) ) ;
#30669=CARTESIAN_POINT ( 'NONE',  ( 4.541265875000002339, 16.43749999863440436, 0.000000000000000000 ) ) ;
#30685=CARTESIAN_POINT ( 'NONE',  ( -4.000000000000001776, 17.43750000000000000, -1.656854249492381470 ) ) ;
#30694=CARTESIAN_POINT ( 'NONE',  ( 4.541265875000002339, 4.499999998634407028, -1.881053915767121776 ) ) ;
#30704=CARTESIAN_POINT ( 'NONE',  ( -1.881053915767124440, 22.12499999863441502, 4.541265875000001451 ) ) ;
#30710=CARTESIAN_POINT ( 'NONE',  ( 4.541265875000002339, 0.3749999986344066949, -1.881053915767121554 ) ) ;
#30726=EDGE_LOOP ( 'NONE', ( #39990, #64097, #58584, #40450 ) ) ;
#30753=CARTESIAN_POINT ( 'NONE',  ( 1.881053915767122664, 5.249999998634406140, 4.541265875000001451 ) ) ;
#30798=CARTESIAN_POINT ( 'NONE',  ( 3.211159895383560947, 12.31249999863440792, 3.211159895383562723 ) ) ;
#30840=CARTESIAN_POINT ( 'NONE',  ( -4.541265875000003227, 12.87499999863440969, 1.881053915767121110 ) ) ;
#30844=ORIENTED_EDGE ( 'NONE', *, *, #52704, .T. ) ;
#30848=VERTEX_POINT ( 'NONE', #9148 ) ;
#30857=CARTESIAN_POINT ( 'NONE',  ( -4.000000000000001776, 13.18749999726881583, -1.656854249492381470 ) ) ;
#30888=CARTESIAN_POINT ( 'NONE',  ( -7.347880794884122694E-16, 16.75000000000000000, 4.000000000000001776 ) ) ;
#30889=CARTESIAN_POINT ( 'NONE',  ( -8.342170076843785083E-16, 14.06249999863440614, 4.541265875000002339 ) ) ;
#30902=ORIENTED_EDGE ( 'NONE', *, *, #49917, .F. ) ;
#30922=CARTESIAN_POINT ( 'NONE',  ( -1.656854249492383468, 12.68750000000000178, 4.000000000000000888 ) ) ;
#30968=CARTESIAN_POINT ( 'NONE',  ( -4.541265875000002339, 18.87499999863441147, -1.881053915767121998 ) ) ;
#30975=( BOUNDED_CURVE ( )  B_SPLINE_CURVE ( 2, ( #69220, #27735, #46572, #57549, #50746, #4742, #34541, #5856, #28853 ),
 .UNSPECIFIED., .F., .F. ) 
 B_SPLINE_CURVE_WITH_KNOTS ( ( 3, 2, 2, 2, 3 ),
 ( 0.1250000000000000000, 0.1306818181818181768, 0.1363636363636363535, 0.1420454545454545581, 0.1477272727272727348 ),
 .UNSPECIFIED. ) 
 CURVE ( )  GEOMETRIC_REPRESENTATION_ITEM ( )  RATIONAL_B_SPLINE_CURVE ( ( 1.000000000000000000, 0.9238795325112867385, 1.000000000000000000, 0.9238795325112867385, 1.000000000000000000, 0.9238795325112867385, 1.000000000000000000, 0.9238795325112867385, 1.000000000000000000 ) ) 
 REPRESENTATION_ITEM ( '' )  );
#30977=CARTESIAN_POINT ( 'NONE',  ( -4.000000000000001776, 0.4375000000000002220, -1.656854249492381470 ) ) ;
#30978=CARTESIAN_POINT ( 'NONE',  ( 2.449293598294707893E-16, 14.99999999726881406, -4.000000000000001776 ) ) ;
#30979=CARTESIAN_POINT ( 'NONE',  ( 1.881053915767122664, 2.124999998634406584, 4.541265875000001451 ) ) ;
#30982=DIRECTION ( 'NONE',  ( -0.000000000000000000, -1.000000000000000000, -0.000000000000000000 ) ) ;
#30986=( LENGTH_UNIT ( ) NAMED_UNIT ( * ) SI_UNIT ( .MILLI., .METRE. ) );
#30988=CARTESIAN_POINT ( 'NONE',  ( -3.211159895383561391, 14.68749999863440792, -3.211159895383561835 ) ) ;
#31014=CARTESIAN_POINT ( 'NONE',  ( 4.541265875000001451, 1.249999998634407028, 1.881053915767124440 ) ) ;
#31018=VERTEX_POINT ( 'NONE', #53494 ) ;
#31033=CARTESIAN_POINT ( 'NONE',  ( 4.541265875000002339, 14.43749999863440792, 0.000000000000000000 ) ) ;
#31052=ORIENTED_EDGE ( 'NONE', *, *, #61987, .F. ) ;
#31054=CARTESIAN_POINT ( 'NONE',  ( -4.541265875000002339, 2.937499998634407028, -5.561446717895856393E-16 ) ) ;
#31065=CARTESIAN_POINT ( 'NONE',  ( 4.000000000000001776, 3.812499997268813168, -1.656854249492381248 ) ) ;
#31070=CARTESIAN_POINT ( 'NONE',  ( -3.211159895383562723, 2.937499998634407028, 3.211159895383561391 ) ) ;
#31101=CARTESIAN_POINT ( 'NONE',  ( 0.000000000000000000, 0.000000000000000000, -4.000000000000001776 ) ) ;
#31108=ADVANCED_FACE ( 'NONE', ( #61750 ), #2545, .T. ) ;
#31118=CARTESIAN_POINT ( 'NONE',  ( 1.881053915767121776, 2.624999998634407028, -4.541265875000002339 ) ) ;
#31166=CARTESIAN_POINT ( 'NONE',  ( 4.541265875000001451, 12.37499999863440969, 1.881053915767124440 ) ) ;
#31179=FACE_OUTER_BOUND ( 'NONE', #45869, .T. ) ;
#31212=CARTESIAN_POINT ( 'NONE',  ( -3.211159895383562723, 14.93749999863440792, 3.211159895383561391 ) ) ;
#31219=DIRECTION ( 'NONE',  ( -0.000000000000000000, -1.000000000000000000, -0.000000000000000000 ) ) ;
#31256=CARTESIAN_POINT ( 'NONE',  ( 4.000000000000000888, 14.93750000000000178, 1.656854249492384135 ) ) ;
#31258=CARTESIAN_POINT ( 'NONE',  ( -4.541265875000002339, 14.74999999863440969, -1.881053915767121998 ) ) ;
#31267=CARTESIAN_POINT ( 'NONE',  ( 1.656854249492381914, 6.562499997268813168, 4.000000000000000888 ) ) ;
#31304=CARTESIAN_POINT ( 'NONE',  ( -7.347880794884122694E-16, 8.499999997268814056, 4.000000000000001776 ) ) ;
#31337=CARTESIAN_POINT ( 'NONE',  ( 2.780723358947928197E-16, 21.68749999863440792, -4.541265875000002339 ) ) ;
#31340=CARTESIAN_POINT ( 'NONE',  ( -4.541265875000002339, 3.937499998634406584, -5.561446717895856393E-16 ) ) ;
#31349=CARTESIAN_POINT ( 'NONE',  ( -4.000000000000001776, 4.500000000000000888, -4.898587196589415787E-16 ) ) ;
#31350=CARTESIAN_POINT ( 'NONE',  ( 4.000000000000001776, 16.74999999726881583, 0.000000000000000000 ) ) ;
#31351=CARTESIAN_POINT ( 'NONE',  ( -4.541265875000003227, 1.874999998634406806, 1.881053915767121110 ) ) ;
#31359=CARTESIAN_POINT ( 'NONE',  ( -8.342170076843785083E-16, 20.06249999863440436, 4.541265875000002339 ) ) ;
#31361=CARTESIAN_POINT ( 'NONE',  ( 2.828427124746190291, 11.87500000000000000, 2.828427124746192067 ) ) ;
#31363=ORIENTED_EDGE ( 'NONE', *, *, #69600, .F. ) ;
#31390=CARTESIAN_POINT ( 'NONE',  ( -3.211159895383562723, 7.937499998634407028, 3.211159895383561391 ) ) ;
#31407=CARTESIAN_POINT ( 'NONE',  ( -3.211159895383561391, 14.81249999863440792, -3.211159895383561835 ) ) ;
#31414=CARTESIAN_POINT ( 'NONE',  ( 2.449293598294707893E-16, 11.99999999726881406, -4.000000000000001776 ) ) ;
#31431=VERTEX_POINT ( 'NONE', #28826 ) ;
#31433=CARTESIAN_POINT ( 'NONE',  ( -3.211159895383561391, 4.812499998634407028, -3.211159895383561835 ) ) ;
#31438=CYLINDRICAL_SURFACE ( 'NONE', #48061, 4.000000000000001776 ) ;
#31446=CARTESIAN_POINT ( 'NONE',  ( 1.656854249492381914, 2.562499997268814056, 4.000000000000000888 ) ) ;
#31454=CARTESIAN_POINT ( 'NONE',  ( -4.541265875000002339, 0.8124999986344066949, -5.561446717895856393E-16 ) ) ;
#31477=CARTESIAN_POINT ( 'NONE',  ( -4.000000000000001776, 17.24999999726881583, -4.898587196589415787E-16 ) ) ;
#31499=CARTESIAN_POINT ( 'NONE',  ( 1.881053915767122664, 4.249999998634406140, 4.541265875000001451 ) ) ;
#31510=CARTESIAN_POINT ( 'NONE',  ( 0.000000000000000000, 1.806524977843537691E-16, 0.000000000000000000 ) ) ;
#31533=CARTESIAN_POINT ( 'NONE',  ( 1.184329452913352121, 21.99999999999999289, 4.197665287320669236 ) ) ;
#31540=( BOUNDED_CURVE ( )  B_SPLINE_CURVE ( 2, ( #43437, #49095, #54030, #26450, #72108, #48722, #19680, #14387, #44200 ),
 .UNSPECIFIED., .F., .F. ) 
 B_SPLINE_CURVE_WITH_KNOTS ( ( 3, 2, 2, 2, 3 ),
 ( 0.2386363636363636465, 0.2443181818181818232, 0.2500000000000000000, 0.2556818181818181768, 0.2613636363636363535 ),
 .UNSPECIFIED. ) 
 CURVE ( )  GEOMETRIC_REPRESENTATION_ITEM ( )  RATIONAL_B_SPLINE_CURVE ( ( 1.000000000000000000, 0.9238795325112867385, 1.000000000000000000, 0.9238795325112867385, 1.000000000000000000, 0.9238795325112867385, 1.000000000000000000, 0.9238795325112867385, 1.000000000000000000 ) ) 
 REPRESENTATION_ITEM ( '' )  );
#31543=CARTESIAN_POINT ( 'NONE',  ( -3.211159895383562723, 10.06249999863440614, 3.211159895383561391 ) ) ;
#31572=FACE_OUTER_BOUND ( 'NONE', #30726, .T. ) ;
#31589=CARTESIAN_POINT ( 'NONE',  ( -3.211159895383561391, 12.68749999863440792, -3.211159895383561835 ) ) ;
#31628=AXIS2_PLACEMENT_3D ( 'NONE', #48580, #60658, #26696 ) ;
#31637=CARTESIAN_POINT ( 'NONE',  ( -4.000000000000002665, 14.56250000000000000, 1.656854249492380804 ) ) ;
#31638=CARTESIAN_POINT ( 'NONE',  ( 4.541265875000001451, 16.24999999863440436, 1.881053915767124440 ) ) ;
#31701=CARTESIAN_POINT ( 'NONE',  ( 2.449293598294707893E-16, 12.25000000000000000, -4.000000000000001776 ) ) ;
#31720=CARTESIAN_POINT ( 'NONE',  ( -1.881053915767121776, 21.74999999863440792, -4.541265875000002339 ) ) ;
#31723=CARTESIAN_POINT ( 'NONE',  ( -3.211159895383561391, 5.812499998634407028, -3.211159895383561835 ) ) ;
#31729=CARTESIAN_POINT ( 'NONE',  ( -2.828427124746192067, 2.625000000000000000, 2.828427124746190735 ) ) ;
#31730=CARTESIAN_POINT ( 'NONE',  ( -1.656854249492381248, 20.06249999726881228, -4.000000000000001776 ) ) ;
#31731=CARTESIAN_POINT ( 'NONE',  ( -4.541265875000003227, 4.874999998634406140, 1.881053915767121110 ) ) ;
#31738=CARTESIAN_POINT ( 'NONE',  ( 4.541265875000002339, 18.37499999863441147, -1.881053915767121554 ) ) ;
#31768=CARTESIAN_POINT ( 'NONE',  ( -1.881053915767124440, 6.999999998634407916, 4.541265875000001451 ) ) ;
#31776=CARTESIAN_POINT ( 'NONE',  ( 2.449293598294707893E-16, 19.99999999726881228, -4.000000000000001776 ) ) ;
#31787=CARTESIAN_POINT ( 'NONE',  ( 2.780723358947928197E-16, 19.68749999863440436, -4.541265875000002339 ) ) ;
#31812=CARTESIAN_POINT ( 'NONE',  ( 4.541265875000001451, 7.374999998634407916, 1.881053915767124440 ) ) ;
#31820=APPLICATION_CONTEXT ( 'automotive_design' ) ;
#31824=CARTESIAN_POINT ( 'NONE',  ( -4.000000000000001776, 5.249999997268813168, -4.898587196589415787E-16 ) ) ;
#31828=CARTESIAN_POINT ( 'NONE',  ( -1.881053915767124440, 7.999999998634407028, 4.541265875000001451 ) ) ;
#31861=VERTEX_POINT ( 'NONE', #21585 ) ;
#31869=AXIS2_PLACEMENT_3D ( 'NONE', #8149, #59835, #42099 ) ;
#31871=CARTESIAN_POINT ( 'NONE',  ( 3.211159895383560947, 8.312499998634407916, 3.211159895383562723 ) ) ;
#31876=VERTEX_POINT ( 'NONE', #74018 ) ;
#31917=CARTESIAN_POINT ( 'NONE',  ( -4.541265875000002339, 15.93749999863440436, -5.561446717895856393E-16 ) ) ;
#31950=ORIENTED_EDGE ( 'NONE', *, *, #989, .T. ) ;
#31960=CARTESIAN_POINT ( 'NONE',  ( 4.541265875000001451, 14.24999999863440969, 1.881053915767124440 ) ) ;
#32002=CARTESIAN_POINT ( 'NONE',  ( -1.656854249492405895, 20.31250000000000000, -3.999999999999976463 ) ) ;
#32008=ORIENTED_EDGE ( 'NONE', *, *, #55983, .F. ) ;
#32013=CARTESIAN_POINT ( 'NONE',  ( -4.000000000000001776, 15.50000000000000000, -4.898587196589415787E-16 ) ) ;
#32014=CARTESIAN_POINT ( 'NONE',  ( -4.541265875000003227, 16.87499999863440436, 1.881053915767121110 ) ) ;
#32017=ORIENTED_EDGE ( 'NONE', *, *, #29992, .F. ) ;
#32073=ORIENTED_EDGE ( 'NONE', *, *, #70064, .T. ) ;
#32090=EDGE_CURVE ( 'NONE', #47792, #56773, #27822, .T. ) ;
#32096=CARTESIAN_POINT ( 'NONE',  ( 4.541265875000001451, 21.37499999863441147, 1.881053915767124440 ) ) ;
#32099=CARTESIAN_POINT ( 'NONE',  ( -8.342170076843785083E-16, 4.187499998634407028, 4.541265875000002339 ) ) ;
#32108=CARTESIAN_POINT ( 'NONE',  ( 2.828427124746191623, 4.125000000000000000, -2.828427124746191623 ) ) ;
#32109=CARTESIAN_POINT ( 'NONE',  ( -4.000000000000001776, 20.24999999726881228, -4.898587196589415787E-16 ) ) ;
#32110=CARTESIAN_POINT ( 'NONE',  ( -8.342170076843785083E-16, 3.062499998634406584, 4.541265875000002339 ) ) ;
#32115=CARTESIAN_POINT ( 'NONE',  ( -4.541265875000002339, 16.74999999863440792, -1.881053915767121998 ) ) ;
#32118=ORIENTED_EDGE ( 'NONE', *, *, #61208, .T. ) ;
#32137=CARTESIAN_POINT ( 'NONE',  ( 0.000000000000000000, 0.000000000000000000, -4.000000000000001776 ) ) ;
#32146=CARTESIAN_POINT ( 'NONE',  ( 4.541265875000002339, 5.312499998634407028, 0.000000000000000000 ) ) ;
#32164=CARTESIAN_POINT ( 'NONE',  ( 4.541265875000002339, 19.43749999863440436, 0.000000000000000000 ) ) ;
#32188=CARTESIAN_POINT ( 'NONE',  ( 3.211159895383561835, 7.562499998634407028, -3.211159895383561835 ) ) ;
#32199=CARTESIAN_POINT ( 'NONE',  ( -7.347880794884122694E-16, 6.499999997268813168, 4.000000000000001776 ) ) ;
#32206=CARTESIAN_POINT ( 'NONE',  ( -1.881053915767121554, 6.624999998634407916, -4.541265875000002339 ) ) ;
#32208=CARTESIAN_POINT ( 'NONE',  ( -7.347880794884122694E-16, 13.75000000000000000, 4.000000000000001776 ) ) ;
#32215=FACE_OUTER_BOUND ( 'NONE', #10799, .T. ) ;
#32228=CARTESIAN_POINT ( 'NONE',  ( -7.347880794884122694E-16, 17.49999999726881583, 4.000000000000001776 ) ) ;
#32242=CARTESIAN_POINT ( 'NONE',  ( -4.000000000000002665, 7.312499997268813168, 1.656854249492380582 ) ) ;
#32253=CARTESIAN_POINT ( 'NONE',  ( -4.541265875000002339, 9.937499998634406140, -5.561446717895856393E-16 ) ) ;
#32257=CARTESIAN_POINT ( 'NONE',  ( -7.347880794884122694E-16, 5.499999997268813168, 4.000000000000001776 ) ) ;
#32296=CARTESIAN_POINT ( 'NONE',  ( 2.780723358947928197E-16, 14.68749999863440792, -4.541265875000002339 ) ) ;
#32334=LINE ( 'NONE', #66644, #27805 ) ;
#32335=ORIENTED_EDGE ( 'NONE', *, *, #58896, .F. ) ;
#32344=CARTESIAN_POINT ( 'NONE',  ( 4.541265875000002339, 20.31249999863440436, 0.000000000000000000 ) ) ;
#32359=CARTESIAN_POINT ( 'NONE',  ( 2.449293598294707893E-16, 8.999999997268814056, -4.000000000000001776 ) ) ;
#32388=EDGE_CURVE ( 'NONE', #25993, #30848, #57773, .T. ) ;
#32392=CARTESIAN_POINT ( 'NONE',  ( 2.449293598294707893E-16, 17.25000000000000000, -4.000000000000001776 ) ) ;
#32393=CARTESIAN_POINT ( 'NONE',  ( 1.881053915767122664, 19.12499999863441147, 4.541265875000001451 ) ) ;
#32397=ORIENTED_EDGE ( 'NONE', *, *, #68852, .T. ) ;
#32409=ORIENTED_EDGE ( 'NONE', *, *, #10238, .T. ) ;
#32474=CARTESIAN_POINT ( 'NONE',  ( 0.000000000000000000, 22.99999999999999645, 0.000000000000000000 ) ) ;
#32477=CARTESIAN_POINT ( 'NONE',  ( 4.541265875000002339, 19.49999999863440436, -1.881053915767121776 ) ) ;
#32481=CARTESIAN_POINT ( 'NONE',  ( 1.881053915767122664, 2.249999998634407028, 4.541265875000001451 ) ) ;
#32488=CARTESIAN_POINT ( 'NONE',  ( 2.449293598294707893E-16, 3.250000000000000444, -4.000000000000001776 ) ) ;
#32489=CARTESIAN_POINT ( 'NONE',  ( -1.656854249492383691, 18.43749999726881583, 4.000000000000000888 ) ) ;
#32490=CARTESIAN_POINT ( 'NONE',  ( -8.342170076843785083E-16, 7.062499998634407028, 4.541265875000002339 ) ) ;
#32497=CARTESIAN_POINT ( 'NONE',  ( 1.881053915767122664, 19.12499999863441147, 4.541265875000001451 ) ) ;
#32530=CARTESIAN_POINT ( 'NONE',  ( 3.211159895383561835, 7.437499998634407028, -3.211159895383561835 ) ) ;
#32548=CARTESIAN_POINT ( 'NONE',  ( 4.541265875000001451, 20.37499999863441147, 1.881053915767124440 ) ) ;
#32570=CARTESIAN_POINT ( 'NONE',  ( 3.211159895383560947, 9.312499998634407916, 3.211159895383562723 ) ) ;
#32583=CARTESIAN_POINT ( 'NONE',  ( 1.656854249492381248, 6.937499997268813168, -4.000000000000001776 ) ) ;
#32591=CARTESIAN_POINT ( 'NONE',  ( 3.211159895383560947, 7.187499998634407028, 3.211159895383562723 ) ) ;
#32611=DIRECTION ( 'NONE',  ( -0.000000000000000000, -1.000000000000000000, -0.000000000000000000 ) ) ;
#32634=CARTESIAN_POINT ( 'NONE',  ( 4.541265875000002339, 8.437499998634407916, 0.000000000000000000 ) ) ;
#32665=CARTESIAN_POINT ( 'NONE',  ( -2.828427124746192067, 4.625000000000000000, 2.828427124746190735 ) ) ;
#32668=CARTESIAN_POINT ( 'NONE',  ( -4.000000000000001776, 7.500000000000000000, -4.898587196589415787E-16 ) ) ;
#32681=CARTESIAN_POINT ( 'NONE',  ( -8.342170076843785083E-16, 15.18749999863440792, 4.541265875000002339 ) ) ;
#32723=CARTESIAN_POINT ( 'NONE',  ( -1.881053915767124440, 16.99999999863440792, 4.541265875000001451 ) ) ;
#32767=ORIENTED_EDGE ( 'NONE', *, *, #8700, .T. ) ;
#32773=CARTESIAN_POINT ( 'NONE',  ( 2.828427124746191623, 21.12500000000000000, -2.828427124746191623 ) ) ;
#32774=CARTESIAN_POINT ( 'NONE',  ( -1.881053915767124440, 18.99999999863440436, 4.541265875000001451 ) ) ;
#32807=PLANE ( 'NONE',  #8224 ) ;
#32829=CARTESIAN_POINT ( 'NONE',  ( 2.449293598294707893E-16, 17.99999999726881583, -4.000000000000001776 ) ) ;
#32861=CARTESIAN_POINT ( 'NONE',  ( -1.881053915767121554, 6.749999998634407916, -4.541265875000002339 ) ) ;
#32867=CARTESIAN_POINT ( 'NONE',  ( 1.656854249492381914, 5.812500000000000000, 4.000000000000000888 ) ) ;
#32868=CARTESIAN_POINT ( 'NONE',  ( 4.000000000000001776, 17.74999999726881583, 0.000000000000000000 ) ) ;
#32869=CARTESIAN_POINT ( 'NONE',  ( 4.541265875000002339, 8.312499998634407916, 0.000000000000000000 ) ) ;
#32876=CARTESIAN_POINT ( 'NONE',  ( -3.211159895383562723, 19.93749999863440436, 3.211159895383561391 ) ) ;
#32910=CARTESIAN_POINT ( 'NONE',  ( 2.780723358947928197E-16, 4.562499998634407028, -4.541265875000002339 ) ) ;
#32921=CARTESIAN_POINT ( 'NONE',  ( -7.347880794884122694E-16, 18.75000000000000000, 4.000000000000001776 ) ) ;
#32928=CARTESIAN_POINT ( 'NONE',  ( -3.211159895383562723, 22.06249999863440792, 3.211159895383561391 ) ) ;
#32949=CARTESIAN_POINT ( 'NONE',  ( 4.541265875000002339, 8.499999998634407916, -1.881053915767121776 ) ) ;
#32962=CARTESIAN_POINT ( 'NONE',  ( 2.828427124746190291, 6.624999997268813168, 2.828427124746192067 ) ) ;
#32969=CARTESIAN_POINT ( 'NONE',  ( -1.881053915767124440, 5.999999998634407028, 4.541265875000001451 ) ) ;
#32990=CARTESIAN_POINT ( 'NONE',  ( 0.000000000000000000, 0.000000000000000000, 0.000000000000000000 ) ) ;
#33010=( BOUNDED_CURVE ( )  B_SPLINE_CURVE ( 2, ( #17586, #34592, #46628, #17210, #22120, #40229, #57599, #12301, #63606 ),
 .UNSPECIFIED., .F., .F. ) 
 B_SPLINE_CURVE_WITH_KNOTS ( ( 3, 2, 2, 2, 3 ),
 ( 0.6704545454545455252, 0.6761363636363637575, 0.6818181818181817677, 0.6875000000000000000, 0.6931818181818182323 ),
 .UNSPECIFIED. ) 
 CURVE ( )  GEOMETRIC_REPRESENTATION_ITEM ( )  RATIONAL_B_SPLINE_CURVE ( ( 0.9999999999999985567, 0.9238795325112881818, 1.000000000000000000, 0.9238795325112867385, 1.000000000000000000, 0.9238795325112867385, 1.000000000000000000, 0.9238795325112867385, 1.000000000000000000 ) ) 
 REPRESENTATION_ITEM ( '' )  );
#33013=CARTESIAN_POINT ( 'NONE',  ( 3.211159895383560947, 9.312499998634407916, 3.211159895383562723 ) ) ;
#33016=CARTESIAN_POINT ( 'NONE',  ( 2.449293598294707893E-16, 4.999999997268813168, -4.000000000000001776 ) ) ;
#33059=EDGE_CURVE ( 'NONE', #28928, #8230, #26432, .T. ) ;
#33061=CARTESIAN_POINT ( 'NONE',  ( 4.541265875000001451, 16.37499999863440436, 1.881053915767124440 ) ) ;
#33104=CARTESIAN_POINT ( 'NONE',  ( -1.881053915767121554, 18.62499999863440792, -4.541265875000002339 ) ) ;
#33125=DIRECTION ( 'NONE',  ( 0.000000000000000000, 0.000000000000000000, -1.000000000000000000 ) ) ;
#33129=CARTESIAN_POINT ( 'NONE',  ( 1.656854249492406783, 14.81250000000000355, 3.999999999999976019 ) ) ;
#33139=CARTESIAN_POINT ( 'NONE',  ( -1.656854249492381248, 2.312500000000000888, -4.000000000000001776 ) ) ;
#33145=AXIS2_PLACEMENT_3D ( 'NONE', #39380, #3563, #73341 ) ;
#33157=CARTESIAN_POINT ( 'NONE',  ( -4.000000000000001776, 19.50000000000000000, -4.898587196589415787E-16 ) ) ;
#33158=CARTESIAN_POINT ( 'NONE',  ( 4.541265875000002339, 18.37499999863441147, -1.881053915767121776 ) ) ;
#33171=EDGE_LOOP ( 'NONE', ( #67343, #65168, #61332, #62033 ) ) ;
#33179=CARTESIAN_POINT ( 'NONE',  ( 4.000000000000000888, 13.93750000000000000, 1.656854249492384135 ) ) ;
#33227=ORIENTED_EDGE ( 'NONE', *, *, #64067, .T. ) ;
#33234=CARTESIAN_POINT ( 'NONE',  ( -4.541265875000002339, 8.874999998634407916, -1.881053915767121998 ) ) ;
#33240=CARTESIAN_POINT ( 'NONE',  ( -4.000000000000002665, 9.562500000000000000, 1.656854249492380804 ) ) ;
#33242=CARTESIAN_POINT ( 'NONE',  ( 3.211159895383560947, 7.187499998634407028, 3.211159895383562723 ) ) ;
#33249=CARTESIAN_POINT ( 'NONE',  ( -1.881053915767121554, 21.62499999863441502, -4.541265875000002339 ) ) ;
#33290=DIRECTION ( 'NONE',  ( -0.000000000000000000, -1.000000000000000000, -0.000000000000000000 ) ) ;
#33298=CARTESIAN_POINT ( 'NONE',  ( 3.211159895383560947, 20.31249999863440436, 3.211159895383562723 ) ) ;
#33319=CARTESIAN_POINT ( 'NONE',  ( 1.881053915767122664, 8.249999998634406140, 4.541265875000001451 ) ) ;
#33329=CARTESIAN_POINT ( 'NONE',  ( -1.656854249492381248, 8.062499997268812280, -4.000000000000001776 ) ) ;
#33331=CARTESIAN_POINT ( 'NONE',  ( 4.000000000000000888, 17.93750000000000355, 1.656854249492384135 ) ) ;
#33336=CARTESIAN_POINT ( 'NONE',  ( -8.342170076843785083E-16, 6.062499998634407028, 4.541265875000002339 ) ) ;
#33342=CARTESIAN_POINT ( 'NONE',  ( -1.656854249492381248, 18.31250000000000000, -4.000000000000001776 ) ) ;
#33366=CARTESIAN_POINT ( 'NONE',  ( -2.828427124746190735, 7.124999997268813168, -2.828427124746191623 ) ) ;
#33377=CARTESIAN_POINT ( 'NONE',  ( -3.211159895383561391, 7.812499998634407028, -3.211159895383561835 ) ) ;
#33400=EDGE_CURVE ( 'NONE', #34152, #27667, #35146, .T. ) ;
#33411=CARTESIAN_POINT ( 'NONE',  ( -4.000000000000002665, 7.562500000000000000, 1.656854249492380582 ) ) ;
#33422=CARTESIAN_POINT ( 'NONE',  ( -8.342170076843785083E-16, 14.18749999863440792, 4.541265875000002339 ) ) ;
#33430=VERTEX_POINT ( 'NONE', #6826 ) ;
#33432=CARTESIAN_POINT ( 'NONE',  ( 0.000000000000000000, 0.000000000000000000, 0.000000000000000000 ) ) ;
#33469=CARTESIAN_POINT ( 'NONE',  ( 3.211159895383560947, 17.18749999863440792, 3.211159895383562723 ) ) ;
#33502=CARTESIAN_POINT ( 'NONE',  ( -4.000000000000002665, 2.562500000000000444, 1.656854249492380582 ) ) ;
#33515=VERTEX_POINT ( 'NONE', #32359 ) ;
#33517=VECTOR ( 'NONE', #64171, 1000.000000000000000 ) ;
#33519=ADVANCED_FACE ( 'NONE', ( #21862 ), #57713, .T. ) ;
#33525=CARTESIAN_POINT ( 'NONE',  ( -1.656854249492383691, 20.68750000000000000, 4.000000000000000888 ) ) ;
#33526=CARTESIAN_POINT ( 'NONE',  ( -4.541265875000002339, 18.81249999863440436, -5.561446717895856393E-16 ) ) ;
#33556=CARTESIAN_POINT ( 'NONE',  ( 0.000000000000000000, 22.00000000000000000, 8.000000000000003553 ) ) ;
#33604=CARTESIAN_POINT ( 'NONE',  ( -3.211159895383561391, 8.812499998634407916, -3.211159895383561835 ) ) ;
#33611=CARTESIAN_POINT ( 'NONE',  ( 4.000000000000000888, 9.937499999999998224, 1.656854249492384135 ) ) ;
#33612=CARTESIAN_POINT ( 'NONE',  ( 2.828427124746191623, 20.87499999726881583, -2.828427124746191623 ) ) ;
#33613=CARTESIAN_POINT ( 'NONE',  ( -3.211159895383562723, 8.937499998634407916, 3.211159895383561391 ) ) ;
#33616=ORIENTED_EDGE ( 'NONE', *, *, #69028, .T. ) ;
#33621=CARTESIAN_POINT ( 'NONE',  ( -4.541265875000002339, 20.74999999863440436, -1.881053915767121998 ) ) ;
#33653=CARTESIAN_POINT ( 'NONE',  ( 1.656854249492381248, 11.93749999726881406, -4.000000000000001776 ) ) ;
#33675=CARTESIAN_POINT ( 'NONE',  ( -1.656854249492381248, 20.06249999726881228, -4.000000000000001776 ) ) ;
#33692=CARTESIAN_POINT ( 'NONE',  ( 4.541265875000002339, 12.49999999863440969, -1.881053915767121776 ) ) ;
#33702=CARTESIAN_POINT ( 'NONE',  ( 4.000000000000001776, 8.812499997268815832, -1.656854249492381248 ) ) ;
#33710=CARTESIAN_POINT ( 'NONE',  ( -4.541265875000002339, 9.812499998634406140, -5.561446717895856393E-16 ) ) ;
#33712=CARTESIAN_POINT ( 'NONE',  ( 2.449293598294707893E-16, 16.25000000000000000, -4.000000000000001776 ) ) ;
#33751=CARTESIAN_POINT ( 'NONE',  ( -1.881053915767124440, 11.12499999863440792, 4.541265875000001451 ) ) ;
#33754=CARTESIAN_POINT ( 'NONE',  ( 2.828427124746191623, 1.125000000000000444, -2.828427124746191623 ) ) ;
#33789=EDGE_CURVE ( 'NONE', #55561, #62160, #30505, .T. ) ;
#33798=CARTESIAN_POINT ( 'NONE',  ( -4.000000000000002665, 15.56249999999999822, 1.656854249492380582 ) ) ;
#33799=CARTESIAN_POINT ( 'NONE',  ( 4.541265875000002339, 20.43749999863440436, 0.000000000000000000 ) ) ;
#33843=CARTESIAN_POINT ( 'NONE',  ( -4.541265875000002339, 19.81249999863440436, -5.561446717895856393E-16 ) ) ;
#33846=( NAMED_UNIT ( * ) PLANE_ANGLE_UNIT ( ) SI_UNIT ( $, .RADIAN. ) );
#33877=CARTESIAN_POINT ( 'NONE',  ( -4.000000000000001776, 2.437500000000000444, -1.656854249492381470 ) ) ;
#33900=CARTESIAN_POINT ( 'NONE',  ( -7.347880794884122694E-16, 18.75000000000000000, 4.000000000000001776 ) ) ;
#33901=CARTESIAN_POINT ( 'NONE',  ( 1.881053915767122664, 18.12499999863441147, 4.541265875000001451 ) ) ;
#33914=VERTEX_POINT ( 'NONE', #48955 ) ;
#33915=VERTEX_POINT ( 'NONE', #71965 ) ;
#33918=CARTESIAN_POINT ( 'NONE',  ( 1.656854249492381248, 21.18750000000000000, -4.000000000000001776 ) ) ;
#33925=DIRECTION ( 'NONE',  ( 0.000000000000000000, 0.000000000000000000, -1.000000000000000000 ) ) ;
#33934=CARTESIAN_POINT ( 'NONE',  ( 4.000000000000001776, 17.74999999726881583, 0.000000000000000000 ) ) ;
#33953=EDGE_CURVE ( 'NONE', #62160, #13147, #49598, .T. ) ;
#33985=CARTESIAN_POINT ( 'NONE',  ( 1.881053915767122664, 8.249999998634406140, 4.541265875000001451 ) ) ;
#33991=CARTESIAN_POINT ( 'NONE',  ( 2.828427124746190291, 9.875000000000000000, 2.828427124746192067 ) ) ;
#33992=CARTESIAN_POINT ( 'NONE',  ( -4.000000000000002665, 22.31249999726881583, 1.656854249492380804 ) ) ;
#33993=CARTESIAN_POINT ( 'NONE',  ( 4.541265875000001451, 6.249999998634407916, 1.881053915767124440 ) ) ;
#34000=CARTESIAN_POINT ( 'NONE',  ( -4.541265875000003227, 21.87499999863441147, 1.881053915767121110 ) ) ;
#34040=CYLINDRICAL_SURFACE ( 'NONE', #64762, 4.000000000000001776 ) ;
#34069=CARTESIAN_POINT ( 'NONE',  ( -8.342170076843785083E-16, 12.18749999863440614, 4.541265875000002339 ) ) ;
#34079=CARTESIAN_POINT ( 'NONE',  ( 1.656854249492381248, 10.93749999726881406, -4.000000000000001776 ) ) ;
#34085=CARTESIAN_POINT ( 'NONE',  ( -1.881053915767124440, 9.999999998634407916, 4.541265875000001451 ) ) ;
#34125=CARTESIAN_POINT ( 'NONE',  ( 1.881053915767121776, 13.62499999863440792, -4.541265875000002339 ) ) ;
#34128=CARTESIAN_POINT ( 'NONE',  ( -4.000000000000001776, 4.187499997268813168, -1.656854249492381470 ) ) ;
#34152=VERTEX_POINT ( 'NONE', #41377 ) ;
#34165=CARTESIAN_POINT ( 'NONE',  ( -1.656854249492381248, 15.31249999999999822, -4.000000000000001776 ) ) ;
#34166=CARTESIAN_POINT ( 'NONE',  ( 4.541265875000002339, 18.49999999863440436, -1.881053915767121554 ) ) ;
#34193=DIRECTION ( 'NONE',  ( -0.000000000000000000, -1.000000000000000000, -0.000000000000000000 ) ) ;
#34196=FACE_OUTER_BOUND ( 'NONE', #9768, .T. ) ;
#34211=CARTESIAN_POINT ( 'NONE',  ( 1.881053915767122664, 22.12499999863441502, 4.541265875000001451 ) ) ;
#34238=CARTESIAN_POINT ( 'NONE',  ( 1.656854249492381248, 6.187500000000000000, -4.000000000000001776 ) ) ;
#34264=VECTOR ( 'NONE', #24747, 1000.000000000000000 ) ;
#34268=CARTESIAN_POINT ( 'NONE',  ( 2.828427124746190291, 19.87500000000000000, 2.828427124746192067 ) ) ;
#34304=CARTESIAN_POINT ( 'NONE',  ( 4.898587196589415787E-16, 0.000000000000000000, 4.000000000000001776 ) ) ;
#34306=CARTESIAN_POINT ( 'NONE',  ( 4.541265875000001451, 11.24999999863440792, 1.881053915767124440 ) ) ;
#34330=DIRECTION ( 'NONE',  ( 0.000000000000000000, 0.000000000000000000, -1.000000000000000000 ) ) ;
#34339=CARTESIAN_POINT ( 'NONE',  ( 4.000000000000001776, 18.74999999726881583, 0.000000000000000000 ) ) ;
#34353=CARTESIAN_POINT ( 'NONE',  ( -3.211159895383561391, 9.812499998634406140, -3.211159895383561835 ) ) ;
#34357=CARTESIAN_POINT ( 'NONE',  ( 2.828427124746191623, 8.125000000000000000, -2.828427124746191623 ) ) ;
#34358=CARTESIAN_POINT ( 'NONE',  ( -1.656854249492383691, 22.43749999726881583, 4.000000000000000888 ) ) ;
#34359=CARTESIAN_POINT ( 'NONE',  ( -1.881053915767121776, 11.62499999863440792, -4.541265875000002339 ) ) ;
#34368=CARTESIAN_POINT ( 'NONE',  ( 1.881053915767122664, 21.12499999863441147, 4.541265875000001451 ) ) ;
#34373=ORIENTED_EDGE ( 'NONE', *, *, #39302, .F. ) ;
#34402=CARTESIAN_POINT ( 'NONE',  ( 1.656854249492381914, 11.56249999726881406, 4.000000000000000888 ) ) ;
#34403=ORIENTED_EDGE ( 'NONE', *, *, #72395, .F. ) ;
#34442=CARTESIAN_POINT ( 'NONE',  ( 4.541265875000002339, 13.49999999863440792, -1.881053915767121776 ) ) ;
#34451=CARTESIAN_POINT ( 'NONE',  ( -2.828427124746192067, 8.374999997268814056, 2.828427124746190735 ) ) ;
#34459=DIRECTION ( 'NONE',  ( 1.000000000000000000, 0.000000000000000000, 0.000000000000000000 ) ) ;
#34460=CARTESIAN_POINT ( 'NONE',  ( 2.780723358947928197E-16, 10.56249999863440792, -4.541265875000002339 ) ) ;
#34504=CARTESIAN_POINT ( 'NONE',  ( 3.211159895383560947, 11.31249999863440792, 3.211159895383562723 ) ) ;
#34507=CARTESIAN_POINT ( 'NONE',  ( 1.656854249492381914, 7.562499997268812280, 4.000000000000000888 ) ) ;
#34531=CARTESIAN_POINT ( 'NONE',  ( 2.780723358947928197E-16, 1.687499998634406806, -4.541265875000002339 ) ) ;
#34541=CARTESIAN_POINT ( 'NONE',  ( 2.828427124746191623, 3.125000000000000000, -2.828427124746191623 ) ) ;
#34542=CARTESIAN_POINT ( 'NONE',  ( 1.881053915767121776, 20.62499999863441147, -4.541265875000002339 ) ) ;
#34586=CARTESIAN_POINT ( 'NONE',  ( 3.211159895383561835, 20.43749999863440436, -3.211159895383561835 ) ) ;
#34592=CARTESIAN_POINT ( 'NONE',  ( 1.656854249492406783, 15.56249999726881406, 3.999999999999976019 ) ) ;
#34634=EDGE_LOOP ( 'NONE', ( #34403, #4144, #56226, #18720 ) ) ;
#34642=ORIENTED_EDGE ( 'NONE', *, *, #72950, .T. ) ;
#34643=CARTESIAN_POINT ( 'NONE',  ( 3.211159895383561835, 3.437499998634407028, -3.211159895383561835 ) ) ;
#34644=CARTESIAN_POINT ( 'NONE',  ( -7.347880794884122694E-16, 2.499999997268813168, 4.000000000000001776 ) ) ;
#34679=CARTESIAN_POINT ( 'NONE',  ( 3.211159895383560947, 12.18749999863440614, 3.211159895383562723 ) ) ;
#34705=CARTESIAN_POINT ( 'NONE',  ( 4.000000000000000888, 18.68749999726881583, 1.656854249492384135 ) ) ;
#34721=CARTESIAN_POINT ( 'NONE',  ( -4.541265875000002339, 10.87499999863440792, -1.881053915767121998 ) ) ;
#34728=CARTESIAN_POINT ( 'NONE',  ( 2.828427124746191623, 9.125000000000000000, -2.828427124746191623 ) ) ;
#34729=CARTESIAN_POINT ( 'NONE',  ( -2.828427124746192067, 20.37499999726881228, 2.828427124746190735 ) ) ;
#34730=CARTESIAN_POINT ( 'NONE',  ( -1.881053915767124440, 9.999999998634407916, 4.541265875000001451 ) ) ;
#34795=CARTESIAN_POINT ( 'NONE',  ( -4.000000000000002665, 20.31249999726881228, 1.656854249492380582 ) ) ;
#34798=CARTESIAN_POINT ( 'NONE',  ( -4.000000000000001776, 3.437500000000000000, -1.656854249492381470 ) ) ;
#34810=CARTESIAN_POINT ( 'NONE',  ( 3.211159895383561835, 14.56249999863440792, -3.211159895383561835 ) ) ;
#34822=CARTESIAN_POINT ( 'NONE',  ( 4.000000000000001776, 9.749999997268814056, 0.000000000000000000 ) ) ;
#34823=CARTESIAN_POINT ( 'NONE',  ( -1.881053915767121776, 1.624999998634407028, -4.541265875000002339 ) ) ;
#34830=CARTESIAN_POINT ( 'NONE',  ( 2.780723358947928197E-16, 8.562499998634407916, -4.541265875000002339 ) ) ;
#34831=CARTESIAN_POINT ( 'NONE',  ( 2.449293598294707893E-16, 0.2500000000000001665, -4.000000000000001776 ) ) ;
#34847=ADVANCED_FACE ( 'NONE', ( #44476 ), #51621, .T. ) ;
#34858=CARTESIAN_POINT ( 'NONE',  ( 2.449293598294707893E-16, 1.999999997268813168, -4.000000000000001776 ) ) ;
#34873=CARTESIAN_POINT ( 'NONE',  ( 3.211159895383561835, 13.56249999863440614, -3.211159895383561835 ) ) ;
#34876=CARTESIAN_POINT ( 'NONE',  ( 1.656854249492381248, 7.937499997268813168, -4.000000000000001776 ) ) ;
#34902=CARTESIAN_POINT ( 'NONE',  ( 4.541265875000002339, 0.4999999986344068059, -1.881053915767121776 ) ) ;
#34914=CARTESIAN_POINT ( 'NONE',  ( 3.211159895383561835, 18.56249999863440436, -3.211159895383561835 ) ) ;
#34957=CARTESIAN_POINT ( 'NONE',  ( 2.780723358947928197E-16, 0.6874999986344068059, -4.541265875000002339 ) ) ;
#34964=CARTESIAN_POINT ( 'NONE',  ( -4.000000000000002665, 19.31249999726881228, 1.656854249492380582 ) ) ;
#34975=FACE_OUTER_BOUND ( 'NONE', #13751, .T. ) ;
#34982=ORIENTED_EDGE ( 'NONE', *, *, #13058, .F. ) ;
#35015=CARTESIAN_POINT ( 'NONE',  ( 2.828427124746191623, 2.874999997268813168, -2.828427124746191623 ) ) ;
#35049=CARTESIAN_POINT ( 'NONE',  ( 1.881053915767122664, 9.124999998634407916, 4.541265875000001451 ) ) ;
#35092=CARTESIAN_POINT ( 'NONE',  ( 4.000000000000001776, 12.06250000000000000, -1.656854249492381248 ) ) ;
#35095=CARTESIAN_POINT ( 'NONE',  ( -8.342170076843785083E-16, 11.06249999863440792, 4.541265875000002339 ) ) ;
#35146=LINE ( 'NONE', #70207, #33517 ) ;
#35176=CARTESIAN_POINT ( 'NONE',  ( -4.541265875000002339, 14.87499999863440969, -1.881053915767121998 ) ) ;
#35186=CARTESIAN_POINT ( 'NONE',  ( 4.000000000000000888, 12.68749999726881406, 1.656854249492384135 ) ) ;
#35194=CARTESIAN_POINT ( 'NONE',  ( 4.541265875000001451, 12.24999999863440969, 1.881053915767124440 ) ) ;
#35195=CARTESIAN_POINT ( 'NONE',  ( -7.347880794884122694E-16, 18.49999999726881583, 4.000000000000001776 ) ) ;
#35198=ORIENTED_EDGE ( 'NONE', *, *, #1189, .F. ) ;
#35221=CARTESIAN_POINT ( 'NONE',  ( -8.342170076843785083E-16, 2.062499998634406584, 4.541265875000002339 ) ) ;
#35237=CARTESIAN_POINT ( 'NONE',  ( 1.881053915767122664, 11.24999999863440792, 4.541265875000001451 ) ) ;
#35266=CARTESIAN_POINT ( 'NONE',  ( 2.780723358947928197E-16, 2.687499998634407028, -4.541265875000002339 ) ) ;
#35280=CARTESIAN_POINT ( 'NONE',  ( -4.541265875000002339, 19.93749999863440436, -5.561446717895856393E-16 ) ) ;
#35328=CARTESIAN_POINT ( 'NONE',  ( 3.211159895383561835, 21.43749999863440792, -3.211159895383561835 ) ) ;
#35350=ORIENTED_EDGE ( 'NONE', *, *, #64002, .T. ) ;
#35416=CARTESIAN_POINT ( 'NONE',  ( -3.211159895383561391, 9.687499998634406140, -3.211159895383561835 ) ) ;
#35425=VECTOR ( 'NONE', #2448, 1000.000000000000000 ) ;
#35456=CARTESIAN_POINT ( 'NONE',  ( 4.000000000000000888, 12.93750000000000000, 1.656854249492384135 ) ) ;
#35458=CARTESIAN_POINT ( 'NONE',  ( 1.881053915767122664, 13.12499999863440969, 4.541265875000001451 ) ) ;
#35471=EDGE_CURVE ( 'NONE', #58564, #56214, #52469, .T. ) ;
#35533=CARTESIAN_POINT ( 'NONE',  ( -2.828427124746190735, 8.375000000000000000, -2.828427124746191623 ) ) ;
#35537=CARTESIAN_POINT ( 'NONE',  ( -4.541265875000002339, 15.87499999863440436, -1.881053915767121998 ) ) ;
#35543=CIRCLE ( 'NONE', #2992, 9.949874371066211864 ) ;
#35548=CARTESIAN_POINT ( 'NONE',  ( -2.828427124746190735, 15.12499999726881406, -2.828427124746191623 ) ) ;
#35557=CARTESIAN_POINT ( 'NONE',  ( 2.780723358947928197E-16, 13.56249999863440614, -4.541265875000002339 ) ) ;
#35583=CARTESIAN_POINT ( 'NONE',  ( 3.211159895383560947, 4.187499998634407028, 3.211159895383562723 ) ) ;
#35595=DIRECTION ( 'NONE',  ( 0.000000000000000000, 0.000000000000000000, -1.000000000000000000 ) ) ;
#35600=CARTESIAN_POINT ( 'NONE',  ( -1.881053915767124440, 18.12499999863440792, 4.541265875000001451 ) ) ;
#35615=EDGE_LOOP ( 'NONE', ( #4077, #20491, #17355 ) ) ;
#35625=CARTESIAN_POINT ( 'NONE',  ( 2.780723358947928197E-16, 5.687499998634407028, -4.541265875000002339 ) ) ;
#35637=CARTESIAN_POINT ( 'NONE',  ( 2.449293598294707893E-16, 1.999999997268813168, -4.000000000000001776 ) ) ;
#35665=FACE_OUTER_BOUND ( 'NONE', #43979, .T. ) ;
#35685=CARTESIAN_POINT ( 'NONE',  ( -3.211159895383561391, 20.68749999863440436, -3.211159895383561835 ) ) ;
#35718=ORIENTED_EDGE ( 'NONE', *, *, #57482, .T. ) ;
#35745=CARTESIAN_POINT ( 'NONE',  ( -2.349324367397504609, 21.99999999999999645, -3.445024555465882266 ) ) ;
#35755=EDGE_CURVE ( 'NONE', #28680, #33915, #25462, .T. ) ;
#35777=CARTESIAN_POINT ( 'NONE',  ( -3.211159895383562723, 10.93749999863440792, 3.211159895383561391 ) ) ;
#35821=CARTESIAN_POINT ( 'NONE',  ( 2.828427124746190291, 11.87500000000000000, 2.828427124746192067 ) ) ;
#35823=CARTESIAN_POINT ( 'NONE',  ( -3.211159895383561391, 13.68749999863440614, -3.211159895383561835 ) ) ;
#35829=( BOUNDED_CURVE ( )  B_SPLINE_CURVE ( 2, ( #5397, #5032, #69138, #28400, #51407, #63469, #52167, #11793, #33712 ),
 .UNSPECIFIED., .F., .F. ) 
 B_SPLINE_CURVE_WITH_KNOTS ( ( 3, 2, 2, 2, 3 ),
 ( 0.7159090909090909394, 0.7215909090909090606, 0.7272727272727272929, 0.7329545454545454142, 0.7386363636363636465 ),
 .UNSPECIFIED. ) 
 CURVE ( )  GEOMETRIC_REPRESENTATION_ITEM ( )  RATIONAL_B_SPLINE_CURVE ( ( 1.000000000000000000, 0.9238795325112867385, 1.000000000000000000, 0.9238795325112867385, 1.000000000000000000, 0.9238795325112867385, 1.000000000000000000, 0.9238795325112867385, 1.000000000000000000 ) ) 
 REPRESENTATION_ITEM ( '' )  );
#35833=EDGE_CURVE ( 'NONE', #62884, #61146, #13032, .T. ) ;
#35847=CARTESIAN_POINT ( 'NONE',  ( -7.347880794884122694E-16, 0.7500000000000002220, 4.000000000000001776 ) ) ;
#35849=CARTESIAN_POINT ( 'NONE',  ( 7.071067811865484387, 22.99999999999999645, -1.000000000000000000 ) ) ;
#35893=CARTESIAN_POINT ( 'NONE',  ( -2.828427124746192067, 16.37499999726881228, 2.828427124746190735 ) ) ;
#35895=CARTESIAN_POINT ( 'NONE',  ( 0.000000000000000000, 0.000000000000000000, 0.000000000000000000 ) ) ;
#35904=EDGE_CURVE ( 'NONE', #25046, #7770, #68234, .T. ) ;
#35905=CARTESIAN_POINT ( 'NONE',  ( -3.211159895383562723, 17.06249999863440792, 3.211159895383561391 ) ) ;
#35914=CARTESIAN_POINT ( 'NONE',  ( -1.656854249492381248, 16.06249999726881228, -4.000000000000001776 ) ) ;
#35915=CARTESIAN_POINT ( 'NONE',  ( 4.541265875000001451, 1.249999998634407028, 1.881053915767124440 ) ) ;
#35916=VERTEX_POINT ( 'NONE', #30402 ) ;
#35924=CARTESIAN_POINT ( 'NONE',  ( -3.211159895383562723, 13.93749999863440614, 3.211159895383561391 ) ) ;
#35950=CARTESIAN_POINT ( 'NONE',  ( -1.881053915767124440, 0.9999999986344065839, 4.541265875000001451 ) ) ;
#35968=CARTESIAN_POINT ( 'NONE',  ( -4.541265875000002339, 15.87499999863440436, -1.881053915767121998 ) ) ;
#35996=CARTESIAN_POINT ( 'NONE',  ( 1.881053915767122664, 6.249999998634407916, 4.541265875000001451 ) ) ;
#36006=CARTESIAN_POINT ( 'NONE',  ( -2.828427124746192067, 3.374999997268813612, 2.828427124746190735 ) ) ;
#36011=CARTESIAN_POINT ( 'NONE',  ( -4.541265875000002339, 3.749999998634407028, -1.881053915767121998 ) ) ;
#36055=CARTESIAN_POINT ( 'NONE',  ( -1.881053915767121554, 2.749999998634406584, -4.541265875000002339 ) ) ;
#36069=DIRECTION ( 'NONE',  ( -0.000000000000000000, -1.000000000000000000, -0.000000000000000000 ) ) ;
#36101=CARTESIAN_POINT ( 'NONE',  ( -4.541265875000002339, 12.93749999863440792, -5.561446717895856393E-16 ) ) ;
#36129=CARTESIAN_POINT ( 'NONE',  ( 0.000000000000000000, 0.000000000000000000, -4.000000000000001776 ) ) ;
#36131=EDGE_CURVE ( 'NONE', #9782, #27854, #10366, .T. ) ;
#36143=CARTESIAN_POINT ( 'NONE',  ( -4.541265875000002339, 14.81249999863440792, -5.561446717895856393E-16 ) ) ;
#36149=ORIENTED_EDGE ( 'NONE', *, *, #40779, .T. ) ;
#36151=LINE ( 'NONE', #58800, #56955 ) ;
#36171=LINE ( 'NONE', #52780, #58167 ) ;
#36173=CARTESIAN_POINT ( 'NONE',  ( -7.240284387734133737E-08, 22.00000000000001066, -4.000000000000000888 ) ) ;
#36190=CARTESIAN_POINT ( 'NONE',  ( -2.828427124746190735, 13.37500000000000000, -2.828427124746191623 ) ) ;
#36192=CARTESIAN_POINT ( 'NONE',  ( 4.541265875000001451, 15.24999999863440969, 1.881053915767124440 ) ) ;
#36205=VERTEX_POINT ( 'NONE', #50717 ) ;
#36216=CARTESIAN_POINT ( 'NONE',  ( -7.347880794884122694E-16, 2.499999997268813168, 4.000000000000001776 ) ) ;
#36233=DIRECTION ( 'NONE',  ( 1.000000000000000000, 0.000000000000000000, 0.000000000000000000 ) ) ;
#36271=CARTESIAN_POINT ( 'NONE',  ( -8.342170076843785083E-16, 17.18749999863440792, 4.541265875000002339 ) ) ;
#36280=CARTESIAN_POINT ( 'NONE',  ( -4.000000000000001776, 1.500000000000000222, -4.898587196589415787E-16 ) ) ;
#36281=CARTESIAN_POINT ( 'NONE',  ( -4.000000000000001776, 13.24999999726881406, -4.898587196589415787E-16 ) ) ;
#36283=ORIENTED_EDGE ( 'NONE', *, *, #55653, .T. ) ;
#36288=( NAMED_UNIT ( * ) PLANE_ANGLE_UNIT ( ) SI_UNIT ( $, .RADIAN. ) );
#36290=CARTESIAN_POINT ( 'NONE',  ( -4.541265875000003227, 12.87499999863440969, 1.881053915767121110 ) ) ;
#36301=LINE ( 'NONE', #24954, #39822 ) ;
#36311=CARTESIAN_POINT ( 'NONE',  ( 2.449293598294707893E-16, 8.250000000000000000, -4.000000000000001776 ) ) ;
#36320=CARTESIAN_POINT ( 'NONE',  ( -4.541265875000002339, 2.749999998634406584, -1.881053915767121998 ) ) ;
#36337=CARTESIAN_POINT ( 'NONE',  ( 4.541265875000001451, 15.37499999863440969, 1.881053915767124440 ) ) ;
#36352=CARTESIAN_POINT ( 'NONE',  ( -1.656854249492358155, 17.68750000000000355, 4.000000000000024869 ) ) ;
#36360=CARTESIAN_POINT ( 'NONE',  ( -4.541265875000002339, 3.937499998634406584, -5.561446717895856393E-16 ) ) ;
#36369=CARTESIAN_POINT ( 'NONE',  ( -1.656854249492381248, 4.062499997268813168, -4.000000000000001776 ) ) ;
#36376=CARTESIAN_POINT ( 'NONE',  ( -8.342170076843785083E-16, 1.062499998634406584, 4.541265875000002339 ) ) ;
#36422=CARTESIAN_POINT ( 'NONE',  ( 3.211159895383560947, 6.312499998634407028, 3.211159895383562723 ) ) ;
#36458=CARTESIAN_POINT ( 'NONE',  ( 0.6771042881593288820, 22.00000000000000355, 4.342542294227817123 ) ) ;
#36466=CARTESIAN_POINT ( 'NONE',  ( -1.881053915767121554, 13.74999999863440969, -4.541265875000002339 ) ) ;
#36491=ORIENTED_EDGE ( 'NONE', *, *, #53181, .T. ) ;
#36513=CARTESIAN_POINT ( 'NONE',  ( -4.541265875000002339, 13.74999999863440969, -1.881053915767121998 ) ) ;
#36555=CARTESIAN_POINT ( 'NONE',  ( -2.828427124746192067, 17.62500000000000000, 2.828427124746190735 ) ) ;
#36556=CARTESIAN_POINT ( 'NONE',  ( -3.211159895383561391, 17.68749999863440792, -3.211159895383561835 ) ) ;
#36560=EDGE_LOOP ( 'NONE', ( #58123, #18764, #32118, #51695 ) ) ;
#36564=CARTESIAN_POINT ( 'NONE',  ( 4.000000000000001776, 13.81249999726881406, -1.656854249492381248 ) ) ;
#36604=CARTESIAN_POINT ( 'NONE',  ( -1.656854249492371034, 8.437499997268815832, 4.000000000000013323 ) ) ;
#36623=( BOUNDED_CURVE ( )  B_SPLINE_CURVE ( 2, ( #52384, #719, #17295, #52012, #23330, #39575, #39943, #74648, #62570 ),
 .UNSPECIFIED., .F., .F. ) 
 B_SPLINE_CURVE_WITH_KNOTS ( ( 3, 2, 2, 2, 3 ),
 ( 0.4431818181818181768, 0.4488636363636363535, 0.4545454545454545858, 0.4602272727272727626, 0.4659090909090909394 ),
 .UNSPECIFIED. ) 
 CURVE ( )  GEOMETRIC_REPRESENTATION_ITEM ( )  RATIONAL_B_SPLINE_CURVE ( ( 1.000000000000000000, 0.9238795325112867385, 1.000000000000000000, 0.9238795325112867385, 1.000000000000000000, 0.9238795325112867385, 1.000000000000000000, 0.9238795325112859613, 1.000000000000000666 ) ) 
 REPRESENTATION_ITEM ( '' )  );
#36639=CARTESIAN_POINT ( 'NONE',  ( 1.881053915767121998, 17.62499999863440436, -4.541265875000002339 ) ) ;
#36642=AXIS2_PLACEMENT_3D ( 'NONE', #59855, #60967, #25134 ) ;
#36650=CARTESIAN_POINT ( 'NONE',  ( -7.347880794884122694E-16, 13.49999999726881406, 4.000000000000001776 ) ) ;
#36651=CARTESIAN_POINT ( 'NONE',  ( 4.541265875000001451, 4.249999998634407028, 1.881053915767124440 ) ) ;
#36659=CARTESIAN_POINT ( 'NONE',  ( 3.211159895383560947, 13.18749999863440792, 3.211159895383562723 ) ) ;
#36663=ORIENTED_EDGE ( 'NONE', *, *, #12476, .F. ) ;
#36679=LINE ( 'NONE', #32137, #37019 ) ;
#36688=CARTESIAN_POINT ( 'NONE',  ( 2.780723358947928197E-16, 3.562499998634407028, -4.541265875000002339 ) ) ;
#36698=DIRECTION ( 'NONE',  ( -0.000000000000000000, -1.000000000000000000, -0.000000000000000000 ) ) ;
#36705=CARTESIAN_POINT ( 'NONE',  ( -8.342170076843785083E-16, 15.18749999863440792, 4.541265875000002339 ) ) ;
#36708=ORIENTED_EDGE ( 'NONE', *, *, #33059, .T. ) ;
#36728=CARTESIAN_POINT ( 'NONE',  ( -8.342170076843785083E-16, 5.187499998634407028, 4.541265875000002339 ) ) ;
#36731=EDGE_CURVE ( 'NONE', #16346, #68294, #66996, .T. ) ;
#36741=CARTESIAN_POINT ( 'NONE',  ( 2.449293598294707893E-16, 9.250000000000000000, -4.000000000000001776 ) ) ;
#36742=CARTESIAN_POINT ( 'NONE',  ( -4.000000000000001776, 1.187499997268813390, -1.656854249492381470 ) ) ;
#36747=CARTESIAN_POINT ( 'NONE',  ( -1.881053915767124440, 1.999999998634406806, 4.541265875000001451 ) ) ;
#36770=DIRECTION ( 'NONE',  ( 0.000000000000000000, -0.000000000000000000, 1.000000000000000000 ) ) ;
#36790=CARTESIAN_POINT ( 'NONE',  ( -3.211159895383562723, 4.062499998634407028, 3.211159895383561391 ) ) ;
#36824=CARTESIAN_POINT ( 'NONE',  ( -1.737867177246331662, 21.99999999999999645, 4.195582608135537406 ) ) ;
#36838=CARTESIAN_POINT ( 'NONE',  ( -3.211159895383562723, 12.06249999863440614, 3.211159895383561391 ) ) ;
#36858=CARTESIAN_POINT ( 'NONE',  ( -1.656854249492381248, 9.062499997268812280, -4.000000000000001776 ) ) ;
#36864=CYLINDRICAL_SURFACE ( 'NONE', #14342, 4.000000000000001776 ) ;
#36874=CARTESIAN_POINT ( 'NONE',  ( 4.898587196589415787E-16, 0.000000000000000000, 4.000000000000001776 ) ) ;
#36879=CARTESIAN_POINT ( 'NONE',  ( -1.881053915767121554, 13.62499999863440792, -4.541265875000002339 ) ) ;
#36896=DIRECTION ( 'NONE',  ( -0.000000000000000000, -1.000000000000000000, -0.000000000000000000 ) ) ;
#36923=CARTESIAN_POINT ( 'NONE',  ( 2.449293598294707893E-16, 6.999999997268813168, -4.000000000000001776 ) ) ;
#36924=CARTESIAN_POINT ( 'NONE',  ( 4.000000000000001776, 16.06250000000000000, -1.656854249492381248 ) ) ;
#36925=CARTESIAN_POINT ( 'NONE',  ( -3.211159895383562723, 13.93749999863440614, 3.211159895383561391 ) ) ;
#36964=CARTESIAN_POINT ( 'NONE',  ( -2.828427124746190735, 6.375000000000000888, -2.828427124746191623 ) ) ;
#36967=ORIENTED_EDGE ( 'NONE', *, *, #53007, .T. ) ;
#37010=CARTESIAN_POINT ( 'NONE',  ( 4.541265875000002339, 4.499999998634407028, -1.881053915767121554 ) ) ;
#37016=CARTESIAN_POINT ( 'NONE',  ( 2.828427124746191623, 5.125000000000000000, -2.828427124746191623 ) ) ;
#37017=CARTESIAN_POINT ( 'NONE',  ( 2.828427124746191623, 17.87499999726881583, -2.828427124746191623 ) ) ;
#37018=CARTESIAN_POINT ( 'NONE',  ( 2.780723358947928197E-16, 2.562499998634407028, -4.541265875000002339 ) ) ;
#37019=VECTOR ( 'NONE', #20803, 1000.000000000000000 ) ;
#37025=CARTESIAN_POINT ( 'NONE',  ( 4.541265875000002339, 15.37499999863440614, -1.881053915767121554 ) ) ;
#37053=CARTESIAN_POINT ( 'NONE',  ( -4.541265875000002339, 4.749999998634407028, -1.881053915767121998 ) ) ;
#37071=CARTESIAN_POINT ( 'NONE',  ( 2.780723358947928197E-16, 17.68749999863440792, -4.541265875000002339 ) ) ;
#37096=CARTESIAN_POINT ( 'NONE',  ( 1.881053915767121998, 6.624999998634407916, -4.541265875000002339 ) ) ;
#37109=CARTESIAN_POINT ( 'NONE',  ( 2.828427124746191623, 0.8749999972688131678, -2.828427124746191623 ) ) ;
#37110=ORIENTED_EDGE ( 'NONE', *, *, #50786, .F. ) ;
#37113=CARTESIAN_POINT ( 'NONE',  ( 2.780723358947928197E-16, 1.562499998634406584, -4.541265875000002339 ) ) ;
#37115=ADVANCED_FACE ( 'NONE', ( #18537 ), #41545, .T. ) ;
#37122=DIRECTION ( 'NONE',  ( -0.000000000000000000, -1.000000000000000000, -0.000000000000000000 ) ) ;
#37136=DIRECTION ( 'NONE',  ( -0.000000000000000000, -1.000000000000000000, -0.000000000000000000 ) ) ;
#37150=LINE ( 'NONE', #20529, #35425 ) ;
#37158=CARTESIAN_POINT ( 'NONE',  ( 4.541265875000001451, 5.374999998634406140, 1.881053915767124440 ) ) ;
#37205=CARTESIAN_POINT ( 'NONE',  ( -3.211159895383561391, 13.81249999863440614, -3.211159895383561835 ) ) ;
#37228=CARTESIAN_POINT ( 'NONE',  ( -4.000000000000001776, 2.187499997268813168, -1.656854249492381470 ) ) ;
#37251=CARTESIAN_POINT ( 'NONE',  ( 3.211159895383560947, 15.18749999863440792, 3.211159895383562723 ) ) ;
#37255=CARTESIAN_POINT ( 'NONE',  ( -9.797174393178831574E-16, 22.00000000000000355, -8.000000000000003553 ) ) ;
#37284=CARTESIAN_POINT ( 'NONE',  ( 1.656854249492381248, 3.937499997268813168, -4.000000000000001776 ) ) ;
#37299=CARTESIAN_POINT ( 'NONE',  ( 4.000000000000001776, 18.06250000000000000, -1.656854249492381248 ) ) ;
#37300=CARTESIAN_POINT ( 'NONE',  ( 3.211159895383561835, 14.43749999863440792, -3.211159895383561835 ) ) ;
#37324=CARTESIAN_POINT ( 'NONE',  ( 2.828427124746190291, 13.87500000000000000, 2.828427124746192067 ) ) ;
#37377=CARTESIAN_POINT ( 'NONE',  ( 1.881053915767121998, 20.62499999863441147, -4.541265875000002339 ) ) ;
#37380=CARTESIAN_POINT ( 'NONE',  ( 3.211159895383561835, 2.562499998634407028, -3.211159895383561835 ) ) ;
#37384=( BOUNDED_CURVE ( )  B_SPLINE_CURVE ( 2, ( #22488, #28535, #23248, #51543, #74561, #34964, #6284, #24356, #47727 ),
 .UNSPECIFIED., .F., .F. ) 
 B_SPLINE_CURVE_WITH_KNOTS ( ( 3, 2, 2, 2, 3 ),
 ( 0.8295454545454545858, 0.8352272727272727071, 0.8409090909090909394, 0.8465909090909090606, 0.8522727272727272929 ),
 .UNSPECIFIED. ) 
 CURVE ( )  GEOMETRIC_REPRESENTATION_ITEM ( )  RATIONAL_B_SPLINE_CURVE ( ( 1.000000000000000000, 0.9238795325112867385, 1.000000000000000000, 0.9238795325112867385, 1.000000000000000000, 0.9238795325112867385, 1.000000000000000000, 0.9238795325112867385, 1.000000000000000000 ) ) 
 REPRESENTATION_ITEM ( '' )  );
#37390=CARTESIAN_POINT ( 'NONE',  ( -2.828427124746190735, 3.375000000000000000, -2.828427124746191623 ) ) ;
#37391=CARTESIAN_POINT ( 'NONE',  ( 4.000000000000000888, 16.68749999726881583, 1.656854249492384135 ) ) ;
#37392=CARTESIAN_POINT ( 'NONE',  ( -3.211159895383561391, 4.687499998634407028, -3.211159895383561835 ) ) ;
#37398=CARTESIAN_POINT ( 'NONE',  ( -3.211159895383562723, 16.93749999863440436, 3.211159895383561391 ) ) ;
#37404=DIRECTION ( 'NONE',  ( -0.000000000000000000, -1.000000000000000000, -0.000000000000000000 ) ) ;
#37424=CARTESIAN_POINT ( 'NONE',  ( -2.828427124746190735, 3.124999997268813168, -2.828427124746191623 ) ) ;
#37430=CARTESIAN_POINT ( 'NONE',  ( -4.541265875000002339, 6.749999998634407916, -1.881053915767121998 ) ) ;
#37447=CARTESIAN_POINT ( 'NONE',  ( -4.541265875000002339, 18.87499999863441147, -1.881053915767121998 ) ) ;
#37457=DIRECTION ( 'NONE',  ( 0.000000000000000000, 0.000000000000000000, -1.000000000000000000 ) ) ;
#37469=CARTESIAN_POINT ( 'NONE',  ( -3.211159895383562723, 8.062499998634406140, 3.211159895383561391 ) ) ;
#37483=CARTESIAN_POINT ( 'NONE',  ( 2.828427124746190291, 5.624999997268813168, 2.828427124746192067 ) ) ;
#37489=CARTESIAN_POINT ( 'NONE',  ( -4.541265875000002339, 7.812499998634407028, -5.561446717895856393E-16 ) ) ;
#37496=ORIENTED_EDGE ( 'NONE', *, *, #1189, .T. ) ;
#37533=CIRCLE ( 'NONE', #55641, 7.141428428542858420 ) ;
#37535=CARTESIAN_POINT ( 'NONE',  ( 1.881053915767121776, 8.624999998634406140, -4.541265875000002339 ) ) ;
#37546=ORIENTED_EDGE ( 'NONE', *, *, #10238, .F. ) ;
#37547=EDGE_CURVE ( 'NONE', #45848, #65881, #44447, .T. ) ;
#37551=CARTESIAN_POINT ( 'NONE',  ( -7.347880794884122694E-16, 6.499999997268813168, 4.000000000000001776 ) ) ;
#37566=DIRECTION ( 'NONE',  ( -0.000000000000000000, -1.000000000000000000, -0.000000000000000000 ) ) ;
#37569=VECTOR ( 'NONE', #31219, 1000.000000000000000 ) ;
#37570=CARTESIAN_POINT ( 'NONE',  ( 1.015769982161393470, 21.99999999999999645, 4.253290409823233809 ) ) ;
#37579=DIRECTION ( 'NONE',  ( 0.000000000000000000, 0.000000000000000000, -1.000000000000000000 ) ) ;
#37580=CARTESIAN_POINT ( 'NONE',  ( 2.780723358947928197E-16, 15.68749999863440436, -4.541265875000002339 ) ) ;
#37617=CIRCLE ( 'NONE', #6288, 9.949874371066211864 ) ;
#37628=CARTESIAN_POINT ( 'NONE',  ( -4.541265875000002339, 15.81249999863440436, -5.561446717895856393E-16 ) ) ;
#37660=CARTESIAN_POINT ( 'NONE',  ( 4.000000000000001776, 3.812499997268813168, -1.656854249492381248 ) ) ;
#37679=CARTESIAN_POINT ( 'NONE',  ( -2.828427124746192067, 16.62500000000000000, 2.828427124746190735 ) ) ;
#37680=CARTESIAN_POINT ( 'NONE',  ( 2.780723358947928197E-16, 16.56249999863440436, -4.541265875000002339 ) ) ;
#37689=ORIENTED_EDGE ( 'NONE', *, *, #29992, .T. ) ;
#37702=CARTESIAN_POINT ( 'NONE',  ( 4.000000000000001776, 14.06250000000000178, -1.656854249492381248 ) ) ;
#37734=CARTESIAN_POINT ( 'NONE',  ( 4.000000000000001776, 10.74999999726881406, 0.000000000000000000 ) ) ;
#37764=CARTESIAN_POINT ( 'NONE',  ( -4.541265875000003227, 5.999999998634407028, 1.881053915767121110 ) ) ;
#37772=CARTESIAN_POINT ( 'NONE',  ( -1.656854249492381248, 2.312500000000000888, -4.000000000000001776 ) ) ;
#37773=CARTESIAN_POINT ( 'NONE',  ( -4.000000000000001776, 18.24999999726881583, -4.898587196589415787E-16 ) ) ;
#37774=CARTESIAN_POINT ( 'NONE',  ( -4.541265875000003227, 3.874999998634407028, 1.881053915767121110 ) ) ;
#37780=CARTESIAN_POINT ( 'NONE',  ( -1.881053915767124440, 19.99999999863440436, 4.541265875000001451 ) ) ;
#37783=ORIENTED_EDGE ( 'NONE', *, *, #11610, .T. ) ;
#37790=CARTESIAN_POINT ( 'NONE',  ( -2.828427124746190735, 21.12499999726881583, -2.828427124746191623 ) ) ;
#37808=CARTESIAN_POINT ( 'NONE',  ( -3.211159895383562723, 6.937499998634407028, 3.211159895383561391 ) ) ;
#37810=CARTESIAN_POINT ( 'NONE',  ( -1.656854249492383468, 14.43749999726881406, 4.000000000000000888 ) ) ;
#37827=CARTESIAN_POINT ( 'NONE',  ( -4.541265875000003227, 20.99999999863440792, 1.881053915767121110 ) ) ;
#37852=CARTESIAN_POINT ( 'NONE',  ( -4.541265875000002339, 10.87499999863440969, -1.881053915767121998 ) ) ;
#37863=CARTESIAN_POINT ( 'NONE',  ( -2.828427124746192067, 7.374999997268813168, 2.828427124746190735 ) ) ;
#37868=CARTESIAN_POINT ( 'NONE',  ( -4.541265875000002339, 7.749999998634407916, -1.881053915767121998 ) ) ;
#37872=CARTESIAN_POINT ( 'NONE',  ( 4.270632937500002058, 0.1562499993172034307, 0.000000000000000000 ) ) ;
#37911=CARTESIAN_POINT ( 'NONE',  ( 3.211159895383560947, 10.31249999863440792, 3.211159895383562723 ) ) ;
#37936=( BOUNDED_CURVE ( )  B_SPLINE_CURVE ( 2, ( #49320, #33129, #14984, #20651, #73828, #39134, #21397, #3312, #72337 ),
 .UNSPECIFIED., .F., .F. ) 
 B_SPLINE_CURVE_WITH_KNOTS ( ( 3, 2, 2, 2, 3 ),
 ( 0.6704545454545455252, 0.6761363636363637575, 0.6818181818181817677, 0.6875000000000000000, 0.6931818181818182323 ),
 .UNSPECIFIED. ) 
 CURVE ( )  GEOMETRIC_REPRESENTATION_ITEM ( )  RATIONAL_B_SPLINE_CURVE ( ( 0.9999999999999985567, 0.9238795325112881818, 1.000000000000000000, 0.9238795325112867385, 1.000000000000000000, 0.9238795325112867385, 1.000000000000000000, 0.9238795325112867385, 1.000000000000000000 ) ) 
 REPRESENTATION_ITEM ( '' )  );
#37944=EDGE_CURVE ( 'NONE', #55561, #35916, #14003, .T. ) ;
#37957=CARTESIAN_POINT ( 'NONE',  ( -1.881053915767124440, 17.12499999863440436, 4.541265875000001451 ) ) ;
#37960=AXIS2_PLACEMENT_3D ( 'NONE', #31510, #13030, #59811 ) ;
#37965=ORIENTED_EDGE ( 'NONE', *, *, #73800, .T. ) ;
#38000=CARTESIAN_POINT ( 'NONE',  ( 1.881053915767122664, 20.12499999863441147, 4.541265875000001451 ) ) ;
#38031=CARTESIAN_POINT ( 'NONE',  ( 4.000000000000000888, 3.687499997268813168, 1.656854249492384135 ) ) ;
#38050=CARTESIAN_POINT ( 'NONE',  ( 1.656854249492381248, 17.18750000000000000, -4.000000000000001776 ) ) ;
#38051=CARTESIAN_POINT ( 'NONE',  ( 2.780723358947928197E-16, 20.56249999863440436, -4.541265875000002339 ) ) ;
#38068=ORIENTED_EDGE ( 'NONE', *, *, #63245, .F. ) ;
#38080=VECTOR ( 'NONE', #36069, 1000.000000000000000 ) ;
#38130=CARTESIAN_POINT ( 'NONE',  ( -8.342170076843785083E-16, 20.18749999863440436, 4.541265875000002339 ) ) ;
#38133=CARTESIAN_POINT ( 'NONE',  ( 3.211159895383561835, 3.562499998634407028, -3.211159895383561835 ) ) ;
#38141=CARTESIAN_POINT ( 'NONE',  ( -4.000000000000001776, 5.437500000000001776, -1.656854249492381470 ) ) ;
#38142=CARTESIAN_POINT ( 'NONE',  ( -1.656854249492383691, 16.43749999726881228, 4.000000000000000888 ) ) ;
#38143=CARTESIAN_POINT ( 'NONE',  ( -4.541265875000002339, 8.749999998634407916, -1.881053915767121998 ) ) ;
#38148=CARTESIAN_POINT ( 'NONE',  ( 2.780723358947928197E-16, 18.56249999863440436, -4.541265875000002339 ) ) ;
#38166=ORIENTED_EDGE ( 'NONE', *, *, #68863, .T. ) ;
#38181=CARTESIAN_POINT ( 'NONE',  ( 3.211159895383560947, 7.187499998634407028, 3.211159895383562723 ) ) ;
#38189=CARTESIAN_POINT ( 'NONE',  ( 2.828427124746190291, 19.62499999726881228, 2.828427124746192067 ) ) ;
#38199=CARTESIAN_POINT ( 'NONE',  ( -1.881053915767124440, 19.12499999863441147, 4.541265875000001451 ) ) ;
#38221=CARTESIAN_POINT ( 'NONE',  ( 3.211159895383560947, 7.312499998634407028, 3.211159895383562723 ) ) ;
#38232=CARTESIAN_POINT ( 'NONE',  ( -4.000000000000001776, 7.249999997268813168, -4.898587196589415787E-16 ) ) ;
#38238=CARTESIAN_POINT ( 'NONE',  ( -4.541265875000003227, 5.874999998634406140, 1.881053915767121110 ) ) ;
#38282=CARTESIAN_POINT ( 'NONE',  ( 3.211159895383561835, 7.562499998634407028, -3.211159895383561835 ) ) ;
#38286=CARTESIAN_POINT ( 'NONE',  ( 2.449293598294707893E-16, 3.999999997268813168, -4.000000000000001776 ) ) ;
#38305=( BOUNDED_CURVE ( )  B_SPLINE_CURVE ( 2, ( #294, #6314, #52327, #19454, #13776, #2115, #71131, #60191, #3232 ),
 .UNSPECIFIED., .F., .F. ) 
 B_SPLINE_CURVE_WITH_KNOTS ( ( 3, 2, 2, 2, 3 ),
 ( 0.8977272727272727071, 0.9034090909090909394, 0.9090909090909091717, 0.9147727272727274039, 0.9204545454545455252 ),
 .UNSPECIFIED. ) 
 CURVE ( )  GEOMETRIC_REPRESENTATION_ITEM ( )  RATIONAL_B_SPLINE_CURVE ( ( 1.000000000000000000, 0.9238795325112867385, 1.000000000000000000, 0.9238795325112867385, 1.000000000000000000, 0.9238795325112867385, 1.000000000000000000, 0.9238795325112852952, 1.000000000000001554 ) ) 
 REPRESENTATION_ITEM ( '' )  );
#38326=CARTESIAN_POINT ( 'NONE',  ( 4.541265875000002339, 17.43749999863440792, 0.000000000000000000 ) ) ;
#38370=CARTESIAN_POINT ( 'NONE',  ( -4.541265875000003227, 16.87499999863440436, 1.881053915767121110 ) ) ;
#38391=EDGE_CURVE ( 'NONE', #40603, #58773, #1851, .T. ) ;
#38403=VERTEX_POINT ( 'NONE', #24837 ) ;
#38405=CARTESIAN_POINT ( 'NONE',  ( 4.000000000000001776, 3.749999997268813168, 0.000000000000000000 ) ) ;
#38411=CARTESIAN_POINT ( 'NONE',  ( -4.000000000000002665, 20.56249999999999645, 1.656854249492380582 ) ) ;
#38423=CARTESIAN_POINT ( 'NONE',  ( -2.828427124746192067, 21.62500000000000355, 2.828427124746190735 ) ) ;
#38424=CARTESIAN_POINT ( 'NONE',  ( -4.541265875000002339, 19.74999999863440081, -1.881053915767121998 ) ) ;
#38507=CARTESIAN_POINT ( 'NONE',  ( 2.780723358947928197E-16, 19.68749999863440436, -4.541265875000002339 ) ) ;
#38510=CARTESIAN_POINT ( 'NONE',  ( 1.881053915767122664, 3.249999998634406584, 4.541265875000001451 ) ) ;
#38516=CARTESIAN_POINT ( 'NONE',  ( -1.656854249492381248, 5.312500000000001776, -4.000000000000001776 ) ) ;
#38517=CARTESIAN_POINT ( 'NONE',  ( -4.000000000000002665, 19.31249999726881583, 1.656854249492380804 ) ) ;
#38518=CARTESIAN_POINT ( 'NONE',  ( 3.211159895383560947, 8.187499998634406140, 3.211159895383562723 ) ) ;
#38522=PRODUCT_DEFINITION_CONTEXT ( 'detailed design', #31820, 'design' ) ;
#38526=CARTESIAN_POINT ( 'NONE',  ( 3.211159895383561835, 19.43749999863440436, -3.211159895383561835 ) ) ;
#38560=CARTESIAN_POINT ( 'NONE',  ( -8.342170076843785083E-16, 6.062499998634407028, 4.541265875000002339 ) ) ;
#38579=CARTESIAN_POINT ( 'NONE',  ( 3.211159895383561835, 19.56249999863440436, -3.211159895383561835 ) ) ;
#38599=CARTESIAN_POINT ( 'NONE',  ( 4.541265875000002339, 9.499999998634404363, -1.881053915767121776 ) ) ;
#38602=FACE_OUTER_BOUND ( 'NONE', #22182, .T. ) ;
#38609=CARTESIAN_POINT ( 'NONE',  ( -2.828427124746192067, 6.374999997268813168, 2.828427124746190735 ) ) ;
#38618=CARTESIAN_POINT ( 'NONE',  ( 2.780723358947928197E-16, 5.562499998634407028, -4.541265875000002339 ) ) ;
#38626=CARTESIAN_POINT ( 'NONE',  ( -4.000000000000002665, 18.56250000000000000, 1.656854249492380582 ) ) ;
#38661=CARTESIAN_POINT ( 'NONE',  ( -3.211159895383561391, 8.812499998634407916, -3.211159895383561835 ) ) ;
#38705=CARTESIAN_POINT ( 'NONE',  ( 3.211159895383560947, 15.31249999863440792, 3.211159895383562723 ) ) ;
#38727=( BOUNDED_CURVE ( )  B_SPLINE_CURVE ( 2, ( #42321, #47247, #48350, #70274, #18586, #7268, #54031, #53661, #36311 ),
 .UNSPECIFIED., .F., .F. ) 
 B_SPLINE_CURVE_WITH_KNOTS ( ( 3, 2, 2, 2, 3 ),
 ( 0.3522727272727272929, 0.3579545454545454697, 0.3636363636363636465, 0.3693181818181818232, 0.3750000000000000000 ),
 .UNSPECIFIED. ) 
 CURVE ( )  GEOMETRIC_REPRESENTATION_ITEM ( )  RATIONAL_B_SPLINE_CURVE ( ( 1.000000000000000000, 0.9238795325112867385, 1.000000000000000000, 0.9238795325112867385, 1.000000000000000000, 0.9238795325112867385, 1.000000000000000000, 0.9238795325112867385, 1.000000000000000000 ) ) 
 REPRESENTATION_ITEM ( '' )  );
#38751=CARTESIAN_POINT ( 'NONE',  ( -8.342170076843785083E-16, 18.06249999863440792, 4.541265875000002339 ) ) ;
#38754=CARTESIAN_POINT ( 'NONE',  ( 4.541265875000002339, 0.3749999986344067504, 0.000000000000000000 ) ) ;
#38762=AXIS2_PLACEMENT_3D ( 'NONE', #23619, #22872, #52668 ) ;
#38798=CARTESIAN_POINT ( 'NONE',  ( 1.656854249492381914, 19.81250000000000000, 4.000000000000000888 ) ) ;
#38799=CARTESIAN_POINT ( 'NONE',  ( 4.541265875000002339, 21.31249999863440792, 0.000000000000000000 ) ) ;
#38841=ORIENTED_EDGE ( 'NONE', *, *, #29591, .F. ) ;
#38877=CARTESIAN_POINT ( 'NONE',  ( -4.541265875000002339, 6.874999998634407916, -1.881053915767121998 ) ) ;
#38884=CARTESIAN_POINT ( 'NONE',  ( -4.000000000000001776, 9.437500000000000000, -1.656854249492381470 ) ) ;
#38886=CARTESIAN_POINT ( 'NONE',  ( 1.881053915767121998, 9.499999998634404363, -4.541265875000002339 ) ) ;
#38893=CARTESIAN_POINT ( 'NONE',  ( -2.828427124746190735, 10.37500000000000000, -2.828427124746191623 ) ) ;
#38937=DIRECTION ( 'NONE',  ( 0.000000000000000000, 0.000000000000000000, -1.000000000000000000 ) ) ;
#38942=CARTESIAN_POINT ( 'NONE',  ( -1.881053915767124440, 21.12499999863441147, 4.541265875000001451 ) ) ;
#38962=CARTESIAN_POINT ( 'NONE',  ( 4.541265875000002339, 10.43749999863440792, 0.000000000000000000 ) ) ;
#38972=CARTESIAN_POINT ( 'NONE',  ( -4.000000000000002665, 4.312499997268814056, 1.656854249492380804 ) ) ;
#38979=CARTESIAN_POINT ( 'NONE',  ( 2.780723358947928197E-16, 6.562499998634407028, -4.541265875000002339 ) ) ;
#39025=CARTESIAN_POINT ( 'NONE',  ( -4.541265875000003227, 9.999999998634407916, 1.881053915767121110 ) ) ;
#39031=CARTESIAN_POINT ( 'NONE',  ( 2.449293598294707893E-16, 5.250000000000000000, -4.000000000000001776 ) ) ;
#39056=CARTESIAN_POINT ( 'NONE',  ( -7.347880794884122694E-16, 4.750000000000000000, 4.000000000000001776 ) ) ;
#39068=FACE_OUTER_BOUND ( 'NONE', #60149, .T. ) ;
#39069=CARTESIAN_POINT ( 'NONE',  ( -3.211159895383562723, 16.06249999863440436, 3.211159895383561391 ) ) ;
#39076=EDGE_LOOP ( 'NONE', ( #46979, #45355, #64280, #51611 ) ) ;
#39111=CARTESIAN_POINT ( 'NONE',  ( -4.541265875000002339, 16.81249999863440436, -5.561446717895856393E-16 ) ) ;
#39134=CARTESIAN_POINT ( 'NONE',  ( 4.000000000000001776, 15.06249999999999822, -1.656854249492381248 ) ) ;
#39163=CARTESIAN_POINT ( 'NONE',  ( 1.656854249492381248, 18.18750000000000000, -4.000000000000001776 ) ) ;
#39164=CARTESIAN_POINT ( 'NONE',  ( -1.881053915767121776, 21.62499999863441147, -4.541265875000002339 ) ) ;
#39246=VERTEX_POINT ( 'NONE', #6786 ) ;
#39247=CARTESIAN_POINT ( 'NONE',  ( 4.541265875000002339, 7.499999998634408804, -1.881053915767121554 ) ) ;
#39255=CARTESIAN_POINT ( 'NONE',  ( 1.656854249492381914, 9.812500000000000000, 4.000000000000000888 ) ) ;
#39256=CARTESIAN_POINT ( 'NONE',  ( 2.449293598294707893E-16, 21.99999999726881583, -4.000000000000001776 ) ) ;
#39257=CARTESIAN_POINT ( 'NONE',  ( 3.211159895383560947, 9.187499998634407916, 3.211159895383562723 ) ) ;
#39264=CARTESIAN_POINT ( 'NONE',  ( 1.881053915767121776, 21.49999999863440792, -4.541265875000002339 ) ) ;
#39302=EDGE_CURVE ( 'NONE', #49926, #13507, #72867, .T. ) ;
#39308=CARTESIAN_POINT ( 'NONE',  ( 0.000000000000000000, 0.000000000000000000, 0.000000000000000000 ) ) ;
#39313=ADVANCED_FACE ( 'NONE', ( #47133 ), #29796, .T. ) ;
#39315=AXIS2_PLACEMENT_3D ( 'NONE', #29915, #5422, #51434 ) ;
#39325=EDGE_CURVE ( 'NONE', #33915, #55673, #41455, .T. ) ;
#39328=VECTOR ( 'NONE', #66581, 1000.000000000000000 ) ;
#39335=CARTESIAN_POINT ( 'NONE',  ( -4.541265875000002339, 11.93749999863440614, -5.561446717895856393E-16 ) ) ;
#39343=CARTESIAN_POINT ( 'NONE',  ( -4.000000000000001776, 9.187499997268814056, -1.656854249492381470 ) ) ;
#39350=CARTESIAN_POINT ( 'NONE',  ( 4.541265875000002339, 11.37499999863440969, -1.881053915767121554 ) ) ;
#39351=CARTESIAN_POINT ( 'NONE',  ( -1.656854249492383468, 10.43749999726881228, 4.000000000000000888 ) ) ;
#39355=ORIENTED_EDGE ( 'NONE', *, *, #23534, .T. ) ;
#39380=CARTESIAN_POINT ( 'NONE',  ( 0.000000000000000000, 0.000000000000000000, 0.000000000000000000 ) ) ;
#39393=CARTESIAN_POINT ( 'NONE',  ( -4.541265875000003227, 13.99999999863440792, 1.881053915767121110 ) ) ;
#39436=CARTESIAN_POINT ( 'NONE',  ( -4.541265875000003227, 18.99999999863440436, 1.881053915767121110 ) ) ;
#39483=CARTESIAN_POINT ( 'NONE',  ( -4.541265875000002339, 19.74999999863440792, -1.881053915767121998 ) ) ;
#39489=ORIENTED_EDGE ( 'NONE', *, *, #33400, .T. ) ;
#39540=CARTESIAN_POINT ( 'NONE',  ( 1.656854249492381248, 20.18749999999999645, -4.000000000000001776 ) ) ;
#39541=CARTESIAN_POINT ( 'NONE',  ( 4.541265875000001451, 21.24999999863440792, 1.881053915767124440 ) ) ;
#39543=CARTESIAN_POINT ( 'NONE',  ( 2.828427124746191623, 4.874999997268813168, -2.828427124746191623 ) ) ;
#39575=CARTESIAN_POINT ( 'NONE',  ( 4.000000000000001776, 10.06250000000000000, -1.656854249492381248 ) ) ;
#39619=CARTESIAN_POINT ( 'NONE',  ( 2.780723358947928197E-16, 8.687499998634407916, -4.541265875000002339 ) ) ;
#39626=CARTESIAN_POINT ( 'NONE',  ( -4.000000000000002665, 8.562500000000001776, 1.656854249492380804 ) ) ;
#39628=CARTESIAN_POINT ( 'NONE',  ( 4.541265875000002339, 7.312499998634407028, 0.000000000000000000 ) ) ;
#39638=ORIENTED_EDGE ( 'NONE', *, *, #47764, .T. ) ;
#39700=CARTESIAN_POINT ( 'NONE',  ( -1.881053915767124440, 12.12499999863440792, 4.541265875000001451 ) ) ;
#39710=CARTESIAN_POINT ( 'NONE',  ( 4.000000000000000888, 8.687499997268814056, 1.656854249492384135 ) ) ;
#39717=CARTESIAN_POINT ( 'NONE',  ( -3.211159895383561391, 8.687499998634407916, -3.211159895383561835 ) ) ;
#39725=CARTESIAN_POINT ( 'NONE',  ( -4.000000000000001776, 18.43750000000000000, -1.656854249492381470 ) ) ;
#39743=FACE_OUTER_BOUND ( 'NONE', #71249, .T. ) ;
#39757=CARTESIAN_POINT ( 'NONE',  ( -4.541265875000002339, 12.93749999863440792, -5.561446717895856393E-16 ) ) ;
#39772=DIRECTION ( 'NONE',  ( 0.000000000000000000, 0.000000000000000000, -1.000000000000000000 ) ) ;
#39775=EDGE_LOOP ( 'NONE', ( #52411, #57810, #41259, #57048 ) ) ;
#39799=CARTESIAN_POINT ( 'NONE',  ( -1.881053915767121554, 20.74999999863440436, -4.541265875000002339 ) ) ;
#39800=ORIENTED_EDGE ( 'NONE', *, *, #12218, .T. ) ;
#39822=VECTOR ( 'NONE', #47971, 1000.000000000000000 ) ;
#39839=ORIENTED_EDGE ( 'NONE', *, *, #1502, .T. ) ;
#39849=CARTESIAN_POINT ( 'NONE',  ( 4.541265875000002339, 0.4999999986344068614, -1.881053915767121554 ) ) ;
#39868=DIRECTION ( 'NONE',  ( -0.000000000000000000, -1.000000000000000000, -0.000000000000000000 ) ) ;
#39875=CARTESIAN_POINT ( 'NONE',  ( 4.000000000000001776, 6.062500000000000000, -1.656854249492381248 ) ) ;
#39876=CARTESIAN_POINT ( 'NONE',  ( 4.000000000000001776, 9.749999997268814056, 0.000000000000000000 ) ) ;
#39883=CARTESIAN_POINT ( 'NONE',  ( -2.828427124746190735, 1.124999997268813390, -2.828427124746191623 ) ) ;
#39905=CARTESIAN_POINT ( 'NONE',  ( -1.656854249492383691, 19.68749999999999645, 4.000000000000000888 ) ) ;
#39936=ORIENTED_EDGE ( 'NONE', *, *, #45586, .T. ) ;
#39943=CARTESIAN_POINT ( 'NONE',  ( 2.828427124746191623, 10.12500000000000000, -2.828427124746191623 ) ) ;
#39944=CARTESIAN_POINT ( 'NONE',  ( -8.342170076843785083E-16, 12.06249999863440614, 4.541265875000002339 ) ) ;
#39990=ORIENTED_EDGE ( 'NONE', *, *, #59665, .F. ) ;
#39992=CARTESIAN_POINT ( 'NONE',  ( -4.541265875000003227, 7.999999998634407028, 1.881053915767121110 ) ) ;
#39998=CARTESIAN_POINT ( 'NONE',  ( 2.828427124746191623, 7.125000000000000000, -2.828427124746191623 ) ) ;
#39999=CARTESIAN_POINT ( 'NONE',  ( 2.828427124746190291, 22.62499999726881583, 2.828427124746192067 ) ) ;
#40000=CARTESIAN_POINT ( 'NONE',  ( 1.881053915767121998, 10.49999999863440969, -4.541265875000002339 ) ) ;
#40006=CARTESIAN_POINT ( 'NONE',  ( 2.780723358947928197E-16, 20.56249999863440436, -4.541265875000002339 ) ) ;
#40023=( BOUNDED_CURVE ( )  B_SPLINE_CURVE ( 2, ( #1014, #58356, #40240, #69287, #17596, #6661, #40614, #29664, #37551 ),
 .UNSPECIFIED., .F., .F. ) 
 B_SPLINE_CURVE_WITH_KNOTS ( ( 3, 2, 2, 2, 3 ),
 ( 0.2386363636363636465, 0.2443181818181818232, 0.2500000000000000000, 0.2556818181818181768, 0.2613636363636363535 ),
 .UNSPECIFIED. ) 
 CURVE ( )  GEOMETRIC_REPRESENTATION_ITEM ( )  RATIONAL_B_SPLINE_CURVE ( ( 1.000000000000000000, 0.9238795325112867385, 1.000000000000000000, 0.9238795325112867385, 1.000000000000000000, 0.9238795325112867385, 1.000000000000000000, 0.9238795325112867385, 1.000000000000000000 ) ) 
 REPRESENTATION_ITEM ( '' )  );
#40039=CARTESIAN_POINT ( 'NONE',  ( 4.000000000000001776, 11.81249999726881228, -1.656854249492381248 ) ) ;
#40076=CARTESIAN_POINT ( 'NONE',  ( -4.541265875000002339, 11.87499999863440792, -1.881053915767121998 ) ) ;
#40086=CARTESIAN_POINT ( 'NONE',  ( 4.000000000000000888, 11.68749999726881406, 1.656854249492384135 ) ) ;
#40089=DIRECTION ( 'NONE',  ( -0.000000000000000000, -1.000000000000000000, -0.000000000000000000 ) ) ;
#40093=CARTESIAN_POINT ( 'NONE',  ( -4.541265875000002339, 10.81249999863440792, -5.561446717895856393E-16 ) ) ;
#40136=CARTESIAN_POINT ( 'NONE',  ( 3.211159895383561835, 10.56249999863440792, -3.211159895383561835 ) ) ;
#40167=CARTESIAN_POINT ( 'NONE',  ( 4.541265875000002339, 1.499999998634407028, -1.881053915767121776 ) ) ;
#40179=CARTESIAN_POINT ( 'NONE',  ( -3.211159895383561391, 21.81249999863440792, -3.211159895383561835 ) ) ;
#40184=PLANE ( 'NONE',  #19942 ) ;
#40222=CARTESIAN_POINT ( 'NONE',  ( 1.881053915767122664, 2.249999998634407028, 4.541265875000001451 ) ) ;
#40229=CARTESIAN_POINT ( 'NONE',  ( 4.000000000000001776, 15.81249999726881406, -1.656854249492381248 ) ) ;
#40240=CARTESIAN_POINT ( 'NONE',  ( -2.828427124746190735, 6.124999997268813168, -2.828427124746191623 ) ) ;
#40279=CARTESIAN_POINT ( 'NONE',  ( 4.541265875000001451, 2.249999998634407028, 1.881053915767124440 ) ) ;
#40293=VERTEX_POINT ( 'NONE', #8100 ) ;
#40314=CARTESIAN_POINT ( 'NONE',  ( -8.342170076843785083E-16, 10.06249999863440614, 4.541265875000002339 ) ) ;
#40326=CARTESIAN_POINT ( 'NONE',  ( 2.828427124746190291, 8.624999997268814056, 2.828427124746192067 ) ) ;
#40359=CARTESIAN_POINT ( 'NONE',  ( 4.541265875000002339, 6.437499998634407028, 0.000000000000000000 ) ) ;
#40364=CARTESIAN_POINT ( 'NONE',  ( 4.000000000000001776, 9.000000000000001776, 0.000000000000000000 ) ) ;
#40367=CARTESIAN_POINT ( 'NONE',  ( -3.211159895383561391, 10.68749999863440792, -3.211159895383561835 ) ) ;
#40408=ADVANCED_FACE ( 'NONE', ( #4315 ), #23136, .F. ) ;
#40444=CARTESIAN_POINT ( 'NONE',  ( 2.449293598294707893E-16, 8.250000000000000000, -4.000000000000001776 ) ) ;
#40446=ORIENTED_EDGE ( 'NONE', *, *, #2931, .F. ) ;
#40448=CARTESIAN_POINT ( 'NONE',  ( -1.881053915767124440, 14.12499999863440792, 4.541265875000001451 ) ) ;
#40450=ORIENTED_EDGE ( 'NONE', *, *, #13168, .T. ) ;
#40458=CARTESIAN_POINT ( 'NONE',  ( 2.828427124746190291, 10.62499999726881406, 2.828427124746192067 ) ) ;
#40465=CARTESIAN_POINT ( 'NONE',  ( -4.541265875000002339, 11.74999999863440792, -1.881053915767121998 ) ) ;
#40510=CARTESIAN_POINT ( 'NONE',  ( -1.881053915767124440, 13.12499999863440969, 4.541265875000001451 ) ) ;
#40535=CARTESIAN_POINT ( 'NONE',  ( -3.211159895383562723, 1.062499998634406806, 3.211159895383561391 ) ) ;
#40548=CARTESIAN_POINT ( 'NONE',  ( 3.211159895383560947, 21.31249999863440792, 3.211159895383562723 ) ) ;
#40558=CARTESIAN_POINT ( 'NONE',  ( -8.000000000000003553, 22.99999999999999645, 1.000000000000000000 ) ) ;
#40588=CARTESIAN_POINT ( 'NONE',  ( 2.449293598294707893E-16, 6.250000000000000000, -4.000000000000001776 ) ) ;
#40597=CARTESIAN_POINT ( 'NONE',  ( -1.881053915767121554, 21.62499999863441502, -4.541265875000002339 ) ) ;
#40600=( NAMED_UNIT ( * ) SI_UNIT ( $, .STERADIAN. ) SOLID_ANGLE_UNIT ( ) );
#40603=VERTEX_POINT ( 'NONE', #7278 ) ;
#40614=CARTESIAN_POINT ( 'NONE',  ( -2.828427124746192067, 6.374999997268813168, 2.828427124746190735 ) ) ;
#40619=CARTESIAN_POINT ( 'NONE',  ( -7.347880794884122694E-16, 13.75000000000000000, 4.000000000000001776 ) ) ;
#40669=CARTESIAN_POINT ( 'NONE',  ( -7.347880794884122694E-16, 20.75000000000000000, 4.000000000000001776 ) ) ;
#40687=CARTESIAN_POINT ( 'NONE',  ( 3.211159895383561835, 8.437499998634407916, -3.211159895383561835 ) ) ;
#40718=CARTESIAN_POINT ( 'NONE',  ( 1.656854249492381248, 21.93749999726881583, -4.000000000000001776 ) ) ;
#40720=DIRECTION ( 'NONE',  ( 0.000000000000000000, 0.000000000000000000, -1.000000000000000000 ) ) ;
#40725=DIRECTION ( 'NONE',  ( -0.000000000000000000, -1.000000000000000000, -0.000000000000000000 ) ) ;
#40728=CARTESIAN_POINT ( 'NONE',  ( -4.541265875000002339, 11.93749999863440614, -5.561446717895856393E-16 ) ) ;
#40730=CARTESIAN_POINT ( 'NONE',  ( 4.000000000000000888, 11.93750000000000000, 1.656854249492384135 ) ) ;
#40732=CARTESIAN_POINT ( 'NONE',  ( 3.211159895383561835, 12.43749999863440792, -3.211159895383561835 ) ) ;
#40735=ORIENTED_EDGE ( 'NONE', *, *, #35755, .T. ) ;
#40756=AXIS2_PLACEMENT_3D ( 'NONE', #43475, #56217, #27526 ) ;
#40779=EDGE_CURVE ( 'NONE', #55673, #8511, #44000, .T. ) ;
#40817=CARTESIAN_POINT ( 'NONE',  ( 3.211159895383560947, 14.31249999863440792, 3.211159895383562723 ) ) ;
#40821=CARTESIAN_POINT ( 'NONE',  ( -3.211159895383562723, 1.062499998634406806, 3.211159895383561391 ) ) ;
#40828=CARTESIAN_POINT ( 'NONE',  ( -2.828427124746190735, 0.3750000000000001665, -2.828427124746191623 ) ) ;
#40829=CARTESIAN_POINT ( 'NONE',  ( -4.000000000000001776, 12.24999999726881406, -4.898587196589415787E-16 ) ) ;
#40836=CARTESIAN_POINT ( 'NONE',  ( 1.881053915767122664, 11.12499999863440792, 4.541265875000001451 ) ) ;
#40837=CARTESIAN_POINT ( 'NONE',  ( -1.656854249492358155, 18.43749999726881228, 4.000000000000024869 ) ) ;
#40871=AXIS2_PLACEMENT_3D ( 'NONE', #64104, #58459, #52785 ) ;
#40882=CARTESIAN_POINT ( 'NONE',  ( -4.541265875000003227, 11.99999999863440969, 1.881053915767121110 ) ) ;
#40885=CARTESIAN_POINT ( 'NONE',  ( -1.656854249492377029, 4.437499997268814056, 4.000000000000007994 ) ) ;
#40922=EDGE_CURVE ( 'NONE', #4559, #40293, #16258, .T. ) ;
#40925=CARTESIAN_POINT ( 'NONE',  ( 4.541265875000001451, 21.37499999863441147, 1.881053915767124440 ) ) ;
#40946=ORIENTED_EDGE ( 'NONE', *, *, #17146, .T. ) ;
#40959=DIRECTION ( 'NONE',  ( 0.000000000000000000, 0.000000000000000000, -1.000000000000000000 ) ) ;
#40970=VECTOR ( 'NONE', #28770, 1000.000000000000000 ) ;
#40973=CARTESIAN_POINT ( 'NONE',  ( 1.881053915767122664, 21.12499999863441147, 4.541265875000001451 ) ) ;
#40979=ORIENTED_EDGE ( 'NONE', *, *, #8568, .T. ) ;
#41063=CARTESIAN_POINT ( 'NONE',  ( -4.541265875000002339, 11.81249999863440614, -5.561446717895856393E-16 ) ) ;
#41108=CARTESIAN_POINT ( 'NONE',  ( 4.000000000000001776, 12.00000000000000000, 0.000000000000000000 ) ) ;
#41110=CARTESIAN_POINT ( 'NONE',  ( 3.211159895383560947, 10.18749999863440614, 3.211159895383562723 ) ) ;
#41172=( BOUNDED_CURVE ( )  B_SPLINE_CURVE ( 2, ( #4444, #33139, #51201, #33877, #28563, #33502, #44428, #67443, #56504 ),
 .UNSPECIFIED., .F., .F. ) 
 B_SPLINE_CURVE_WITH_KNOTS ( ( 3, 2, 2, 2, 3 ),
 ( 0.1022727272727272790, 0.1079545454545454558, 0.1136363636363636326, 0.1193181818181818232, 0.1250000000000000000 ),
 .UNSPECIFIED. ) 
 CURVE ( )  GEOMETRIC_REPRESENTATION_ITEM ( )  RATIONAL_B_SPLINE_CURVE ( ( 1.000000000000000000, 0.9238795325112867385, 1.000000000000000000, 0.9238795325112867385, 1.000000000000000000, 0.9238795325112867385, 1.000000000000000000, 0.9238795325112867385, 1.000000000000000000 ) ) 
 REPRESENTATION_ITEM ( '' )  );
#41178=CARTESIAN_POINT ( 'NONE',  ( 4.000000000000001776, 14.81249999726881406, -1.656854249492381248 ) ) ;
#41192=CARTESIAN_POINT ( 'NONE',  ( 1.881053915767121998, 16.62499999863440436, -4.541265875000002339 ) ) ;
#41196=CARTESIAN_POINT ( 'NONE',  ( -1.881053915767121554, 0.7499999986344069169, -4.541265875000002339 ) ) ;
#41202=CARTESIAN_POINT ( 'NONE',  ( 4.000000000000001776, 2.000000000000000000, 0.000000000000000000 ) ) ;
#41203=CARTESIAN_POINT ( 'NONE',  ( 2.828427124746191623, 14.87499999726881406, -2.828427124746191623 ) ) ;
#41206=CARTESIAN_POINT ( 'NONE',  ( 4.898587196589415787E-16, 0.000000000000000000, 4.000000000000001776 ) ) ;
#41209=CARTESIAN_POINT ( 'NONE',  ( 4.541265875000002339, 16.31249999863440436, 0.000000000000000000 ) ) ;
#41213=ORIENTED_EDGE ( 'NONE', *, *, #45849, .T. ) ;
#41235=( BOUNDED_CURVE ( )  B_SPLINE_CURVE ( 2, ( #55021, #32002, #67820, #3329, #4085, #38411, #21041, #43685, #14999 ),
 .UNSPECIFIED., .F., .F. ) 
 B_SPLINE_CURVE_WITH_KNOTS ( ( 3, 2, 2, 2, 3 ),
 ( 0.9204545454545455252, 0.9261363636363637575, 0.9318181818181817677, 0.9375000000000000000, 0.9431818181818182323 ),
 .UNSPECIFIED. ) 
 CURVE ( )  GEOMETRIC_REPRESENTATION_ITEM ( )  RATIONAL_B_SPLINE_CURVE ( ( 0.9999999999999985567, 0.9238795325112881818, 1.000000000000000000, 0.9238795325112867385, 1.000000000000000000, 0.9238795325112867385, 1.000000000000000000, 0.9238795325112867385, 1.000000000000000000 ) ) 
 REPRESENTATION_ITEM ( '' )  );
#41239=CARTESIAN_POINT ( 'NONE',  ( 4.541265875000002339, 2.312499998634407028, 0.000000000000000000 ) ) ;
#41254=CARTESIAN_POINT ( 'NONE',  ( -4.541265875000003227, 17.99999999863440436, 1.881053915767121110 ) ) ;
#41258=ORIENTED_EDGE ( 'NONE', *, *, #46382, .F. ) ;
#41259=ORIENTED_EDGE ( 'NONE', *, *, #53007, .F. ) ;
#41279=ORIENTED_EDGE ( 'NONE', *, *, #44541, .T. ) ;
#41281=CARTESIAN_POINT ( 'NONE',  ( 3.211159895383561835, 5.562499998634407028, -3.211159895383561835 ) ) ;
#41295=CARTESIAN_POINT ( 'NONE',  ( 3.211159895383560947, 22.31249999863440792, 3.211159895383562723 ) ) ;
#41341=CARTESIAN_POINT ( 'NONE',  ( 1.881053915767121776, 21.49999999863440792, -4.541265875000002339 ) ) ;
#41356=CARTESIAN_POINT ( 'NONE',  ( 0.000000000000000000, 0.000000000000000000, -4.000000000000001776 ) ) ;
#41367=CARTESIAN_POINT ( 'NONE',  ( -7.347880794884122694E-16, 21.75000000000000355, 4.000000000000001776 ) ) ;
#41377=CARTESIAN_POINT ( 'NONE',  ( -7.347880794884122694E-16, 5.750000000000000000, 4.000000000000001776 ) ) ;
#41380=CARTESIAN_POINT ( 'NONE',  ( 4.023044438063403838, 21.99999999999999645, 0.3527035116121371994 ) ) ;
#41421=ORIENTED_EDGE ( 'NONE', *, *, #65945, .T. ) ;
#41433=CARTESIAN_POINT ( 'NONE',  ( 1.881053915767121776, 9.499999998634406140, -4.541265875000002339 ) ) ;
#41446=CARTESIAN_POINT ( 'NONE',  ( 2.828427124746191623, 8.874999997268814056, -2.828427124746191623 ) ) ;
#41455=( BOUNDED_CURVE ( )  B_SPLINE_CURVE ( 2, ( #13894, #53179, #1864, #59215, #65221, #36564, #47869, #8252, #1517 ),
 .UNSPECIFIED., .F., .F. ) 
 B_SPLINE_CURVE_WITH_KNOTS ( ( 3, 2, 2, 2, 3 ),
 ( 0.5795454545454545858, 0.5852272727272727071, 0.5909090909090909394, 0.5965909090909090606, 0.6022727272727272929 ),
 .UNSPECIFIED. ) 
 CURVE ( )  GEOMETRIC_REPRESENTATION_ITEM ( )  RATIONAL_B_SPLINE_CURVE ( ( 1.000000000000000000, 0.9238795325112867385, 1.000000000000000000, 0.9238795325112867385, 1.000000000000000000, 0.9238795325112867385, 1.000000000000000000, 0.9238795325112867385, 1.000000000000000000 ) ) 
 REPRESENTATION_ITEM ( '' )  );
#41470=( BOUNDED_CURVE ( )  B_SPLINE_CURVE ( 2, ( #8368, #43064, #37424, #48352, #60424, #25337, #60047, #66455, #18953 ),
 .UNSPECIFIED., .F., .F. ) 
 B_SPLINE_CURVE_WITH_KNOTS ( ( 3, 2, 2, 2, 3 ),
 ( 0.1022727272727272790, 0.1079545454545454558, 0.1136363636363636326, 0.1193181818181818232, 0.1250000000000000000 ),
 .UNSPECIFIED. ) 
 CURVE ( )  GEOMETRIC_REPRESENTATION_ITEM ( )  RATIONAL_B_SPLINE_CURVE ( ( 1.000000000000000000, 0.9238795325112867385, 1.000000000000000000, 0.9238795325112867385, 1.000000000000000000, 0.9238795325112867385, 1.000000000000000000, 0.9238795325112867385, 1.000000000000000000 ) ) 
 REPRESENTATION_ITEM ( '' )  );
#41471=ORIENTED_EDGE ( 'NONE', *, *, #63812, .T. ) ;
#41473=CARTESIAN_POINT ( 'NONE',  ( 2.449293598294707893E-16, 11.25000000000000000, -4.000000000000001776 ) ) ;
#41475=CARTESIAN_POINT ( 'NONE',  ( -8.342170076843785083E-16, 12.06249999863440614, 4.541265875000002339 ) ) ;
#41477=AXIS2_PLACEMENT_3D ( 'NONE', #28790, #12179, #58592 ) ;
#41486=EDGE_CURVE ( 'NONE', #46633, #55561, #50424, .T. ) ;
#41542=CARTESIAN_POINT ( 'NONE',  ( -4.000000000000002665, 16.31249999726881228, 1.656854249492380582 ) ) ;
#41545=CYLINDRICAL_SURFACE ( 'NONE', #56238, 4.000000000000001776 ) ;
#41550=CARTESIAN_POINT ( 'NONE',  ( -2.828427124746192067, 8.625000000000000000, 2.828427124746190735 ) ) ;
#41553=CARTESIAN_POINT ( 'NONE',  ( 3.211159895383561835, 17.56249999863440792, -3.211159895383561835 ) ) ;
#41568=CARTESIAN_POINT ( 'NONE',  ( 2.449293598294707893E-16, 15.99999999726881406, -4.000000000000001776 ) ) ;
#41576=CARTESIAN_POINT ( 'NONE',  ( -4.541265875000002339, 12.81249999863440792, -5.561446717895856393E-16 ) ) ;
#41604=CARTESIAN_POINT ( 'NONE',  ( -1.881053915767124440, 2.999999998634407028, 4.541265875000001451 ) ) ;
#41608=VERTEX_POINT ( 'NONE', #56844 ) ;
#41611=MANIFOLD_SOLID_BREP ( 'Thread1', #17747 ) ;
#41623=CARTESIAN_POINT ( 'NONE',  ( -8.342170076843785083E-16, 16.18749999863440436, 4.541265875000002339 ) ) ;
#41640=CARTESIAN_POINT ( 'NONE',  ( -2.828427124746192067, 17.62500000000000000, 2.828427124746190735 ) ) ;
#41648=CARTESIAN_POINT ( 'NONE',  ( -4.541265875000002339, 5.874999998634407916, -1.881053915767121998 ) ) ;
#41658=CARTESIAN_POINT ( 'NONE',  ( 2.449293598294707893E-16, 0.9999999972688131678, -4.000000000000001776 ) ) ;
#41665=CARTESIAN_POINT ( 'NONE',  ( -1.881053915767124440, 3.999999998634406140, 4.541265875000001451 ) ) ;
#41687=CARTESIAN_POINT ( 'NONE',  ( -7.347880794884122694E-16, 17.49999999726881583, 4.000000000000001776 ) ) ;
#41707=CARTESIAN_POINT ( 'NONE',  ( -1.881053915767121554, 4.749999998634407028, -4.541265875000002339 ) ) ;
#41732=EDGE_CURVE ( 'NONE', #1512, #58564, #18010, .T. ) ;
#41766=CARTESIAN_POINT ( 'NONE',  ( -1.216988651335362936, 22.00000000000001066, -3.901072361666817034 ) ) ;
#41786=( BOUNDED_CURVE ( )  B_SPLINE_CURVE ( 2, ( #15429, #4883, #21836, #56569, #15059, #10533, #49393, #27878, #16541 ),
 .UNSPECIFIED., .F., .F. ) 
 B_SPLINE_CURVE_WITH_KNOTS ( ( 3, 2, 2, 2, 3 ),
 ( 0.7613636363636363535, 0.7670454545454545858, 0.7727272727272727071, 0.7784090909090909394, 0.7840909090909090606 ),
 .UNSPECIFIED. ) 
 CURVE ( )  GEOMETRIC_REPRESENTATION_ITEM ( )  RATIONAL_B_SPLINE_CURVE ( ( 1.000000000000000000, 0.9238795325112867385, 1.000000000000000000, 0.9238795325112867385, 1.000000000000000000, 0.9238795325112867385, 1.000000000000000000, 0.9238795325112867385, 1.000000000000000000 ) ) 
 REPRESENTATION_ITEM ( '' )  );
#41796=CARTESIAN_POINT ( 'NONE',  ( -3.211159895383561391, 14.68749999863440792, -3.211159895383561835 ) ) ;
#41828=ORIENTED_EDGE ( 'NONE', *, *, #13625, .F. ) ;
#41839=CARTESIAN_POINT ( 'NONE',  ( 2.828427124746191623, 11.12500000000000000, -2.828427124746191623 ) ) ;
#41841=CARTESIAN_POINT ( 'NONE',  ( -1.881053915767121776, 16.62499999863440436, -4.541265875000002339 ) ) ;
#41855=EDGE_LOOP ( 'NONE', ( #63716, #28798, #35198, #3421, #43696, #22243 ) ) ;
#41907=CARTESIAN_POINT ( 'NONE',  ( -4.000000000000002665, 3.562500000000000000, 1.656854249492380582 ) ) ;
#41917=CARTESIAN_POINT ( 'NONE',  ( -3.211159895383562723, 16.06249999863440436, 3.211159895383561391 ) ) ;
#41921=CARTESIAN_POINT ( 'NONE',  ( -4.541265875000002339, 0.9374999986344068059, -5.561446717895856393E-16 ) ) ;
#41927=CARTESIAN_POINT ( 'NONE',  ( 4.000000000000001776, 1.000000000000000222, 0.000000000000000000 ) ) ;
#41928=CARTESIAN_POINT ( 'NONE',  ( 2.828427124746191623, 13.87499999726881406, -2.828427124746191623 ) ) ;
#41937=CARTESIAN_POINT ( 'NONE',  ( 4.541265875000002339, 12.37499999863440969, -1.881053915767121554 ) ) ;
#41963=CARTESIAN_POINT ( 'NONE',  ( -1.881053915767121554, 0.6249999986344065839, -4.541265875000002339 ) ) ;
#41979=CARTESIAN_POINT ( 'NONE',  ( -4.541265875000002339, 14.93749999863440792, -5.561446717895856393E-16 ) ) ;
#42005=CARTESIAN_POINT ( 'NONE',  ( 3.211159895383560947, 4.312499998634407028, 3.211159895383562723 ) ) ;
#42016=CARTESIAN_POINT ( 'NONE',  ( -7.347880794884122694E-16, 1.499999997268813168, 4.000000000000001776 ) ) ;
#42022=CARTESIAN_POINT ( 'NONE',  ( -1.881053915767124440, 0.9999999986344065839, 4.541265875000001451 ) ) ;
#42063=CARTESIAN_POINT ( 'NONE',  ( 3.211159895383560947, 4.312499998634407028, 3.211159895383562723 ) ) ;
#42086=CARTESIAN_POINT ( 'NONE',  ( -4.000000000000001776, 9.500000000000000000, -4.898587196589415787E-16 ) ) ;
#42099=DIRECTION ( 'NONE',  ( 0.000000000000000000, 0.000000000000000000, -1.000000000000000000 ) ) ;
#42105=( BOUNDED_CURVE ( )  B_SPLINE_CURVE ( 2, ( #52083, #36858, #65142, #415, #42867, #46036, #19861, #17732, #7815 ),
 .UNSPECIFIED., .F., .F. ) 
 B_SPLINE_CURVE_WITH_KNOTS ( ( 3, 2, 2, 2, 3 ),
 ( 0.3750000000000000000, 0.3806818181818181768, 0.3863636363636363535, 0.3920454545454545858, 0.3977272727272727626 ),
 .UNSPECIFIED. ) 
 CURVE ( )  GEOMETRIC_REPRESENTATION_ITEM ( )  RATIONAL_B_SPLINE_CURVE ( ( 1.000000000000000000, 0.9238795325112867385, 1.000000000000000000, 0.9238795325112867385, 1.000000000000000000, 0.9238795325112867385, 1.000000000000000000, 0.9238795325112859613, 1.000000000000000666 ) ) 
 REPRESENTATION_ITEM ( '' )  );
#42108=CARTESIAN_POINT ( 'NONE',  ( -1.881053915767121554, 12.74999999863440969, -4.541265875000002339 ) ) ;
#42119=CARTESIAN_POINT ( 'NONE',  ( 4.000000000000000888, 19.93750000000000000, 1.656854249492384135 ) ) ;
#42145=LINE ( 'NONE', #36874, #44884 ) ;
#42150=CARTESIAN_POINT ( 'NONE',  ( -8.342170076843785083E-16, 13.06249999863440792, 4.541265875000002339 ) ) ;
#42160=ORIENTED_EDGE ( 'NONE', *, *, #1678, .T. ) ;
#42197=CARTESIAN_POINT ( 'NONE',  ( -2.828427124746192067, 13.62500000000000000, 2.828427124746190735 ) ) ;
#42198=CARTESIAN_POINT ( 'NONE',  ( -4.541265875000002339, 15.74999999863440436, -1.881053915767121998 ) ) ;
#42206=CARTESIAN_POINT ( 'NONE',  ( 2.828427124746190291, 6.624999997268813168, 2.828427124746192067 ) ) ;
#42216=ORIENTED_EDGE ( 'NONE', *, *, #68890, .T. ) ;
#42234=CYLINDRICAL_SURFACE ( 'NONE', #4646, 4.000000000000001776 ) ;
#42235=CARTESIAN_POINT ( 'NONE',  ( -1.656854249492381248, 16.31250000000000000, -4.000000000000001776 ) ) ;
#42246=EDGE_CURVE ( 'NONE', #30848, #62884, #38727, .T. ) ;
#42248=CARTESIAN_POINT ( 'NONE',  ( -4.000000000000001776, 8.249999997268814056, -4.898587196589415787E-16 ) ) ;
#42283=CARTESIAN_POINT ( 'NONE',  ( 3.211159895383560947, 17.31249999863440792, 3.211159895383562723 ) ) ;
#42284=ORIENTED_EDGE ( 'NONE', *, *, #23941, .T. ) ;
#42293=CARTESIAN_POINT ( 'NONE',  ( 2.828427124746190291, 15.62499999726881406, 2.828427124746192067 ) ) ;
#42294=CARTESIAN_POINT ( 'NONE',  ( 1.881053915767121998, 5.499999998634407028, -4.541265875000002339 ) ) ;
#42300=CARTESIAN_POINT ( 'NONE',  ( -8.342170076843785083E-16, 15.06249999863440792, 4.541265875000002339 ) ) ;
#42321=CARTESIAN_POINT ( 'NONE',  ( -7.347880794884122694E-16, 7.750000000000000000, 4.000000000000001776 ) ) ;
#42330=CARTESIAN_POINT ( 'NONE',  ( 4.541265875000002339, 2.374999998634407028, -1.881053915767121554 ) ) ;
#42349=CARTESIAN_POINT ( 'NONE',  ( 3.211159895383560947, 16.31249999863440436, 3.211159895383562723 ) ) ;
#42350=CARTESIAN_POINT ( 'NONE',  ( 2.449293598294707893E-16, 11.25000000000000000, -4.000000000000001776 ) ) ;
#42366=CARTESIAN_POINT ( 'NONE',  ( -2.828427124746190735, 17.37500000000000000, -2.828427124746191623 ) ) ;
#42374=CARTESIAN_POINT ( 'NONE',  ( 4.541265875000002339, 3.437499998634407028, 0.000000000000000000 ) ) ;
#42384=CARTESIAN_POINT ( 'NONE',  ( 1.656854249492381914, 1.562499997268813612, 4.000000000000000888 ) ) ;
#42390=CARTESIAN_POINT ( 'NONE',  ( -4.541265875000003227, 2.874999998634407028, 1.881053915767121110 ) ) ;
#42422=ORIENTED_EDGE ( 'NONE', *, *, #1308, .F. ) ;
#42429=( BOUNDED_CURVE ( )  B_SPLINE_CURVE ( 2, ( #55710, #10046, #19860, #37228, #4024, #60225, #67386, #66261, #49276 ),
 .UNSPECIFIED., .F., .F. ) 
 B_SPLINE_CURVE_WITH_KNOTS ( ( 3, 2, 2, 2, 3 ),
 ( 0.05681818181818182323, 0.06250000000000000000, 0.06818181818181817677, 0.07386363636363636742, 0.07954545454545454419 ),
 .UNSPECIFIED. ) 
 CURVE ( )  GEOMETRIC_REPRESENTATION_ITEM ( )  RATIONAL_B_SPLINE_CURVE ( ( 0.9999999999999998890, 0.9238795325112868495, 1.000000000000000000, 0.9238795325112867385, 1.000000000000000000, 0.9238795325112867385, 1.000000000000000000, 0.9238795325112867385, 1.000000000000000000 ) ) 
 REPRESENTATION_ITEM ( '' )  );
#42434=CARTESIAN_POINT ( 'NONE',  ( -4.541265875000002339, 3.874999998634407028, -1.881053915767121998 ) ) ;
#42481=CARTESIAN_POINT ( 'NONE',  ( -8.342170076843785083E-16, 10.18749999863440614, 4.541265875000002339 ) ) ;
#42499=CARTESIAN_POINT ( 'NONE',  ( -2.828427124746192067, 15.37499999726881406, 2.828427124746190735 ) ) ;
#42510=DIRECTION ( 'NONE',  ( -0.000000000000000000, -1.000000000000000000, -0.000000000000000000 ) ) ;
#42528=CARTESIAN_POINT ( 'NONE',  ( 3.211159895383560947, 13.18749999863440792, 3.211159895383562723 ) ) ;
#42538=ORIENTED_EDGE ( 'NONE', *, *, #44850, .T. ) ;
#42542=CARTESIAN_POINT ( 'NONE',  ( -7.347880794884122694E-16, 20.75000000000000000, 4.000000000000001776 ) ) ;
#42573=CARTESIAN_POINT ( 'NONE',  ( 4.000000000000000888, 17.93750000000000000, 1.656854249492384135 ) ) ;
#42574=CARTESIAN_POINT ( 'NONE',  ( 4.541265875000002339, 15.37499999863440614, -1.881053915767121776 ) ) ;
#42605=DIRECTION ( 'NONE',  ( -0.000000000000000000, -1.000000000000000000, -0.000000000000000000 ) ) ;
#42608=CARTESIAN_POINT ( 'NONE',  ( -2.828427124746190735, 16.37500000000000000, -2.828427124746191623 ) ) ;
#42635=ORIENTED_EDGE ( 'NONE', *, *, #48153, .T. ) ;
#42654=CARTESIAN_POINT ( 'NONE',  ( 4.541265875000001451, 16.37499999863440436, 1.881053915767124440 ) ) ;
#42656=VERTEX_POINT ( 'NONE', #67954 ) ;
#42658=CARTESIAN_POINT ( 'NONE',  ( 4.541265875000002339, 3.499999998634407028, -1.881053915767121554 ) ) ;
#42664=CARTESIAN_POINT ( 'NONE',  ( -4.000000000000002665, 3.562500000000000444, 1.656854249492380804 ) ) ;
#42665=CARTESIAN_POINT ( 'NONE',  ( 4.000000000000001776, 15.81249999726881228, -1.656854249492381248 ) ) ;
#42666=CARTESIAN_POINT ( 'NONE',  ( -1.881053915767124440, 1.999999998634406584, 4.541265875000001451 ) ) ;
#42672=CARTESIAN_POINT ( 'NONE',  ( -4.541265875000002339, 15.81249999863440436, -5.561446717895856393E-16 ) ) ;
#42699=CARTESIAN_POINT ( 'NONE',  ( 1.881053915767121776, 0.4999999986344067504, -4.541265875000002339 ) ) ;
#42719=CARTESIAN_POINT ( 'NONE',  ( 4.541265875000002339, 14.49999999863440969, -1.881053915767121554 ) ) ;
#42720=CARTESIAN_POINT ( 'NONE',  ( 1.656854249492381914, 10.81250000000000178, 4.000000000000000888 ) ) ;
#42742=CARTESIAN_POINT ( 'NONE',  ( -3.211159895383561391, 6.812499998634407028, -3.211159895383561835 ) ) ;
#42752=CARTESIAN_POINT ( 'NONE',  ( 2.828427124746191623, 9.125000000000000000, -2.828427124746191623 ) ) ;
#42753=CARTESIAN_POINT ( 'NONE',  ( -4.000000000000001776, 2.187499997268813168, -1.656854249492381470 ) ) ;
#42758=CARTESIAN_POINT ( 'NONE',  ( 1.881053915767121776, 3.499999998634407028, -4.541265875000002339 ) ) ;
#42801=CARTESIAN_POINT ( 'NONE',  ( -1.881053915767124440, 4.124999998634407028, 4.541265875000001451 ) ) ;
#42822=CARTESIAN_POINT ( 'NONE',  ( -1.656854249492383468, 9.687500000000000000, 4.000000000000000888 ) ) ;
#42843=AXIS2_PLACEMENT_3D ( 'NONE', #12520, #30982, #70607 ) ;
#42845=CARTESIAN_POINT ( 'NONE',  ( -4.541265875000003227, 10.99999999863440969, 1.881053915767121110 ) ) ;
#42863=ORIENTED_EDGE ( 'NONE', *, *, #4626, .F. ) ;
#42867=CARTESIAN_POINT ( 'NONE',  ( -4.000000000000001776, 9.249999997268814056, -4.898587196589415787E-16 ) ) ;
#42888=CARTESIAN_POINT ( 'NONE',  ( -8.342170076843785083E-16, 16.06249999863440436, 4.541265875000002339 ) ) ;
#42922=CARTESIAN_POINT ( 'NONE',  ( -4.000000000000001776, 19.50000000000000000, -4.898587196589415787E-16 ) ) ;
#42937=CARTESIAN_POINT ( 'NONE',  ( 4.000000000000001776, 15.00000000000000000, 0.000000000000000000 ) ) ;
#42938=CARTESIAN_POINT ( 'NONE',  ( 4.541265875000002339, 16.31249999863440436, 0.000000000000000000 ) ) ;
#42941=EDGE_LOOP ( 'NONE', ( #37110, #48382, #52158 ) ) ;
#42944=ADVANCED_FACE ( 'NONE', ( #48265 ), #42234, .T. ) ;
#43018=CARTESIAN_POINT ( 'NONE',  ( -3.211159895383561391, 20.81249999863440436, -3.211159895383561835 ) ) ;
#43021=CARTESIAN_POINT ( 'NONE',  ( 4.541265875000001451, 5.374999998634406140, 1.881053915767124440 ) ) ;
#43028=CARTESIAN_POINT ( 'NONE',  ( 2.449293598294707893E-16, 2.250000000000000444, -4.000000000000001776 ) ) ;
#43029=CARTESIAN_POINT ( 'NONE',  ( -1.656854249492383691, 19.43749999726880873, 4.000000000000000888 ) ) ;
#43030=CARTESIAN_POINT ( 'NONE',  ( -4.541265875000002339, 3.812499998634407028, -5.561446717895856393E-16 ) ) ;
#43038=CARTESIAN_POINT ( 'NONE',  ( 4.541265875000001451, 19.24999999863440436, 1.881053915767124440 ) ) ;
#43064=CARTESIAN_POINT ( 'NONE',  ( -1.656854249492381248, 3.062499997268813612, -4.000000000000001776 ) ) ;
#43070=CARTESIAN_POINT ( 'NONE',  ( -4.541265875000002339, 4.812499998634407028, -5.561446717895856393E-16 ) ) ;
#43088=CARTESIAN_POINT ( 'NONE',  ( -1.881053915767121554, 18.74999999863440436, -4.541265875000002339 ) ) ;
#43095=CARTESIAN_POINT ( 'NONE',  ( -1.656854249492383468, 12.43749999726881406, 4.000000000000000888 ) ) ;
#43102=ORIENTED_EDGE ( 'NONE', *, *, #62304, .T. ) ;
#43112=CARTESIAN_POINT ( 'NONE',  ( -4.541265875000002339, 8.937499998634407916, -5.561446717895856393E-16 ) ) ;
#43126=CARTESIAN_POINT ( 'NONE',  ( -7.347880794884122694E-16, 5.499999997268813168, 4.000000000000001776 ) ) ;
#43132=CARTESIAN_POINT ( 'NONE',  ( -3.211159895383561391, 4.687499998634407028, -3.211159895383561835 ) ) ;
#43176=CARTESIAN_POINT ( 'NONE',  ( 4.541265875000002339, 3.437499998634407028, 0.000000000000000000 ) ) ;
#43221=( BOUNDED_CURVE ( )  B_SPLINE_CURVE ( 2, ( #72210, #10342, #33366, #9221, #45045, #32242, #56367, #4688, #73708 ),
 .UNSPECIFIED., .F., .F. ) 
 B_SPLINE_CURVE_WITH_KNOTS ( ( 3, 2, 2, 2, 3 ),
 ( 0.2840909090909091161, 0.2897727272727272929, 0.2954545454545454697, 0.3011363636363636465, 0.3068181818181818232 ),
 .UNSPECIFIED. ) 
 CURVE ( )  GEOMETRIC_REPRESENTATION_ITEM ( )  RATIONAL_B_SPLINE_CURVE ( ( 1.000000000000000000, 0.9238795325112867385, 1.000000000000000000, 0.9238795325112867385, 1.000000000000000000, 0.9238795325112867385, 1.000000000000000000, 0.9238795325112867385, 1.000000000000000000 ) ) 
 REPRESENTATION_ITEM ( '' )  );
#43223=CARTESIAN_POINT ( 'NONE',  ( 3.211159895383560947, 10.31249999863440792, 3.211159895383562723 ) ) ;
#43249=LINE ( 'NONE', #66265, #16227 ) ;
#43256=VERTEX_POINT ( 'NONE', #57683 ) ;
#43260=EDGE_CURVE ( 'NONE', #22922, #27854, #9850, .T. ) ;
#43267=CARTESIAN_POINT ( 'NONE',  ( 1.881053915767122664, 14.12499999863440969, 4.541265875000001451 ) ) ;
#43297=EDGE_CURVE ( 'NONE', #3011, #33914, #192, .T. ) ;
#43302=CARTESIAN_POINT ( 'NONE',  ( -2.828427124746190735, 19.37500000000000000, -2.828427124746191623 ) ) ;
#43315=CARTESIAN_POINT ( 'NONE',  ( 2.449293598294707893E-16, 16.25000000000000000, -4.000000000000001776 ) ) ;
#43316=CARTESIAN_POINT ( 'NONE',  ( 4.541265875000001451, 14.24999999863440969, 1.881053915767124440 ) ) ;
#43330=EDGE_LOOP ( 'NONE', ( #64939, #31950, #7506, #34982 ) ) ;
#43338=CARTESIAN_POINT ( 'NONE',  ( -7.347880794884122694E-16, 13.75000000000000000, 4.000000000000001776 ) ) ;
#43343=EDGE_CURVE ( 'NONE', #23983, #62814, #52011, .T. ) ;
#43356=CARTESIAN_POINT ( 'NONE',  ( 2.449293598294707893E-16, 6.250000000000000000, -4.000000000000001776 ) ) ;
#43360=CARTESIAN_POINT ( 'NONE',  ( -4.000000000000002665, 8.312499997268814056, 1.656854249492380582 ) ) ;
#43371=CARTESIAN_POINT ( 'NONE',  ( 1.656854249492381914, 10.56249999726881406, 4.000000000000000888 ) ) ;
#43397=CARTESIAN_POINT ( 'NONE',  ( -4.195582579073398932, 22.00000000000000355, 1.737867247408543925 ) ) ;
#43400=CARTESIAN_POINT ( 'NONE',  ( -1.881053915767124440, 5.124999998634406140, 4.541265875000001451 ) ) ;
#43407=CARTESIAN_POINT ( 'NONE',  ( -4.000000000000001776, 4.437500000000000888, -1.656854249492381470 ) ) ;
#43408=CARTESIAN_POINT ( 'NONE',  ( -1.656854249492381248, 17.06249999726881938, -4.000000000000001776 ) ) ;
#43409=CARTESIAN_POINT ( 'NONE',  ( -3.211159895383561391, 2.687499998634407028, -3.211159895383561835 ) ) ;
#43414=CARTESIAN_POINT ( 'NONE',  ( -1.881053915767124440, 17.99999999863440436, 4.541265875000001451 ) ) ;
#43421=ORIENTED_EDGE ( 'NONE', *, *, #55810, .F. ) ;
#43437=CARTESIAN_POINT ( 'NONE',  ( 2.449293598294707893E-16, 5.250000000000000000, -4.000000000000001776 ) ) ;
#43446=CARTESIAN_POINT ( 'NONE',  ( 3.211159895383560947, 5.187499998634407028, 3.211159895383562723 ) ) ;
#43455=CARTESIAN_POINT ( 'NONE',  ( -7.347880794884122694E-16, 19.49999999726881228, 4.000000000000001776 ) ) ;
#43465=CARTESIAN_POINT ( 'NONE',  ( 4.541265875000002339, 21.49999999863440792, -1.881053915767121554 ) ) ;
#43475=CARTESIAN_POINT ( 'NONE',  ( 0.000000000000000000, 0.000000000000000000, 0.000000000000000000 ) ) ;
#43488=CARTESIAN_POINT ( 'NONE',  ( 1.881053915767121998, 10.62499999863440969, -4.541265875000002339 ) ) ;
#43499=CARTESIAN_POINT ( 'NONE',  ( 4.000000000000000888, 7.687499997268812280, 1.656854249492384135 ) ) ;
#43504=CARTESIAN_POINT ( 'NONE',  ( -8.342170076843785083E-16, 7.062499998634407028, 4.541265875000002339 ) ) ;
#43524=FACE_OUTER_BOUND ( 'NONE', #15400, .T. ) ;
#43549=CARTESIAN_POINT ( 'NONE',  ( -4.541265875000002339, 8.874999998634407916, -1.881053915767121998 ) ) ;
#43596=CARTESIAN_POINT ( 'NONE',  ( -3.211159895383562723, 15.06249999863440792, 3.211159895383561391 ) ) ;
#43645=CARTESIAN_POINT ( 'NONE',  ( -1.881053915767124440, 19.99999999863440436, 4.541265875000001451 ) ) ;
#43654=LINE ( 'NONE', #48931, #24209 ) ;
#43671=CARTESIAN_POINT ( 'NONE',  ( 0.000000000000000000, 0.000000000000000000, 0.000000000000000000 ) ) ;
#43685=CARTESIAN_POINT ( 'NONE',  ( -1.656854249492383468, 20.68750000000000000, 4.000000000000000888 ) ) ;
#43696=ORIENTED_EDGE ( 'NONE', *, *, #12476, .T. ) ;
#43697=CARTESIAN_POINT ( 'NONE',  ( 1.656854249492381914, 16.81250000000000355, 4.000000000000000888 ) ) ;
#43698=CARTESIAN_POINT ( 'NONE',  ( -1.881053915767121776, 20.62499999863441147, -4.541265875000002339 ) ) ;
#43761=VERTEX_POINT ( 'NONE', #62022 ) ;
#43772=VERTEX_POINT ( 'NONE', #72974 ) ;
#43780=CARTESIAN_POINT ( 'NONE',  ( -3.211159895383562723, 19.06249999863440436, 3.211159895383561391 ) ) ;
#43783=CARTESIAN_POINT ( 'NONE',  ( 4.541265875000002339, 4.437499998634407028, 0.000000000000000000 ) ) ;
#43791=CARTESIAN_POINT ( 'NONE',  ( -4.000000000000001776, 2.437500000000000444, -1.656854249492381470 ) ) ;
#43792=CARTESIAN_POINT ( 'NONE',  ( 1.656854249492381914, 16.56249999726881228, 4.000000000000000888 ) ) ;
#43793=CARTESIAN_POINT ( 'NONE',  ( -8.342170076843785083E-16, 2.062499998634406584, 4.541265875000002339 ) ) ;
#43801=CARTESIAN_POINT ( 'NONE',  ( -4.541265875000003227, 17.87499999863441147, 1.881053915767121110 ) ) ;
#43811=CARTESIAN_POINT ( 'NONE',  ( -1.656854249492383468, 21.43749999726881583, 4.000000000000000888 ) ) ;
#43831=CARTESIAN_POINT ( 'NONE',  ( 1.881053915767122664, 5.124999998634406140, 4.541265875000001451 ) ) ;
#43848=CARTESIAN_POINT ( 'NONE',  ( 4.541265875000002339, 18.43749999863440792, 0.000000000000000000 ) ) ;
#43871=CARTESIAN_POINT ( 'NONE',  ( -1.881053915767121776, 8.749999998634407916, -4.541265875000002339 ) ) ;
#43882=CARTESIAN_POINT ( 'NONE',  ( 2.449293598294707893E-16, 4.999999997268813168, -4.000000000000001776 ) ) ;
#43891=CARTESIAN_POINT ( 'NONE',  ( 2.780723358947928197E-16, 7.562499998634407028, -4.541265875000002339 ) ) ;
#43935=CARTESIAN_POINT ( 'NONE',  ( 3.211159895383561835, 9.562499998634406140, -3.211159895383561835 ) ) ;
#43939=CARTESIAN_POINT ( 'NONE',  ( 4.000000000000001776, 1.062500000000000222, -1.656854249492381248 ) ) ;
#43968=CARTESIAN_POINT ( 'NONE',  ( -2.828427124746190735, 7.375000000000000888, -2.828427124746191623 ) ) ;
#43977=CYLINDRICAL_SURFACE ( 'NONE', #24545, 4.000000000000001776 ) ;
#43978=CARTESIAN_POINT ( 'NONE',  ( -4.541265875000002339, 16.93749999863440436, -5.561446717895856393E-16 ) ) ;
#43979=EDGE_LOOP ( 'NONE', ( #28599, #45796, #26885, #67669 ) ) ;
#44000=( BOUNDED_CURVE ( )  B_SPLINE_CURVE ( 2, ( #2725, #8376, #54789, #14772, #71004, #13650, #3854, #37810, #3101 ),
 .UNSPECIFIED., .F., .F. ) 
 B_SPLINE_CURVE_WITH_KNOTS ( ( 3, 2, 2, 2, 3 ),
 ( 0.6022727272727272929, 0.6079545454545454142, 0.6136363636363636465, 0.6193181818181817677, 0.6250000000000000000 ),
 .UNSPECIFIED. ) 
 CURVE ( )  GEOMETRIC_REPRESENTATION_ITEM ( )  RATIONAL_B_SPLINE_CURVE ( ( 1.000000000000000000, 0.9238795325112867385, 1.000000000000000000, 0.9238795325112867385, 1.000000000000000000, 0.9238795325112867385, 1.000000000000000000, 0.9238795325112867385, 1.000000000000000000 ) ) 
 REPRESENTATION_ITEM ( '' )  );
#44027=CARTESIAN_POINT ( 'NONE',  ( 1.881053915767121776, 19.49999999863440436, -4.541265875000002339 ) ) ;
#44061=CARTESIAN_POINT ( 'NONE',  ( -4.000000000000001776, 11.18749999726881406, -1.656854249492381470 ) ) ;
#44078=CARTESIAN_POINT ( 'NONE',  ( -2.828427124746190735, 15.37500000000000000, -2.828427124746191623 ) ) ;
#44079=CARTESIAN_POINT ( 'NONE',  ( 3.211159895383561835, 21.43749999863440792, -3.211159895383561835 ) ) ;
#44109=AXIS2_PLACEMENT_3D ( 'NONE', #55566, #14797, #37457 ) ;
#44160=CARTESIAN_POINT ( 'NONE',  ( 3.211159895383561835, 21.56249999863440792, -3.211159895383561835 ) ) ;
#44163=CARTESIAN_POINT ( 'NONE',  ( -4.541265875000002339, 2.874999998634407028, -1.881053915767121998 ) ) ;
#44169=CARTESIAN_POINT ( 'NONE',  ( 2.828427124746190291, 5.875000000000000000, 2.828427124746192067 ) ) ;
#44170=CARTESIAN_POINT ( 'NONE',  ( 2.828427124746190291, 17.62499999726881583, 2.828427124746192067 ) ) ;
#44171=CARTESIAN_POINT ( 'NONE',  ( -4.541265875000002339, 6.812499998634407028, -5.561446717895856393E-16 ) ) ;
#44178=CARTESIAN_POINT ( 'NONE',  ( 3.211159895383560947, 18.18749999863440792, 3.211159895383562723 ) ) ;
#44200=CARTESIAN_POINT ( 'NONE',  ( -7.347880794884122694E-16, 5.750000000000000000, 4.000000000000001776 ) ) ;
#44211=CARTESIAN_POINT ( 'NONE',  ( 3.211159895383560947, 6.187499998634407028, 3.211159895383562723 ) ) ;
#44231=CARTESIAN_POINT ( 'NONE',  ( 2.780723358947928197E-16, 21.68749999863440792, -4.541265875000002339 ) ) ;
#44244=EDGE_CURVE ( 'NONE', #11511, #33915, #54141, .T. ) ;
#44253=CARTESIAN_POINT ( 'NONE',  ( -1.881053915767121776, 7.749999998634407916, -4.541265875000002339 ) ) ;
#44263=CARTESIAN_POINT ( 'NONE',  ( -2.828427124746190735, 5.124999997268813168, -2.828427124746191623 ) ) ;
#44265=ORIENTED_EDGE ( 'NONE', *, *, #58642, .F. ) ;
#44269=CARTESIAN_POINT ( 'NONE',  ( 2.780723358947928197E-16, 4.562499998634407028, -4.541265875000002339 ) ) ;
#44276=CARTESIAN_POINT ( 'NONE',  ( -7.347880794884122694E-16, 18.75000000000000000, 4.000000000000001776 ) ) ;
#44309=CARTESIAN_POINT ( 'NONE',  ( -8.342170076843785083E-16, 7.187499998634407028, 4.541265875000002339 ) ) ;
#44322=ORIENTED_EDGE ( 'NONE', *, *, #30634, .F. ) ;
#44340=ORIENTED_EDGE ( 'NONE', *, *, #28356, .T. ) ;
#44350=ORIENTED_EDGE ( 'NONE', *, *, #55945, .F. ) ;
#44355=CARTESIAN_POINT ( 'NONE',  ( 1.881053915767121776, 14.62499999863440969, -4.541265875000002339 ) ) ;
#44368=CARTESIAN_POINT ( 'NONE',  ( 0.000000000000000000, 22.00000000000000355, 0.000000000000000000 ) ) ;
#44397=CARTESIAN_POINT ( 'NONE',  ( -4.541265875000002339, 17.81249999863440792, -5.561446717895856393E-16 ) ) ;
#44428=CARTESIAN_POINT ( 'NONE',  ( -2.828427124746192067, 2.625000000000000000, 2.828427124746190735 ) ) ;
#44431=CARTESIAN_POINT ( 'NONE',  ( -4.000000000000001776, 11.24999999726881406, -4.898587196589415787E-16 ) ) ;
#44447=( BOUNDED_CURVE ( )  B_SPLINE_CURVE ( 2, ( #46377, #52046, #7503, #57717, #19180, #30141, #7133, #40718, #36173 ),
 .UNSPECIFIED., .F., .F. ) 
 B_SPLINE_CURVE_WITH_KNOTS ( ( 3, 2, 2, 2, 3 ),
 ( 0.9431818181818182323, 0.9488636363636363535, 0.9545454545454545858, 0.9602272727272727071, 0.9659090910434643407 ),
 .UNSPECIFIED. ) 
 CURVE ( )  GEOMETRIC_REPRESENTATION_ITEM ( )  RATIONAL_B_SPLINE_CURVE ( ( 1.000000000000000000, 0.9238795325112867385, 1.000000000000000000, 0.9238795325112867385, 1.000000000000000000, 0.9238795325112867385, 1.000000000000000000, 0.9238795325112867385, 1.000000000000000000 ) ) 
 REPRESENTATION_ITEM ( '' )  );
#44451=CARTESIAN_POINT ( 'NONE',  ( -1.656854249492381248, 20.31250000000000000, -4.000000000000001776 ) ) ;
#44452=CARTESIAN_POINT ( 'NONE',  ( -8.342170076843785083E-16, 21.06249999863440792, 4.541265875000002339 ) ) ;
#44461=ORIENTED_EDGE ( 'NONE', *, *, #36131, .F. ) ;
#44476=FACE_OUTER_BOUND ( 'NONE', #938, .T. ) ;
#44532=CARTESIAN_POINT ( 'NONE',  ( -1.881053915767124440, 21.12499999863441147, 4.541265875000001451 ) ) ;
#44535=CARTESIAN_POINT ( 'NONE',  ( -4.541265875000002339, 6.937499998634407916, -5.561446717895856393E-16 ) ) ;
#44541=EDGE_CURVE ( 'NONE', #33430, #56422, #28923, .T. ) ;
#44543=CARTESIAN_POINT ( 'NONE',  ( -2.828427124746190735, 7.375000000000000888, -2.828427124746191623 ) ) ;
#44544=CARTESIAN_POINT ( 'NONE',  ( 2.449293598294707893E-16, 16.99999999726881583, -4.000000000000001776 ) ) ;
#44545=CARTESIAN_POINT ( 'NONE',  ( -3.211159895383561391, 8.687499998634407916, -3.211159895383561835 ) ) ;
#44547=ORIENTED_EDGE ( 'NONE', *, *, #45849, .F. ) ;
#44551=CARTESIAN_POINT ( 'NONE',  ( -1.881053915767121554, 16.62499999863440436, -4.541265875000002339 ) ) ;
#44567=ADVANCED_FACE ( 'NONE', ( #44790 ), #68537, .F. ) ;
#44584=CARTESIAN_POINT ( 'NONE',  ( 3.211159895383561835, 5.437499998634407028, -3.211159895383561835 ) ) ;
#44597=CARTESIAN_POINT ( 'NONE',  ( 0.000000000000000000, 22.00000000000000000, 0.000000000000000000 ) ) ;
#44601=CARTESIAN_POINT ( 'NONE',  ( 4.541265875000002339, 19.49999999863440436, -1.881053915767121554 ) ) ;
#44622=CARTESIAN_POINT ( 'NONE',  ( 4.541265875000001451, 8.374999998634407916, 1.881053915767124440 ) ) ;
#44632=CARTESIAN_POINT ( 'NONE',  ( -4.000000000000001776, 7.187499997268813168, -1.656854249492381470 ) ) ;
#44639=CARTESIAN_POINT ( 'NONE',  ( 4.541265875000002339, 6.312499998634407028, 0.000000000000000000 ) ) ;
#44671=DIRECTION ( 'NONE',  ( 0.000000000000000000, -0.000000000000000000, 1.000000000000000000 ) ) ;
#44682=CARTESIAN_POINT ( 'NONE',  ( -1.881053915767121554, 6.749999998634407916, -4.541265875000002339 ) ) ;
#44698=CARTESIAN_POINT ( 'NONE',  ( 4.000000000000000888, 14.68749999726881406, 1.656854249492384135 ) ) ;
#44725=CARTESIAN_POINT ( 'NONE',  ( 1.881053915767122664, 14.24999999863440969, 4.541265875000001451 ) ) ;
#44771=CARTESIAN_POINT ( 'NONE',  ( 2.780723358947928197E-16, 19.56249999863440436, -4.541265875000002339 ) ) ;
#44778=DIRECTION ( 'NONE',  ( -0.000000000000000000, -1.000000000000000000, -0.000000000000000000 ) ) ;
#44790=FACE_OUTER_BOUND ( 'NONE', #35615, .T. ) ;
#44821=CARTESIAN_POINT ( 'NONE',  ( 4.000000000000001776, 22.00000000000000000, 0.000000000000000000 ) ) ;
#44822=CARTESIAN_POINT ( 'NONE',  ( -3.211159895383562723, 17.93749999863440792, 3.211159895383561391 ) ) ;
#44850=EDGE_CURVE ( 'NONE', #25046, #57615, #46073, .T. ) ;
#44856=AXIS2_PLACEMENT_3D ( 'NONE', #593, #69985, #6609 ) ;
#44884=VECTOR ( 'NONE', #70830, 1000.000000000000000 ) ;
#44910=CARTESIAN_POINT ( 'NONE',  ( -8.342170076843785083E-16, 6.187499998634407028, 4.541265875000002339 ) ) ;
#44915=CARTESIAN_POINT ( 'NONE',  ( -4.000000000000001776, 7.500000000000000000, -4.898587196589415787E-16 ) ) ;
#44916=CARTESIAN_POINT ( 'NONE',  ( 2.828427124746190291, 20.62499999726881583, 2.828427124746192067 ) ) ;
#44917=CARTESIAN_POINT ( 'NONE',  ( 4.541265875000001451, 8.249999998634406140, 1.881053915767124440 ) ) ;
#44926=CARTESIAN_POINT ( 'NONE',  ( 4.541265875000002339, 22.31249999863440436, 0.000000000000000000 ) ) ;
#44960=ORIENTED_EDGE ( 'NONE', *, *, #50964, .T. ) ;
#44995=CARTESIAN_POINT ( 'NONE',  ( -3.211159895383561391, 13.81249999863440614, -3.211159895383561835 ) ) ;
#45007=CARTESIAN_POINT ( 'NONE',  ( 2.449293598294707893E-16, 8.999999997268814056, -4.000000000000001776 ) ) ;
#45014=CARTESIAN_POINT ( 'NONE',  ( 3.211159895383561835, 10.43749999863440792, -3.211159895383561835 ) ) ;
#45045=CARTESIAN_POINT ( 'NONE',  ( -4.000000000000001776, 7.249999997268813168, -4.898587196589415787E-16 ) ) ;
#45055=CARTESIAN_POINT ( 'NONE',  ( 4.541265875000002339, 6.499999998634407028, -1.881053915767121554 ) ) ;
#45057=CARTESIAN_POINT ( 'NONE',  ( -2.828427124746190735, 5.124999997268813168, -2.828427124746191623 ) ) ;
#45070=CARTESIAN_POINT ( 'NONE',  ( 2.828427124746191623, 14.87499999726881406, -2.828427124746191623 ) ) ;
#45082=CARTESIAN_POINT ( 'NONE',  ( -1.656854249492383468, 4.687500000000000888, 4.000000000000000888 ) ) ;
#45095=CARTESIAN_POINT ( 'NONE',  ( -4.541265875000002339, 18.93749999863440436, -5.561446717895856393E-16 ) ) ;
#45138=CARTESIAN_POINT ( 'NONE',  ( -8.342170076843785083E-16, 17.06249999863440792, 4.541265875000002339 ) ) ;
#45162=ORIENTED_EDGE ( 'NONE', *, *, #74547, .T. ) ;
#45163=ADVANCED_FACE ( 'NONE', ( #27332 ), #6842, .T. ) ;
#45166=CARTESIAN_POINT ( 'NONE',  ( 4.000000000000001776, 6.000000000000000000, 0.000000000000000000 ) ) ;
#45193=CARTESIAN_POINT ( 'NONE',  ( 4.000000000000000888, 20.93750000000000000, 1.656854249492384135 ) ) ;
#45194=CARTESIAN_POINT ( 'NONE',  ( -3.211159895383562723, 18.93749999863440436, 3.211159895383561391 ) ) ;
#45227=DIRECTION ( 'NONE',  ( 0.000000000000000000, 1.000000000000000000, 0.000000000000000000 ) ) ;
#45255=VERTEX_POINT ( 'NONE', #73735 ) ;
#45265=EDGE_CURVE ( 'NONE', #8511, #31876, #47500, .T. ) ;
#45269=ORIENTED_EDGE ( 'NONE', *, *, #23459, .T. ) ;
#45275=CARTESIAN_POINT ( 'NONE',  ( -4.541265875000002339, 9.874999998634404363, -1.881053915767121998 ) ) ;
#45280=CARTESIAN_POINT ( 'NONE',  ( 4.000000000000001776, 7.000000000000000000, 0.000000000000000000 ) ) ;
#45282=CARTESIAN_POINT ( 'NONE',  ( 1.881053915767122664, 6.124999998634407916, 4.541265875000001451 ) ) ;
#45340=CARTESIAN_POINT ( 'NONE',  ( -1.656854249492383468, 20.43749999726881228, 4.000000000000000888 ) ) ;
#45355=ORIENTED_EDGE ( 'NONE', *, *, #757, .F. ) ;
#45357=CARTESIAN_POINT ( 'NONE',  ( 4.541265875000001451, 13.37499999863440969, 1.881053915767124440 ) ) ;
#45365=CARTESIAN_POINT ( 'NONE',  ( -4.000000000000001776, 10.18749999726881406, -1.656854249492381470 ) ) ;
#45372=CARTESIAN_POINT ( 'NONE',  ( -4.541265875000002339, 10.74999999863440969, -1.881053915767121998 ) ) ;
#45412=CARTESIAN_POINT ( 'NONE',  ( -3.211159895383561391, 10.81249999863440792, -3.211159895383561835 ) ) ;
#45434=ORIENTED_EDGE ( 'NONE', *, *, #23941, .F. ) ;
#45457=CARTESIAN_POINT ( 'NONE',  ( 4.541265875000002339, 18.43749999863440792, 0.000000000000000000 ) ) ;
#45464=VERTEX_POINT ( 'NONE', #60746 ) ;
#45483=DIRECTION ( 'NONE',  ( 0.000000000000000000, 0.000000000000000000, -1.000000000000000000 ) ) ;
#45501=CARTESIAN_POINT ( 'NONE',  ( -8.342170076843785083E-16, 21.06249999863440792, 4.541265875000002339 ) ) ;
#45504=CARTESIAN_POINT ( 'NONE',  ( -2.828427124746190735, 1.375000000000000222, -2.828427124746191623 ) ) ;
#45533=EDGE_CURVE ( 'NONE', #25548, #47792, #50383, .T. ) ;
#45537=CARTESIAN_POINT ( 'NONE',  ( -4.000000000000002665, 1.312499997268813168, 1.656854249492380582 ) ) ;
#45539=CARTESIAN_POINT ( 'NONE',  ( 2.828427124746191623, 0.8749999972688131678, -2.828427124746191623 ) ) ;
#45562=CARTESIAN_POINT ( 'NONE',  ( 1.656854249492381914, 18.81250000000000000, 4.000000000000000888 ) ) ;
#45586=EDGE_CURVE ( 'NONE', #62814, #31018, #9402, .T. ) ;
#45625=CARTESIAN_POINT ( 'NONE',  ( -7.347880794884122694E-16, 3.750000000000000000, 4.000000000000001776 ) ) ;
#45641=CARTESIAN_POINT ( 'NONE',  ( -8.342170076843785083E-16, 7.187499998634407028, 4.541265875000002339 ) ) ;
#45645=CARTESIAN_POINT ( 'NONE',  ( -4.000000000000001776, 6.437500000000000888, -1.656854249492381470 ) ) ;
#45647=CARTESIAN_POINT ( 'NONE',  ( 1.656854249492381914, 21.56249999726881583, 4.000000000000000888 ) ) ;
#45648=CARTESIAN_POINT ( 'NONE',  ( 2.780723358947928197E-16, 8.562499998634407916, -4.541265875000002339 ) ) ;
#45657=CARTESIAN_POINT ( 'NONE',  ( -1.881053915767121554, 20.62499999863441147, -4.541265875000002339 ) ) ;
#45689=CARTESIAN_POINT ( 'NONE',  ( 2.828427124746191623, 11.87499999726881406, -2.828427124746191623 ) ) ;
#45726=CARTESIAN_POINT ( 'NONE',  ( 2.780723358947928197E-16, 11.68749999863440614, -4.541265875000002339 ) ) ;
#45736=CARTESIAN_POINT ( 'NONE',  ( 2.828427124746191623, 9.874999997268814056, -2.828427124746191623 ) ) ;
#45737=CARTESIAN_POINT ( 'NONE',  ( 2.449293598294707893E-16, 18.25000000000000000, -4.000000000000001776 ) ) ;
#45746=CARTESIAN_POINT ( 'NONE',  ( 4.541265875000001451, 10.24999999863440792, 1.881053915767124440 ) ) ;
#45747=AXIS2_PLACEMENT_3D ( 'NONE', #4312, #15607, #60520 ) ;
#45792=CARTESIAN_POINT ( 'NONE',  ( 4.541265875000002339, 10.43749999863440792, 0.000000000000000000 ) ) ;
#45796=ORIENTED_EDGE ( 'NONE', *, *, #50082, .F. ) ;
#45802=CARTESIAN_POINT ( 'NONE',  ( 4.000000000000001776, 7.000000000000000000, 0.000000000000000000 ) ) ;
#45819=CARTESIAN_POINT ( 'NONE',  ( -4.541265875000003227, 0.9999999986344068059, 1.881053915767121110 ) ) ;
#45822=VECTOR ( 'NONE', #20621, 1000.000000000000000 ) ;
#45831=CARTESIAN_POINT ( 'NONE',  ( -1.656854249492383468, 15.68750000000000000, 4.000000000000000888 ) ) ;
#45832=CARTESIAN_POINT ( 'NONE',  ( 2.780723358947928197E-16, 21.68749999863440792, -4.541265875000002339 ) ) ;
#45840=ORIENTED_EDGE ( 'NONE', *, *, #2931, .T. ) ;
#45848=VERTEX_POINT ( 'NONE', #64100 ) ;
#45849=EDGE_CURVE ( 'NONE', #48578, #54437, #36171, .T. ) ;
#45864=CARTESIAN_POINT ( 'NONE',  ( 0.000000000000000000, 0.000000000000000000, 0.000000000000000000 ) ) ;
#45869=EDGE_LOOP ( 'NONE', ( #16894, #42538, #14619, #52515, #44960, #65144 ) ) ;
#45879=CARTESIAN_POINT ( 'NONE',  ( -1.881053915767124440, 2.124999998634406584, 4.541265875000001451 ) ) ;
#45886=DIRECTION ( 'NONE',  ( 1.000000000000000000, -0.000000000000000000, -0.000000000000000000 ) ) ;
#45896=CARTESIAN_POINT ( 'NONE',  ( 0.000000000000000000, 0.000000000000000000, 0.000000000000000000 ) ) ;
#45906=CARTESIAN_POINT ( 'NONE',  ( 4.000000000000000888, 9.687499997268814056, 1.656854249492384135 ) ) ;
#45937=CARTESIAN_POINT ( 'NONE',  ( -4.000000000000002665, 20.56250000000000355, 1.656854249492380804 ) ) ;
#45953=CARTESIAN_POINT ( 'NONE',  ( 2.449293598294707893E-16, 21.25000000000000000, -4.000000000000001776 ) ) ;
#45962=( BOUNDED_CURVE ( )  B_SPLINE_CURVE ( 2, ( #51783, #51039, #16315, #131, #23107, #46120, #11057, #39351, #10679 ),
 .UNSPECIFIED., .F., .F. ) 
 B_SPLINE_CURVE_WITH_KNOTS ( ( 3, 2, 2, 2, 3 ),
 ( 0.4204545454545454697, 0.4261363636363636465, 0.4318181818181818232, 0.4375000000000000000, 0.4431818181818181768 ),
 .UNSPECIFIED. ) 
 CURVE ( )  GEOMETRIC_REPRESENTATION_ITEM ( )  RATIONAL_B_SPLINE_CURVE ( ( 1.000000000000000000, 0.9238795325112867385, 1.000000000000000000, 0.9238795325112867385, 1.000000000000000000, 0.9238795325112867385, 1.000000000000000000, 0.9238795325112867385, 1.000000000000000000 ) ) 
 REPRESENTATION_ITEM ( '' )  );
#45966=EDGE_CURVE ( 'NONE', #29151, #38403, #6982, .T. ) ;
#45972=CARTESIAN_POINT ( 'NONE',  ( -4.541265875000002339, 9.812499998634406140, -5.561446717895856393E-16 ) ) ;
#46007=ORIENTED_EDGE ( 'NONE', *, *, #72395, .T. ) ;
#46009=DIRECTION ( 'NONE',  ( 1.000000000000000000, 0.000000000000000000, -0.000000000000000000 ) ) ;
#46013=CARTESIAN_POINT ( 'NONE',  ( -4.541265875000003227, 6.999999998634407916, 1.881053915767121110 ) ) ;
#46019=CARTESIAN_POINT ( 'NONE',  ( -4.000000000000001776, 8.500000000000000000, -4.898587196589415787E-16 ) ) ;
#46020=CARTESIAN_POINT ( 'NONE',  ( -4.000000000000001776, 21.18749999726881583, -1.656854249492381470 ) ) ;
#46021=CARTESIAN_POINT ( 'NONE',  ( 4.541265875000001451, 10.24999999863440792, 1.881053915767124440 ) ) ;
#46031=CARTESIAN_POINT ( 'NONE',  ( 2.780723358947928197E-16, 21.56249999863440792, -4.541265875000002339 ) ) ;
#46036=CARTESIAN_POINT ( 'NONE',  ( -4.000000000000002665, 9.312499997268814056, 1.656854249492380582 ) ) ;
#46073=CIRCLE ( 'NONE', #64114, 9.949874371066211864 ) ;
#46083=CARTESIAN_POINT ( 'NONE',  ( 2.449293598294707893E-16, 19.99999999726881228, -4.000000000000001776 ) ) ;
#46092=EDGE_CURVE ( 'NONE', #55774, #40293, #24818, .T. ) ;
#46100=CARTESIAN_POINT ( 'NONE',  ( -8.342170076843785083E-16, 13.18749999863440792, 4.541265875000002339 ) ) ;
#46111=CARTESIAN_POINT ( 'NONE',  ( -4.000000000000001776, 11.24999999726881406, -4.898587196589415787E-16 ) ) ;
#46114=AXIS2_PLACEMENT_3D ( 'NONE', #43671, #66682, #61023 ) ;
#46119=CARTESIAN_POINT ( 'NONE',  ( -3.211159895383562723, 10.93749999863440792, 3.211159895383561391 ) ) ;
#46120=CARTESIAN_POINT ( 'NONE',  ( -4.000000000000002665, 10.31249999726881406, 1.656854249492380582 ) ) ;
#46163=CARTESIAN_POINT ( 'NONE',  ( 2.780723358947928197E-16, 12.68749999863440792, -4.541265875000002339 ) ) ;
#46165=CARTESIAN_POINT ( 'NONE',  ( 2.828427124746191623, 7.874999997268813168, -2.828427124746191623 ) ) ;
#46190=CARTESIAN_POINT ( 'NONE',  ( -1.881053915767124440, 1.124999998634406584, 4.541265875000001451 ) ) ;
#46207=CARTESIAN_POINT ( 'NONE',  ( 3.211159895383560947, 18.31249999863440792, 3.211159895383562723 ) ) ;
#46237=DIRECTION ( 'NONE',  ( -0.000000000000000000, -1.000000000000000000, -0.000000000000000000 ) ) ;
#46245=CARTESIAN_POINT ( 'NONE',  ( -4.000000000000002665, 11.56250000000000000, 1.656854249492380582 ) ) ;
#46249=CARTESIAN_POINT ( 'NONE',  ( 2.780723358947928197E-16, 20.56249999863440436, -4.541265875000002339 ) ) ;
#46255=VERTEX_POINT ( 'NONE', #14100 ) ;
#46258=LINE ( 'NONE', #28913, #61542 ) ;
#46262=ADVANCED_FACE ( 'NONE', ( #35665 ), #59412, .T. ) ;
#46301=EDGE_CURVE ( 'NONE', #33914, #22922, #63374, .T. ) ;
#46343=CARTESIAN_POINT ( 'NONE',  ( 1.881053915767121776, 8.499999998634406140, -4.541265875000002339 ) ) ;
#46371=CARTESIAN_POINT ( 'NONE',  ( 4.000000000000000888, 3.937500000000000000, 1.656854249492384135 ) ) ;
#46377=CARTESIAN_POINT ( 'NONE',  ( -7.347880794884122694E-16, 21.49999999726881583, 4.000000000000001776 ) ) ;
#46382=EDGE_CURVE ( 'NONE', #62160, #16346, #61641, .T. ) ;
#46387=CARTESIAN_POINT ( 'NONE',  ( -8.342170076843785083E-16, 12.18749999863440614, 4.541265875000002339 ) ) ;
#46391=CARTESIAN_POINT ( 'NONE',  ( 4.000000000000000888, 13.93750000000000000, 1.656854249492384135 ) ) ;
#46393=CARTESIAN_POINT ( 'NONE',  ( -3.211159895383562723, 10.93749999863440792, 3.211159895383561391 ) ) ;
#46404=CARTESIAN_POINT ( 'NONE',  ( 2.449293598294707893E-16, 10.25000000000000000, -4.000000000000001776 ) ) ;
#46472=CARTESIAN_POINT ( 'NONE',  ( 4.541265875000001451, 12.37499999863440969, 1.881053915767124440 ) ) ;
#46476=CARTESIAN_POINT ( 'NONE',  ( 3.211159895383561835, 0.5624999986344069169, -3.211159895383561835 ) ) ;
#46481=CARTESIAN_POINT ( 'NONE',  ( -4.000000000000001776, 1.437500000000000444, -1.656854249492381470 ) ) ;
#46482=CARTESIAN_POINT ( 'NONE',  ( 2.828427124746191623, 8.874999997268814056, -2.828427124746191623 ) ) ;
#46483=CARTESIAN_POINT ( 'NONE',  ( 2.780723358947928197E-16, 0.5624999986344066949, -4.541265875000002339 ) ) ;
#46489=CARTESIAN_POINT ( 'NONE',  ( 3.211159895383560947, 11.18749999863440792, 3.211159895383562723 ) ) ;
#46490=CARTESIAN_POINT ( 'NONE',  ( -4.000000000000001776, 18.18749999726881583, -1.656854249492381470 ) ) ;
#46530=LINE ( 'NONE', #23892, #71568 ) ;
#46536=CARTESIAN_POINT ( 'NONE',  ( -4.541265875000002339, 13.93749999863440614, -5.561446717895856393E-16 ) ) ;
#46539=CARTESIAN_POINT ( 'NONE',  ( -7.347880794884122694E-16, 4.499999997268813168, 4.000000000000001776 ) ) ;
#46572=CARTESIAN_POINT ( 'NONE',  ( 2.828427124746190291, 2.875000000000000000, 2.828427124746192067 ) ) ;
#46573=CARTESIAN_POINT ( 'NONE',  ( -1.881053915767121554, 19.74999999863440792, -4.541265875000002339 ) ) ;
#46587=CARTESIAN_POINT ( 'NONE',  ( -7.071067811865482611, 22.99999999999999645, 1.000000000000000000 ) ) ;
#46594=EDGE_LOOP ( 'NONE', ( #61828, #19693, #41213, #50642 ) ) ;
#46621=CARTESIAN_POINT ( 'NONE',  ( -3.211159895383562723, 20.93749999863440436, 3.211159895383561391 ) ) ;
#46628=CARTESIAN_POINT ( 'NONE',  ( 2.828427124746190291, 15.62499999726881406, 2.828427124746192067 ) ) ;
#46633=VERTEX_POINT ( 'NONE', #66923 ) ;
#46692=CARTESIAN_POINT ( 'NONE',  ( 2.828427124746190291, 20.87500000000000000, 2.828427124746192067 ) ) ;
#46708=CARTESIAN_POINT ( 'NONE',  ( -3.211159895383561391, 11.68749999863440614, -3.211159895383561835 ) ) ;
#46738=CARTESIAN_POINT ( 'NONE',  ( 2.828427124746190291, 18.62499999726881583, 2.828427124746192067 ) ) ;
#46754=CARTESIAN_POINT ( 'NONE',  ( 4.000000000000001776, 13.06250000000000000, -1.656854249492381248 ) ) ;
#46756=CARTESIAN_POINT ( 'NONE',  ( -4.541265875000003227, 10.87499999863440969, 1.881053915767121110 ) ) ;
#46825=CARTESIAN_POINT ( 'NONE',  ( 0.000000000000000000, 0.000000000000000000, 0.000000000000000000 ) ) ;
#46841=CARTESIAN_POINT ( 'NONE',  ( -4.541265875000002339, 17.87499999863441147, -1.881053915767121998 ) ) ;
#46851=CARTESIAN_POINT ( 'NONE',  ( 2.828427124746190291, 1.875000000000000222, 2.828427124746192067 ) ) ;
#46852=CARTESIAN_POINT ( 'NONE',  ( 4.000000000000001776, 13.81249999726881406, -1.656854249492381248 ) ) ;
#46861=CARTESIAN_POINT ( 'NONE',  ( -4.541265875000002339, 15.74999999863440614, -1.881053915767121998 ) ) ;
#46885=CARTESIAN_POINT ( 'NONE',  ( 0.000000000000000000, 0.000000000000000000, -4.000000000000001776 ) ) ;
#46890=CARTESIAN_POINT ( 'NONE',  ( 4.541265875000002339, 0.3749999986344066949, -1.881053915767121554 ) ) ;
#46905=CARTESIAN_POINT ( 'NONE',  ( -8.342170076843785083E-16, 12.18749999863440614, 4.541265875000002339 ) ) ;
#46908=CARTESIAN_POINT ( 'NONE',  ( 2.828427124746190291, 7.624999997268813168, 2.828427124746192067 ) ) ;
#46931=CARTESIAN_POINT ( 'NONE',  ( -4.541265875000002339, 5.937499998634407028, -5.561446717895856393E-16 ) ) ;
#46941=CARTESIAN_POINT ( 'NONE',  ( 2.828427124746190291, 3.624999997268813168, 2.828427124746192067 ) ) ;
#46979=ORIENTED_EDGE ( 'NONE', *, *, #40922, .F. ) ;
#46983=CARTESIAN_POINT ( 'NONE',  ( -4.000000000000001776, 11.50000000000000000, -4.898587196589415787E-16 ) ) ;
#46987=CARTESIAN_POINT ( 'NONE',  ( -4.541265875000002339, 0.8749999986344069169, -1.881053915767121998 ) ) ;
#46998=ORIENTED_EDGE ( 'NONE', *, *, #69485, .T. ) ;
#47039=VECTOR ( 'NONE', #70907, 1000.000000000000000 ) ;
#47043=CARTESIAN_POINT ( 'NONE',  ( 2.449293598294707893E-16, 2.999999997268813168, -4.000000000000001776 ) ) ;
#47076=CARTESIAN_POINT ( 'NONE',  ( -4.541265875000002339, 10.81249999863440792, -5.561446717895856393E-16 ) ) ;
#47100=CARTESIAN_POINT ( 'NONE',  ( 4.000000000000001776, 4.000000000000000000, 0.000000000000000000 ) ) ;
#47123=CARTESIAN_POINT ( 'NONE',  ( 4.000000000000001776, 11.00000000000000000, 0.000000000000000000 ) ) ;
#47125=CARTESIAN_POINT ( 'NONE',  ( -4.541265875000002339, 12.74999999863440969, -1.881053915767121998 ) ) ;
#47133=FACE_OUTER_BOUND ( 'NONE', #64395, .T. ) ;
#47194=CARTESIAN_POINT ( 'NONE',  ( -2.828427124746190735, 16.12499999726881228, -2.828427124746191623 ) ) ;
#47203=CARTESIAN_POINT ( 'NONE',  ( -4.000000000000002665, 8.562500000000000000, 1.656854249492380582 ) ) ;
#47206=CARTESIAN_POINT ( 'NONE',  ( -1.881053915767124440, 16.12499999863440436, 4.541265875000001451 ) ) ;
#47214=CARTESIAN_POINT ( 'NONE',  ( 1.656854249492381248, 1.187500000000000444, -4.000000000000001776 ) ) ;
#47215=CARTESIAN_POINT ( 'NONE',  ( -7.347880794884122694E-16, 15.49999999726881406, 4.000000000000001776 ) ) ;
#47225=CARTESIAN_POINT ( 'NONE',  ( 4.541265875000002339, 14.37499999863440969, -1.881053915767121554 ) ) ;
#47247=CARTESIAN_POINT ( 'NONE',  ( 1.656854249492381914, 7.812500000000000000, 4.000000000000000888 ) ) ;
#47254=CARTESIAN_POINT ( 'NONE',  ( 2.780723358947928197E-16, 0.5624999986344066949, -4.541265875000002339 ) ) ;
#47266=DIRECTION ( 'NONE',  ( -0.000000000000000000, -1.000000000000000000, -0.000000000000000000 ) ) ;
#47271=CARTESIAN_POINT ( 'NONE',  ( 3.211159895383561835, 15.56249999863440614, -3.211159895383561835 ) ) ;
#47300=CARTESIAN_POINT ( 'NONE',  ( 3.211159895383561835, 4.562499998634407028, -3.211159895383561835 ) ) ;
#47312=CARTESIAN_POINT ( 'NONE',  ( 1.881053915767122664, 22.24999999863440792, 4.541265875000001451 ) ) ;
#47318=CARTESIAN_POINT ( 'NONE',  ( -4.541265875000002339, 1.812499998634406584, -5.561446717895856393E-16 ) ) ;
#47322=ORIENTED_EDGE ( 'NONE', *, *, #17707, .F. ) ;
#47359=CARTESIAN_POINT ( 'NONE',  ( -1.881053915767124440, 6.124999998634407916, 4.541265875000001451 ) ) ;
#47431=CARTESIAN_POINT ( 'NONE',  ( 0.000000000000000000, 0.000000000000000000, 0.000000000000000000 ) ) ;
#47449=CARTESIAN_POINT ( 'NONE',  ( 1.881053915767121776, 13.49999999863440969, -4.541265875000002339 ) ) ;
#47489=CARTESIAN_POINT ( 'NONE',  ( -7.347880794884122694E-16, 11.75000000000000000, 4.000000000000001776 ) ) ;
#47491=CARTESIAN_POINT ( 'NONE',  ( 3.211159895383560947, 11.18749999863440792, 3.211159895383562723 ) ) ;
#47500=( BOUNDED_CURVE ( )  B_SPLINE_CURVE ( 2, ( #56395, #18162, #10000, #44698, #62044, #41178, #45070, #10735, #64188 ),
 .UNSPECIFIED., .F., .F. ) 
 B_SPLINE_CURVE_WITH_KNOTS ( ( 3, 2, 2, 2, 3 ),
 ( 0.6250000000000000000, 0.6306818181818182323, 0.6363636363636363535, 0.6420454545454545858, 0.6477272727272727071 ),
 .UNSPECIFIED. ) 
 CURVE ( )  GEOMETRIC_REPRESENTATION_ITEM ( )  RATIONAL_B_SPLINE_CURVE ( ( 1.000000000000000000, 0.9238795325112867385, 1.000000000000000000, 0.9238795325112867385, 1.000000000000000000, 0.9238795325112867385, 1.000000000000000000, 0.9238795325112867385, 1.000000000000000000 ) ) 
 REPRESENTATION_ITEM ( '' )  );
#47515=CARTESIAN_POINT ( 'NONE',  ( -4.000000000000001776, 0.4375000000000002220, -1.656854249492381470 ) ) ;
#47559=CARTESIAN_POINT ( 'NONE',  ( -4.000000000000001776, 3.500000000000000000, -4.898587196589415787E-16 ) ) ;
#47564=EDGE_CURVE ( 'NONE', #65881, #47792, #62861, .T. ) ;
#47571=CARTESIAN_POINT ( 'NONE',  ( 1.881053915767122664, 16.24999999863440436, 4.541265875000001451 ) ) ;
#47580=CARTESIAN_POINT ( 'NONE',  ( -7.347880794884122694E-16, 0.7500000000000002220, 4.000000000000001776 ) ) ;
#47581=CARTESIAN_POINT ( 'NONE',  ( -1.656854249492381248, 15.06249999726881406, -4.000000000000001776 ) ) ;
#47582=CARTESIAN_POINT ( 'NONE',  ( 1.881053915767121998, 0.4999999986344067504, -4.541265875000002339 ) ) ;
#47588=CARTESIAN_POINT ( 'NONE',  ( -8.342170076843785083E-16, 16.06249999863440436, 4.541265875000002339 ) ) ;
#47610=FACE_OUTER_BOUND ( 'NONE', #20919, .T. ) ;
#47616=CARTESIAN_POINT ( 'NONE',  ( -3.211159895383562723, 0.9374999986344068059, 3.211159895383561391 ) ) ;
#47619=CARTESIAN_POINT ( 'NONE',  ( 1.656854249492381248, 5.187500000000000888, -4.000000000000001776 ) ) ;
#47636=CARTESIAN_POINT ( 'NONE',  ( -3.211159895383562723, 17.06249999863440792, 3.211159895383561391 ) ) ;
#47638=CARTESIAN_POINT ( 'NONE',  ( 4.000000000000000888, 10.68749999726881406, 1.656854249492384135 ) ) ;
#47660=CARTESIAN_POINT ( 'NONE',  ( 1.881053915767121998, 5.624999998634407028, -4.541265875000002339 ) ) ;
#47671=CARTESIAN_POINT ( 'NONE',  ( 1.656854249492381914, 3.562499997268812724, 4.000000000000000888 ) ) ;
#47677=CARTESIAN_POINT ( 'NONE',  ( 1.881053915767122664, 1.124999998634406584, 4.541265875000001451 ) ) ;
#47722=CARTESIAN_POINT ( 'NONE',  ( -3.211159895383562723, 6.062499998634407028, 3.211159895383561391 ) ) ;
#47727=CARTESIAN_POINT ( 'NONE',  ( -7.347880794884122694E-16, 19.49999999726881228, 4.000000000000001776 ) ) ;
#47745=CARTESIAN_POINT ( 'NONE',  ( -2.828427124746190735, 9.375000000000000000, -2.828427124746191623 ) ) ;
#47757=CARTESIAN_POINT ( 'NONE',  ( 3.260352326811678303, 22.00000000000002842, 2.654260131296421132 ) ) ;
#47764=EDGE_CURVE ( 'NONE', #21170, #57934, #59894, .T. ) ;
#47767=CARTESIAN_POINT ( 'NONE',  ( 1.881053915767122664, 13.24999999863441147, 4.541265875000001451 ) ) ;
#47792=VERTEX_POINT ( 'NONE', #7478 ) ;
#47801=CARTESIAN_POINT ( 'NONE',  ( 1.656854249492381248, 19.18749999999999645, -4.000000000000001776 ) ) ;
#47812=CARTESIAN_POINT ( 'NONE',  ( 1.881053915767122664, 16.12499999863440792, 4.541265875000001451 ) ) ;
#47829=CARTESIAN_POINT ( 'NONE',  ( -7.347880794884122694E-16, 13.49999999726881406, 4.000000000000001776 ) ) ;
#47832=CARTESIAN_POINT ( 'NONE',  ( 2.449293598294707893E-16, 13.25000000000000000, -4.000000000000001776 ) ) ;
#47859=CARTESIAN_POINT ( 'NONE',  ( 1.656854249492381248, 12.18750000000000000, -4.000000000000001776 ) ) ;
#47861=CARTESIAN_POINT ( 'NONE',  ( 1.881053915767121998, 17.49999999863440436, -4.541265875000002339 ) ) ;
#47867=ADVANCED_FACE ( 'NONE', ( #26668 ), #10076, .T. ) ;
#47869=CARTESIAN_POINT ( 'NONE',  ( 2.828427124746191623, 13.87499999726881406, -2.828427124746191623 ) ) ;
#47897=CARTESIAN_POINT ( 'NONE',  ( 2.449293598294707893E-16, 12.25000000000000000, -4.000000000000001776 ) ) ;
#47907=CARTESIAN_POINT ( 'NONE',  ( -1.656854249492358155, 14.68750000000000000, 4.000000000000024869 ) ) ;
#47924=CARTESIAN_POINT ( 'NONE',  ( 2.449293598294707893E-16, 7.250000000000000000, -4.000000000000001776 ) ) ;
#47928=CARTESIAN_POINT ( 'NONE',  ( 2.449293598294707893E-16, 3.250000000000000444, -4.000000000000001776 ) ) ;
#47934=CARTESIAN_POINT ( 'NONE',  ( 4.898587196589415787E-16, 0.000000000000000000, 4.000000000000001776 ) ) ;
#47938=CARTESIAN_POINT ( 'NONE',  ( 1.881053915767122664, 18.24999999863440792, 4.541265875000001451 ) ) ;
#47942=CARTESIAN_POINT ( 'NONE',  ( -4.541265875000002339, 0.8749999986344069169, -1.881053915767121998 ) ) ;
#47951=CARTESIAN_POINT ( 'NONE',  ( 1.656854249492381914, 0.8125000000000004441, 4.000000000000000888 ) ) ;
#47952=CARTESIAN_POINT ( 'NONE',  ( -2.828427124746192067, 13.37499999726881406, 2.828427124746190735 ) ) ;
#47953=CARTESIAN_POINT ( 'NONE',  ( -1.881053915767121776, 3.624999998634406584, -4.541265875000002339 ) ) ;
#47961=CARTESIAN_POINT ( 'NONE',  ( 4.541265875000001451, 13.24999999863441147, 1.881053915767124440 ) ) ;
#47971=DIRECTION ( 'NONE',  ( -0.000000000000000000, -1.000000000000000000, -0.000000000000000000 ) ) ;
#47989=CARTESIAN_POINT ( 'NONE',  ( 1.881053915767121776, 1.499999998634406806, -4.541265875000002339 ) ) ;
#48007=CARTESIAN_POINT ( 'NONE',  ( -4.541265875000003227, 16.99999999863440792, 1.881053915767121110 ) ) ;
#48008=CARTESIAN_POINT ( 'NONE',  ( 4.000000000000000888, 10.93750000000000178, 1.656854249492384135 ) ) ;
#48031=CARTESIAN_POINT ( 'NONE',  ( 2.780723358947928197E-16, 3.687499998634407472, -4.541265875000002339 ) ) ;
#48042=CARTESIAN_POINT ( 'NONE',  ( -4.000000000000001776, 1.249999997268813168, -4.898587196589415787E-16 ) ) ;
#48049=CARTESIAN_POINT ( 'NONE',  ( -8.342170076843785083E-16, 4.062499998634407028, 4.541265875000002339 ) ) ;
#48055=( BOUNDED_CURVE ( )  B_SPLINE_CURVE ( 2, ( #11473, #34507, #46908, #69932, #5818, #28813, #46165, #34876, #57882 ),
 .UNSPECIFIED., .F., .F. ) 
 B_SPLINE_CURVE_WITH_KNOTS ( ( 3, 2, 2, 2, 3 ),
 ( 0.3068181818181818232, 0.3125000000000000000, 0.3181818181818181768, 0.3238636363636363535, 0.3295454545454545303 ),
 .UNSPECIFIED. ) 
 CURVE ( )  GEOMETRIC_REPRESENTATION_ITEM ( )  RATIONAL_B_SPLINE_CURVE ( ( 1.000000000000000000, 0.9238795325112867385, 1.000000000000000000, 0.9238795325112867385, 1.000000000000000000, 0.9238795325112867385, 1.000000000000000000, 0.9238795325112867385, 1.000000000000000000 ) ) 
 REPRESENTATION_ITEM ( '' )  );
#48061=AXIS2_PLACEMENT_3D ( 'NONE', #65762, #14064, #60104 ) ;
#48083=VERTEX_POINT ( 'NONE', #63232 ) ;
#48092=CARTESIAN_POINT ( 'NONE',  ( 1.881053915767121776, 5.624999998634407028, -4.541265875000002339 ) ) ;
#48131=CYLINDRICAL_SURFACE ( 'NONE', #31869, 4.000000000000001776 ) ;
#48138=CARTESIAN_POINT ( 'NONE',  ( -1.881053915767121554, 10.74999999863440969, -4.541265875000002339 ) ) ;
#48144=ADVANCED_FACE ( 'NONE', ( #637 ), #11559, .T. ) ;
#48151=CARTESIAN_POINT ( 'NONE',  ( -4.437079077512471770, 22.00000000000000355, 0.01162584019489742125 ) ) ;
#48153=EDGE_CURVE ( 'NONE', #12049, #11773, #68900, .T. ) ;
#48165=CARTESIAN_POINT ( 'NONE',  ( 0.000000000000000000, 1.806524977843537691E-16, 0.000000000000000000 ) ) ;
#48180=EDGE_CURVE ( 'NONE', #54025, #43761, #33010, .T. ) ;
#48184=CARTESIAN_POINT ( 'NONE',  ( 3.211159895383561835, 14.43749999863440792, -3.211159895383561835 ) ) ;
#48201=CARTESIAN_POINT ( 'NONE',  ( 4.000000000000001776, 13.00000000000000178, 0.000000000000000000 ) ) ;
#48225=AXIS2_PLACEMENT_3D ( 'NONE', #28896, #10802, #62111 ) ;
#48231=CARTESIAN_POINT ( 'NONE',  ( 2.828427124746191623, 16.12500000000000000, -2.828427124746191623 ) ) ;
#48232=CARTESIAN_POINT ( 'NONE',  ( -8.342170076843785083E-16, 15.06249999863440792, 4.541265875000002339 ) ) ;
#48263=CYLINDRICAL_SURFACE ( 'NONE', #5812, 4.000000000000001776 ) ;
#48265=FACE_OUTER_BOUND ( 'NONE', #8259, .T. ) ;
#48312=EDGE_CURVE ( 'NONE', #31018, #28928, #37384, .T. ) ;
#48313=CARTESIAN_POINT ( 'NONE',  ( 1.881053915767122664, 15.24999999863440969, 4.541265875000001451 ) ) ;
#48318=CARTESIAN_POINT ( 'NONE',  ( 3.211159895383560947, 5.312499998634407028, 3.211159895383562723 ) ) ;
#48323=CARTESIAN_POINT ( 'NONE',  ( -4.000000000000001776, 3.500000000000000000, -4.898587196589415787E-16 ) ) ;
#48324=CARTESIAN_POINT ( 'NONE',  ( -1.656854249492381248, 14.06249999726881406, -4.000000000000001776 ) ) ;
#48325=CARTESIAN_POINT ( 'NONE',  ( -4.541265875000002339, 5.812499998634406140, -5.561446717895856393E-16 ) ) ;
#48330=CARTESIAN_POINT ( 'NONE',  ( -3.211159895383561391, 15.68749999863440436, -3.211159895383561835 ) ) ;
#48341=CARTESIAN_POINT ( 'NONE',  ( -7.347880794884122694E-16, 1.750000000000000222, 4.000000000000001776 ) ) ;
#48350=CARTESIAN_POINT ( 'NONE',  ( 2.828427124746190291, 7.875000000000000000, 2.828427124746192067 ) ) ;
#48352=CARTESIAN_POINT ( 'NONE',  ( -4.000000000000001776, 3.187499997268814056, -1.656854249492381470 ) ) ;
#48358=CARTESIAN_POINT ( 'NONE',  ( 3.211159895383560947, 3.187499998634407028, 3.211159895383562723 ) ) ;
#48379=CARTESIAN_POINT ( 'NONE',  ( -4.541265875000002339, 14.87499999863441147, -1.881053915767121998 ) ) ;
#48382=ORIENTED_EDGE ( 'NONE', *, *, #68834, .F. ) ;
#48403=CARTESIAN_POINT ( 'NONE',  ( 1.881053915767121998, 3.624999998634407028, -4.541265875000002339 ) ) ;
#48414=CARTESIAN_POINT ( 'NONE',  ( -4.000000000000001776, 4.187499997268813168, -1.656854249492381470 ) ) ;
#48420=CARTESIAN_POINT ( 'NONE',  ( 1.881053915767121776, 0.4999999986344067504, -4.541265875000002339 ) ) ;
#48456=CARTESIAN_POINT ( 'NONE',  ( 2.449293598294707893E-16, 18.25000000000000000, -4.000000000000001776 ) ) ;
#48463=CARTESIAN_POINT ( 'NONE',  ( -3.211159895383562723, 5.062499998634407028, 3.211159895383561391 ) ) ;
#48474=ORIENTED_EDGE ( 'NONE', *, *, #28295, .T. ) ;
#48488=CARTESIAN_POINT ( 'NONE',  ( -1.656854249492381248, 9.312500000000000000, -4.000000000000001776 ) ) ;
#48509=CARTESIAN_POINT ( 'NONE',  ( -4.541265875000002339, 12.87499999863440969, -1.881053915767121998 ) ) ;
#48550=CARTESIAN_POINT ( 'NONE',  ( 1.881053915767121776, 14.49999999863440969, -4.541265875000002339 ) ) ;
#48570=FACE_OUTER_BOUND ( 'NONE', #7841, .T. ) ;
#48578=VERTEX_POINT ( 'NONE', #39031 ) ;
#48580=CARTESIAN_POINT ( 'NONE',  ( 0.000000000000000000, 0.000000000000000000, 0.000000000000000000 ) ) ;
#48603=CARTESIAN_POINT ( 'NONE',  ( -4.000000000000001776, 14.43750000000000000, -1.656854249492381470 ) ) ;
#48604=CARTESIAN_POINT ( 'NONE',  ( -4.541265875000003227, 15.87499999863440436, 1.881053915767121110 ) ) ;
#48627=CARTESIAN_POINT ( 'NONE',  ( 2.449293598294707893E-16, 13.25000000000000000, -4.000000000000001776 ) ) ;
#48632=CARTESIAN_POINT ( 'NONE',  ( 2.828427124746191623, 5.874999997268813168, -2.828427124746191623 ) ) ;
#48635=CARTESIAN_POINT ( 'NONE',  ( -4.000000000000002665, 16.56250000000000000, 1.656854249492380582 ) ) ;
#48683=CARTESIAN_POINT ( 'NONE',  ( 1.881053915767121998, 19.62499999863441147, -4.541265875000002339 ) ) ;
#48687=CARTESIAN_POINT ( 'NONE',  ( 2.780723358947928197E-16, 3.687499998634407472, -4.541265875000002339 ) ) ;
#48694=CARTESIAN_POINT ( 'NONE',  ( 1.656854249492381914, 3.812500000000000000, 4.000000000000000888 ) ) ;
#48695=CARTESIAN_POINT ( 'NONE',  ( 2.449293598294707893E-16, 18.99999999726881228, -4.000000000000001776 ) ) ;
#48696=CARTESIAN_POINT ( 'NONE',  ( 4.541265875000002339, 3.374999998634407028, -1.881053915767121776 ) ) ;
#48701=CARTESIAN_POINT ( 'NONE',  ( -3.211159895383561391, 17.68749999863440792, -3.211159895383561835 ) ) ;
#48722=CARTESIAN_POINT ( 'NONE',  ( -4.000000000000002665, 5.562500000000000000, 1.656854249492380582 ) ) ;
#48732=CARTESIAN_POINT ( 'NONE',  ( 3.211159895383560947, 8.187499998634406140, 3.211159895383562723 ) ) ;
#48749=CARTESIAN_POINT ( 'NONE',  ( 3.211159895383560947, 22.31249999863440792, 3.211159895383562723 ) ) ;
#48766=CIRCLE ( 'NONE', #17433, 4.000000000000000000 ) ;
#48775=CARTESIAN_POINT ( 'NONE',  ( -3.211159895383562723, 9.062499998634407916, 3.211159895383561391 ) ) ;
#48785=CARTESIAN_POINT ( 'NONE',  ( -4.000000000000001776, 8.249999997268814056, -4.898587196589415787E-16 ) ) ;
#48791=CARTESIAN_POINT ( 'NONE',  ( -4.541265875000002339, 4.749999998634407028, -1.881053915767121998 ) ) ;
#48836=CARTESIAN_POINT ( 'NONE',  ( 3.211159895383561835, 5.562499998634407028, -3.211159895383561835 ) ) ;
#48855=ORIENTED_EDGE ( 'NONE', *, *, #25648, .F. ) ;
#48880=CARTESIAN_POINT ( 'NONE',  ( 2.780723358947928197E-16, 11.68749999863440614, -4.541265875000002339 ) ) ;
#48895=CARTESIAN_POINT ( 'NONE',  ( -1.656854249492358155, 15.43749999726881406, 4.000000000000024869 ) ) ;
#48906=CARTESIAN_POINT ( 'NONE',  ( 0.000000000000000000, 0.000000000000000000, 0.000000000000000000 ) ) ;
#48922=CARTESIAN_POINT ( 'NONE',  ( -3.211159895383561391, 15.68749999863440436, -3.211159895383561835 ) ) ;
#48931=CARTESIAN_POINT ( 'NONE',  ( 0.000000000000000000, 0.000000000000000000, -4.000000000000001776 ) ) ;
#48955=CARTESIAN_POINT ( 'NONE',  ( 2.449293598294707893E-16, 16.99999999726881583, -4.000000000000001776 ) ) ;
#48970=CARTESIAN_POINT ( 'NONE',  ( 1.656854249492381248, 14.18750000000000000, -4.000000000000001776 ) ) ;
#48971=CARTESIAN_POINT ( 'NONE',  ( 4.541265875000002339, 16.37499999863440436, -1.881053915767121776 ) ) ;
#49009=CARTESIAN_POINT ( 'NONE',  ( -4.000000000000001776, 16.50000000000000000, -4.898587196589415787E-16 ) ) ;
#49042=CARTESIAN_POINT ( 'NONE',  ( 4.000000000000000888, 21.93750000000000355, 1.656854249492384135 ) ) ;
#49055=CARTESIAN_POINT ( 'NONE',  ( -3.211159895383562723, 20.06249999863440436, 3.211159895383561391 ) ) ;
#49058=CARTESIAN_POINT ( 'NONE',  ( 1.881053915767121776, 4.624999998634407028, -4.541265875000002339 ) ) ;
#49064=CARTESIAN_POINT ( 'NONE',  ( 4.000000000000001776, 3.000000000000000000, 0.000000000000000000 ) ) ;
#49065=CARTESIAN_POINT ( 'NONE',  ( -4.000000000000001776, 20.18749999726881228, -1.656854249492381470 ) ) ;
#49066=CARTESIAN_POINT ( 'NONE',  ( 1.881053915767122664, 3.124999998634406584, 4.541265875000001451 ) ) ;
#49074=CARTESIAN_POINT ( 'NONE',  ( -3.211159895383562723, 17.93749999863440792, 3.211159895383561391 ) ) ;
#49095=CARTESIAN_POINT ( 'NONE',  ( -1.656854249492381248, 5.312500000000000888, -4.000000000000001776 ) ) ;
#49105=CARTESIAN_POINT ( 'NONE',  ( -8.342170076843785083E-16, 7.062499998634407028, 4.541265875000002339 ) ) ;
#49123=CARTESIAN_POINT ( 'NONE',  ( 4.541265875000001451, 21.37499999863441147, 1.881053915767124440 ) ) ;
#49146=CARTESIAN_POINT ( 'NONE',  ( -8.342170076843785083E-16, 10.18749999863440614, 4.541265875000002339 ) ) ;
#49161=CARTESIAN_POINT ( 'NONE',  ( -1.656854249492381248, 7.062499997268812280, -4.000000000000001776 ) ) ;
#49165=CARTESIAN_POINT ( 'NONE',  ( -4.541265875000002339, 5.749999998634407028, -1.881053915767121998 ) ) ;
#49201=AXIS2_PLACEMENT_3D ( 'NONE', #62560, #68977, #33925 ) ;
#49211=CARTESIAN_POINT ( 'NONE',  ( -4.541265875000002339, 6.937499998634407916, -5.561446717895856393E-16 ) ) ;
#49216=ORIENTED_EDGE ( 'NONE', *, *, #6730, .F. ) ;
#49222=LINE ( 'NONE', #70755, #23511 ) ;
#49254=CARTESIAN_POINT ( 'NONE',  ( 4.541265875000002339, 15.43749999863440614, 0.000000000000000000 ) ) ;
#49276=CARTESIAN_POINT ( 'NONE',  ( -7.347880794884122694E-16, 2.499999997268813168, 4.000000000000001776 ) ) ;
#49299=CARTESIAN_POINT ( 'NONE',  ( 4.541265875000001451, 17.24999999863440792, 1.881053915767124440 ) ) ;
#49320=CARTESIAN_POINT ( 'NONE',  ( -7.347880794884122694E-16, 14.75000000000000178, 4.000000000000001776 ) ) ;
#49350=CARTESIAN_POINT ( 'NONE',  ( -2.828427124746192067, 15.62500000000000000, 2.828427124746190735 ) ) ;
#49351=CARTESIAN_POINT ( 'NONE',  ( -4.541265875000002339, 20.74999999863440436, -1.881053915767121998 ) ) ;
#49393=CARTESIAN_POINT ( 'NONE',  ( 2.828427124746191623, 17.12500000000000000, -2.828427124746191623 ) ) ;
#49396=CARTESIAN_POINT ( 'NONE',  ( -2.828427124746190735, 8.124999997268814056, -2.828427124746191623 ) ) ;
#49425=EDGE_CURVE ( 'NONE', #48083, #25046, #37617, .T. ) ;
#49435=CARTESIAN_POINT ( 'NONE',  ( 4.541265875000002339, 21.43749999863440792, 0.000000000000000000 ) ) ;
#49438=CARTESIAN_POINT ( 'NONE',  ( -3.211159895383562723, 4.062499998634407028, 3.211159895383561391 ) ) ;
#49446=CARTESIAN_POINT ( 'NONE',  ( 4.000000000000000888, 4.937500000000001776, 1.656854249492384135 ) ) ;
#49447=CARTESIAN_POINT ( 'NONE',  ( -4.000000000000001776, 17.24999999726881583, -4.898587196589415787E-16 ) ) ;
#49448=CARTESIAN_POINT ( 'NONE',  ( -1.881053915767124440, 3.999999998634406584, 4.541265875000001451 ) ) ;
#49454=CARTESIAN_POINT ( 'NONE',  ( -4.541265875000002339, 17.74999999863440792, -1.881053915767121998 ) ) ;
#49485=CARTESIAN_POINT ( 'NONE',  ( -8.342170076843785083E-16, 5.062499998634407028, 4.541265875000002339 ) ) ;
#49499=DIRECTION ( 'NONE',  ( -0.000000000000000000, -1.000000000000000000, -0.000000000000000000 ) ) ;
#49504=CARTESIAN_POINT ( 'NONE',  ( 4.541265875000002339, 18.49999999863440436, -1.881053915767121554 ) ) ;
#49527=CARTESIAN_POINT ( 'NONE',  ( 3.211159895383561835, 9.562499998634406140, -3.211159895383561835 ) ) ;
#49540=CARTESIAN_POINT ( 'NONE',  ( 4.000000000000001776, 7.812499997268813168, -1.656854249492381248 ) ) ;
#49547=CARTESIAN_POINT ( 'NONE',  ( 4.541265875000002339, 7.374999998634408804, -1.881053915767121554 ) ) ;
#49549=CARTESIAN_POINT ( 'NONE',  ( -2.828427124746192067, 13.62500000000000000, 2.828427124746190735 ) ) ;
#49558=AXIS2_PLACEMENT_3D ( 'NONE', #13360, #37136, #24327 ) ;
#49592=CARTESIAN_POINT ( 'NONE',  ( -1.881053915767124440, 7.124999998634407916, 4.541265875000001451 ) ) ;
#49596=CARTESIAN_POINT ( 'NONE',  ( 2.828427124746190291, 0.8750000000000002220, 2.828427124746192067 ) ) ;
#49598=( BOUNDED_CURVE ( )  B_SPLINE_CURVE ( 2, ( #66316, #74214, #45539, #27074, #16484 ),
 .UNSPECIFIED., .F., .F. ) 
 B_SPLINE_CURVE_WITH_KNOTS ( ( 3, 2, 3 ),
 ( 0.000000000000000000, 0.005681818181818181976, 0.01136363636363636395 ),
 .UNSPECIFIED. ) 
 CURVE ( )  GEOMETRIC_REPRESENTATION_ITEM ( )  RATIONAL_B_SPLINE_CURVE ( ( 1.000000000000000000, 0.9238795325112867385, 1.000000000000000000, 0.9238795325112867385, 1.000000000000000000 ) ) 
 REPRESENTATION_ITEM ( '' )  );
#49639=CARTESIAN_POINT ( 'NONE',  ( -4.541265875000002339, 14.93749999863440792, -5.561446717895856393E-16 ) ) ;
#49644=AXIS2_PLACEMENT_3D ( 'NONE', #60498, #37122, #20496 ) ;
#49649=CARTESIAN_POINT ( 'NONE',  ( 7.071067811865482611, 22.99999999999999645, 1.000000000000000000 ) ) ;
#49685=CARTESIAN_POINT ( 'NONE',  ( 4.541265875000001451, 19.24999999863440436, 1.881053915767124440 ) ) ;
#49693=DIRECTION ( 'NONE',  ( 0.000000000000000000, 0.000000000000000000, -1.000000000000000000 ) ) ;
#49717=CARTESIAN_POINT ( 'NONE',  ( 2.828427124746190291, 3.624999997268813168, 2.828427124746192067 ) ) ;
#49718=CARTESIAN_POINT ( 'NONE',  ( -1.656854249492383468, 11.43749999726881406, 4.000000000000000888 ) ) ;
#49735=CARTESIAN_POINT ( 'NONE',  ( -4.000000000000002665, 17.56250000000000355, 1.656854249492380804 ) ) ;
#49736=CARTESIAN_POINT ( 'NONE',  ( 4.541265875000001451, 20.24999999863440436, 1.881053915767124440 ) ) ;
#49767=FACE_OUTER_BOUND ( 'NONE', #73762, .T. ) ;
#49772=ADVANCED_FACE ( 'NONE', ( #67062 ), #4072, .T. ) ;
#49813=CARTESIAN_POINT ( 'NONE',  ( -3.211159895383562723, 21.06249999863440792, 3.211159895383561391 ) ) ;
#49816=CARTESIAN_POINT ( 'NONE',  ( 2.780723358947928197E-16, 5.687499998634407028, -4.541265875000002339 ) ) ;
#49822=( BOUNDED_CURVE ( )  B_SPLINE_CURVE ( 2, ( #51414, #33342, #15586, #39725, #62354, #38626, #4289, #27657, #44276 ),
 .UNSPECIFIED., .F., .F. ) 
 B_SPLINE_CURVE_WITH_KNOTS ( ( 3, 2, 2, 2, 3 ),
 ( 0.8295454545454545858, 0.8352272727272727071, 0.8409090909090909394, 0.8465909090909090606, 0.8522727272727272929 ),
 .UNSPECIFIED. ) 
 CURVE ( )  GEOMETRIC_REPRESENTATION_ITEM ( )  RATIONAL_B_SPLINE_CURVE ( ( 1.000000000000000000, 0.9238795325112867385, 1.000000000000000000, 0.9238795325112867385, 1.000000000000000000, 0.9238795325112867385, 1.000000000000000000, 0.9238795325112867385, 1.000000000000000000 ) ) 
 REPRESENTATION_ITEM ( '' )  );
#49823=CARTESIAN_POINT ( 'NONE',  ( 2.449293598294707893E-16, 4.250000000000000000, -4.000000000000001776 ) ) ;
#49824=CARTESIAN_POINT ( 'NONE',  ( -4.000000000000002665, 17.31249999726881938, 1.656854249492380804 ) ) ;
#49825=CARTESIAN_POINT ( 'NONE',  ( -3.211159895383561391, 7.687499998634407028, -3.211159895383561835 ) ) ;
#49831=CARTESIAN_POINT ( 'NONE',  ( 1.881053915767122664, 17.12499999863440436, 4.541265875000001451 ) ) ;
#49841=CARTESIAN_POINT ( 'NONE',  ( -4.000000000000001776, 21.18749999726881583, -1.656854249492381470 ) ) ;
#49863=CARTESIAN_POINT ( 'NONE',  ( -4.541265875000003227, 5.874999998634406140, 1.881053915767121110 ) ) ;
#49881=CARTESIAN_POINT ( 'NONE',  ( 3.211159895383561835, 18.56249999863440436, -3.211159895383561835 ) ) ;
#49887=CARTESIAN_POINT ( 'NONE',  ( -7.347880794884122694E-16, 12.49999999726881406, 4.000000000000001776 ) ) ;
#49904=CARTESIAN_POINT ( 'NONE',  ( -3.211159895383561391, 8.812499998634407916, -3.211159895383561835 ) ) ;
#49914=CARTESIAN_POINT ( 'NONE',  ( -4.000000000000002665, 5.312499997268813168, 1.656854249492380804 ) ) ;
#49915=CARTESIAN_POINT ( 'NONE',  ( 1.656854249492381248, 18.18750000000000000, -4.000000000000001776 ) ) ;
#49917=EDGE_CURVE ( 'NONE', #10305, #13303, #16212, .T. ) ;
#49921=CARTESIAN_POINT ( 'NONE',  ( -1.881053915767121554, 4.624999998634407028, -4.541265875000002339 ) ) ;
#49926=VERTEX_POINT ( 'NONE', #62878 ) ;
#49966=CARTESIAN_POINT ( 'NONE',  ( 4.541265875000002339, 6.437499998634407028, 0.000000000000000000 ) ) ;
#50006=CARTESIAN_POINT ( 'NONE',  ( -4.541265875000002339, 17.87499999863441147, -1.881053915767121998 ) ) ;
#50043=ORIENTED_EDGE ( 'NONE', *, *, #7136, .T. ) ;
#50044=CARTESIAN_POINT ( 'NONE',  ( -7.347880794884122694E-16, 1.750000000000000222, 4.000000000000001776 ) ) ;
#50051=CARTESIAN_POINT ( 'NONE',  ( 3.211159895383561835, 19.43749999863440436, -3.211159895383561835 ) ) ;
#50082=EDGE_CURVE ( 'NONE', #46255, #66256, #70232, .T. ) ;
#50086=CARTESIAN_POINT ( 'NONE',  ( -2.828427124746192067, 1.374999997268813168, 2.828427124746190735 ) ) ;
#50106=CARTESIAN_POINT ( 'NONE',  ( 1.656854249492381248, 21.18750000000000000, -4.000000000000001776 ) ) ;
#50107=CARTESIAN_POINT ( 'NONE',  ( -1.881053915767124440, 20.99999999863440792, 4.541265875000001451 ) ) ;
#50183=CARTESIAN_POINT ( 'NONE',  ( -4.541265875000003227, 20.99999999863440792, 1.881053915767121110 ) ) ;
#50186=CARTESIAN_POINT ( 'NONE',  ( 4.541265875000002339, 8.499999998634406140, -1.881053915767121554 ) ) ;
#50194=CARTESIAN_POINT ( 'NONE',  ( 2.449293598294707893E-16, 6.250000000000000000, -4.000000000000001776 ) ) ;
#50195=CARTESIAN_POINT ( 'NONE',  ( 1.656854249492381248, 18.93749999726881228, -4.000000000000001776 ) ) ;
#50196=CARTESIAN_POINT ( 'NONE',  ( -4.541265875000002339, 6.749999998634407916, -1.881053915767121998 ) ) ;
#50198=ORIENTED_EDGE ( 'NONE', *, *, #35471, .F. ) ;
#50202=CARTESIAN_POINT ( 'NONE',  ( 1.881053915767121776, 17.49999999863440436, -4.541265875000002339 ) ) ;
#50232=CARTESIAN_POINT ( 'NONE',  ( 4.541265875000001451, 6.249999998634407916, 1.881053915767124440 ) ) ;
#50236=ORIENTED_EDGE ( 'NONE', *, *, #35471, .T. ) ;
#50249=CARTESIAN_POINT ( 'NONE',  ( -1.881053915767121554, 19.74999999863440792, -4.541265875000002339 ) ) ;
#50260=ORIENTED_EDGE ( 'NONE', *, *, #21519, .T. ) ;
#50272=CARTESIAN_POINT ( 'NONE',  ( -1.881053915767124440, 10.12499999863440792, 4.541265875000001451 ) ) ;
#50283=CARTESIAN_POINT ( 'NONE',  ( 4.000000000000001776, 5.749999997268813168, 0.000000000000000000 ) ) ;
#50289=CARTESIAN_POINT ( 'NONE',  ( 4.000000000000000888, 12.68749999726881406, 1.656854249492384135 ) ) ;
#50291=CARTESIAN_POINT ( 'NONE',  ( 4.541265875000002339, 5.312499998634407028, 0.000000000000000000 ) ) ;
#50320=CYLINDRICAL_SURFACE ( 'NONE', #33145, 4.000000000000001776 ) ;
#50331=CARTESIAN_POINT ( 'NONE',  ( -3.211159895383562723, 8.062499998634406140, 3.211159895383561391 ) ) ;
#50335=ORIENTED_EDGE ( 'NONE', *, *, #20794, .T. ) ;
#50376=CARTESIAN_POINT ( 'NONE',  ( 3.211159895383560947, 14.31249999863440792, 3.211159895383562723 ) ) ;
#50383=( BOUNDED_CURVE ( )  B_SPLINE_CURVE ( 2, ( #3036, #26019, #14708, #49042, #72049 ),
 .UNSPECIFIED., .F., .F. ) 
 B_SPLINE_CURVE_WITH_KNOTS ( ( 3, 2, 3 ),
 ( 0.9886363636363636465, 0.9943181818181817677, 1.000000000000000000 ),
 .UNSPECIFIED. ) 
 CURVE ( )  GEOMETRIC_REPRESENTATION_ITEM ( )  RATIONAL_B_SPLINE_CURVE ( ( 1.000000000000000000, 0.9238795325112867385, 1.000000000000000000, 0.9238795325112867385, 1.000000000000000000 ) ) 
 REPRESENTATION_ITEM ( '' )  );
#50404=CARTESIAN_POINT ( 'NONE',  ( -3.614602657737266966, 22.00000000000000000, 2.764888201658305178 ) ) ;
#50421=CARTESIAN_POINT ( 'NONE',  ( 1.881053915767121776, 17.49999999863440436, -4.541265875000002339 ) ) ;
#50424=LINE ( 'NONE', #38754, #55216 ) ;
#50459=EDGE_CURVE ( 'NONE', #61992, #22328, #54360, .T. ) ;
#50471=CARTESIAN_POINT ( 'NONE',  ( 4.000000000000000888, 21.93750000000000355, 1.656854249492384135 ) ) ;
#50472=CARTESIAN_POINT ( 'NONE',  ( 3.211159895383561835, 19.43749999863440436, -3.211159895383561835 ) ) ;
#50556=CARTESIAN_POINT ( 'NONE',  ( 4.541265875000002339, 9.499999998634406140, -1.881053915767121554 ) ) ;
#50563=CARTESIAN_POINT ( 'NONE',  ( 1.656854249492381248, 9.187500000000000000, -4.000000000000001776 ) ) ;
#50564=CARTESIAN_POINT ( 'NONE',  ( 4.541265875000002339, 8.374999998634407916, -1.881053915767121776 ) ) ;
#50571=CARTESIAN_POINT ( 'NONE',  ( 3.211159895383561835, 21.43749999863440792, -3.211159895383561835 ) ) ;
#50585=( BOUNDED_CURVE ( )  B_SPLINE_CURVE ( 2, ( #14749, #73597, #37790, #49841, #60786, #26439, #72484, #43811, #66826 ),
 .UNSPECIFIED., .F., .F. ) 
 B_SPLINE_CURVE_WITH_KNOTS ( ( 3, 2, 2, 2, 3 ),
 ( 0.9204545454545455252, 0.9261363636363637575, 0.9318181818181817677, 0.9375000000000000000, 0.9431818181818182323 ),
 .UNSPECIFIED. ) 
 CURVE ( )  GEOMETRIC_REPRESENTATION_ITEM ( )  RATIONAL_B_SPLINE_CURVE ( ( 0.9999999999999985567, 0.9238795325112881818, 1.000000000000000000, 0.9238795325112867385, 1.000000000000000000, 0.9238795325112867385, 1.000000000000000000, 0.9238795325112867385, 1.000000000000000000 ) ) 
 REPRESENTATION_ITEM ( '' )  );
#50603=CARTESIAN_POINT ( 'NONE',  ( -7.347880794884122694E-16, 11.49999999726881406, 4.000000000000001776 ) ) ;
#50641=CARTESIAN_POINT ( 'NONE',  ( -3.211159895383561391, 11.81249999863440614, -3.211159895383561835 ) ) ;
#50642=ORIENTED_EDGE ( 'NONE', *, *, #8548, .T. ) ;
#50650=CARTESIAN_POINT ( 'NONE',  ( -7.347880794884122694E-16, 9.499999997268814056, 4.000000000000001776 ) ) ;
#50658=CARTESIAN_POINT ( 'NONE',  ( -4.541265875000002339, 8.812499998634407916, -5.561446717895856393E-16 ) ) ;
#50661=ORIENTED_EDGE ( 'NONE', *, *, #643, .T. ) ;
#50690=ORIENTED_EDGE ( 'NONE', *, *, #989, .F. ) ;
#50701=CARTESIAN_POINT ( 'NONE',  ( -1.881053915767121554, 9.749999998634406140, -4.541265875000002339 ) ) ;
#50717=CARTESIAN_POINT ( 'NONE',  ( -7.347880794884122694E-16, 7.499999997268813168, 4.000000000000001776 ) ) ;
#50737=CARTESIAN_POINT ( 'NONE',  ( -1.656854249492381248, 7.312500000000000000, -4.000000000000001776 ) ) ;
#50746=CARTESIAN_POINT ( 'NONE',  ( 4.000000000000001776, 3.000000000000000000, 0.000000000000000000 ) ) ;
#50747=CARTESIAN_POINT ( 'NONE',  ( 3.211159895383561835, 17.56249999863440792, -3.211159895383561835 ) ) ;
#50748=ORIENTED_EDGE ( 'NONE', *, *, #15763, .T. ) ;
#50786=EDGE_CURVE ( 'NONE', #52055, #51031, #63441, .T. ) ;
#50787=CARTESIAN_POINT ( 'NONE',  ( 1.656854249492381248, 2.187500000000000444, -4.000000000000001776 ) ) ;
#50793=CARTESIAN_POINT ( 'NONE',  ( 2.780723358947928197E-16, 18.56249999863440436, -4.541265875000002339 ) ) ;
#50796=CARTESIAN_POINT ( 'NONE',  ( -1.656854249492382580, 1.312500000000000444, -4.000000000000000000 ) ) ;
#50803=( BOUNDED_CURVE ( )  B_SPLINE_CURVE ( 2, ( #19606, #19238, #49396, #15062, #42248, #43360, #13566, #36604, #31304 ),
 .UNSPECIFIED., .F., .F. ) 
 B_SPLINE_CURVE_WITH_KNOTS ( ( 3, 2, 2, 2, 3 ),
 ( 0.3295454545454545303, 0.3352272727272727071, 0.3409090909090909394, 0.3465909090909091717, 0.3522727272727273484 ),
 .UNSPECIFIED. ) 
 CURVE ( )  GEOMETRIC_REPRESENTATION_ITEM ( )  RATIONAL_B_SPLINE_CURVE ( ( 1.000000000000000000, 0.9238795325112867385, 1.000000000000000000, 0.9238795325112867385, 1.000000000000000000, 0.9238795325112867385, 1.000000000000000000, 0.9238795325112859613, 1.000000000000000666 ) ) 
 REPRESENTATION_ITEM ( '' )  );
#50846=CARTESIAN_POINT ( 'NONE',  ( -4.000000000000001776, 19.43750000000000000, -1.656854249492381470 ) ) ;
#50847=CARTESIAN_POINT ( 'NONE',  ( 3.211159895383561835, 20.43749999863440436, -3.211159895383561835 ) ) ;
#50883=CARTESIAN_POINT ( 'NONE',  ( 1.656854249492381914, 17.56249999726881938, 4.000000000000000888 ) ) ;
#50927=DIRECTION ( 'NONE',  ( 0.000000000000000000, 0.000000000000000000, -1.000000000000000000 ) ) ;
#50933=CARTESIAN_POINT ( 'NONE',  ( -1.881053915767121554, 8.749999998634406140, -4.541265875000002339 ) ) ;
#50937=CARTESIAN_POINT ( 'NONE',  ( 2.828427124746190291, 7.875000000000000000, 2.828427124746192067 ) ) ;
#50939=CARTESIAN_POINT ( 'NONE',  ( 2.828427124746191623, 21.87499999726881583, -2.828427124746191623 ) ) ;
#50940=CARTESIAN_POINT ( 'NONE',  ( -3.211159895383561391, 6.687499998634407028, -3.211159895383561835 ) ) ;
#50963=DIRECTION ( 'NONE',  ( 0.000000000000000000, 0.000000000000000000, -1.000000000000000000 ) ) ;
#50964=EDGE_CURVE ( 'NONE', #9987, #59197, #72665, .T. ) ;
#50968=CARTESIAN_POINT ( 'NONE',  ( -7.347880794884122694E-16, 4.750000000000000000, 4.000000000000001776 ) ) ;
#50981=CARTESIAN_POINT ( 'NONE',  ( 4.000000000000001776, 11.74999999726881406, 0.000000000000000000 ) ) ;
#51013=DIRECTION ( 'NONE',  ( -0.000000000000000000, -1.000000000000000000, -0.000000000000000000 ) ) ;
#51019=CARTESIAN_POINT ( 'NONE',  ( -1.881053915767124440, 13.12499999863440969, 4.541265875000001451 ) ) ;
#51028=FACE_OUTER_BOUND ( 'NONE', #8134, .T. ) ;
#51029=CARTESIAN_POINT ( 'NONE',  ( 2.449293598294707893E-16, 9.999999997268814056, -4.000000000000001776 ) ) ;
#51031=VERTEX_POINT ( 'NONE', #70591 ) ;
#51038=CARTESIAN_POINT ( 'NONE',  ( 1.881053915767122664, 9.124999998634407916, 4.541265875000001451 ) ) ;
#51039=CARTESIAN_POINT ( 'NONE',  ( -1.656854249492381248, 10.06249999726881406, -4.000000000000001776 ) ) ;
#51043=EDGE_CURVE ( 'NONE', #5243, #49926, #1931, .T. ) ;
#51079=CARTESIAN_POINT ( 'NONE',  ( 3.211159895383561835, 11.56249999863440614, -3.211159895383561835 ) ) ;
#51122=CARTESIAN_POINT ( 'NONE',  ( 3.211159895383560947, 20.31249999863440436, 3.211159895383562723 ) ) ;
#51167=CARTESIAN_POINT ( 'NONE',  ( -1.881053915767121554, 1.749999998634407250, -4.541265875000002339 ) ) ;
#51177=VECTOR ( 'NONE', #11445, 1000.000000000000000 ) ;
#51193=CARTESIAN_POINT ( 'NONE',  ( 4.000000000000000888, 5.937500000000000000, 1.656854249492384135 ) ) ;
#51201=CARTESIAN_POINT ( 'NONE',  ( -2.828427124746190735, 2.375000000000000000, -2.828427124746191623 ) ) ;
#51223=CARTESIAN_POINT ( 'NONE',  ( 2.828427124746191623, 19.12500000000000000, -2.828427124746191623 ) ) ;
#51225=CARTESIAN_POINT ( 'NONE',  ( 1.656854249492381248, 4.937499997268813168, -4.000000000000001776 ) ) ;
#51247=AXIS2_PLACEMENT_3D ( 'NONE', #69015, #73551, #4907 ) ;
#51289=CARTESIAN_POINT ( 'NONE',  ( 2.828427124746191623, 18.87499999726881228, -2.828427124746191623 ) ) ;
#51296=( BOUNDED_CURVE ( )  B_SPLINE_CURVE ( 2, ( #61783, #27435, #39883, #10101, #73099, #45537, #50086, #4078, #68186 ),
 .UNSPECIFIED., .F., .F. ) 
 B_SPLINE_CURVE_WITH_KNOTS ( ( 3, 2, 2, 2, 3 ),
 ( 0.01136363636363636395, 0.01704545454545454419, 0.02272727272727272790, 0.02840909090909090814, 0.03409090909090908839 ),
 .UNSPECIFIED. ) 
 CURVE ( )  GEOMETRIC_REPRESENTATION_ITEM ( )  RATIONAL_B_SPLINE_CURVE ( ( 1.000000000000000000, 0.9238795325112867385, 1.000000000000000000, 0.9238795325112867385, 1.000000000000000000, 0.9238795325112867385, 1.000000000000000000, 0.9238795325112867385, 1.000000000000000000 ) ) 
 REPRESENTATION_ITEM ( '' )  );
#51301=CARTESIAN_POINT ( 'NONE',  ( 4.541265875000001451, 8.374999998634406140, 1.881053915767124440 ) ) ;
#51309=CARTESIAN_POINT ( 'NONE',  ( -2.828427124746192067, 6.625000000000000000, 2.828427124746190735 ) ) ;
#51310=CARTESIAN_POINT ( 'NONE',  ( -4.000000000000001776, 22.18749999726881583, -1.656854249492381470 ) ) ;
#51311=CARTESIAN_POINT ( 'NONE',  ( 4.541265875000002339, 7.374999998634407916, -1.881053915767121776 ) ) ;
#51320=CARTESIAN_POINT ( 'NONE',  ( -4.541265875000003227, 20.87499999863441147, 1.881053915767121110 ) ) ;
#51388=CARTESIAN_POINT ( 'NONE',  ( -1.881053915767124440, 11.12499999863440969, 4.541265875000001451 ) ) ;
#51398=CARTESIAN_POINT ( 'NONE',  ( -1.656854249492381248, 11.06249999726881406, -4.000000000000001776 ) ) ;
#51406=CARTESIAN_POINT ( 'NONE',  ( -1.881053915767121554, 8.624999998634406140, -4.541265875000002339 ) ) ;
#51407=CARTESIAN_POINT ( 'NONE',  ( 4.000000000000001776, 16.00000000000000000, 0.000000000000000000 ) ) ;
#51414=CARTESIAN_POINT ( 'NONE',  ( 2.449293598294707893E-16, 18.25000000000000000, -4.000000000000001776 ) ) ;
#51420=ORIENTED_EDGE ( 'NONE', *, *, #38391, .T. ) ;
#51434=DIRECTION ( 'NONE',  ( 0.000000000000000000, 0.000000000000000000, -1.000000000000000000 ) ) ;
#51448=CARTESIAN_POINT ( 'NONE',  ( 3.211159895383560947, 14.31249999863440792, 3.211159895383562723 ) ) ;
#51480=CARTESIAN_POINT ( 'NONE',  ( -3.211159895383561391, 0.8124999986344069169, -3.211159895383561835 ) ) ;
#51492=CARTESIAN_POINT ( 'NONE',  ( -4.000000000000001776, 15.43749999999999822, -1.656854249492381470 ) ) ;
#51493=CARTESIAN_POINT ( 'NONE',  ( -1.881053915767124440, 18.12499999863440792, 4.541265875000001451 ) ) ;
#51536=CARTESIAN_POINT ( 'NONE',  ( -4.541265875000002339, 1.937499998634406806, -5.561446717895856393E-16 ) ) ;
#51543=CARTESIAN_POINT ( 'NONE',  ( -4.000000000000001776, 19.18749999726881228, -1.656854249492381470 ) ) ;
#51593=CARTESIAN_POINT ( 'NONE',  ( 2.828427124746191623, 20.12500000000000000, -2.828427124746191623 ) ) ;
#51595=CARTESIAN_POINT ( 'NONE',  ( -2.572420464602065859, 21.96751355773091774, 3.849899326165059144 ) ) ;
#51605=PRODUCT_CONTEXT ( 'NONE', #18274, 'mechanical' ) ;
#51611=ORIENTED_EDGE ( 'NONE', *, *, #46092, .T. ) ;
#51621=CYLINDRICAL_SURFACE ( 'NONE', #49201, 4.000000000000001776 ) ;
#51634=CARTESIAN_POINT ( 'NONE',  ( 1.881053915767122664, 11.12499999863440792, 4.541265875000001451 ) ) ;
#51671=DIRECTION ( 'NONE',  ( 0.000000000000000000, 0.000000000000000000, 1.000000000000000000 ) ) ;
#51675=CARTESIAN_POINT ( 'NONE',  ( -1.881053915767124440, 9.124999998634407916, 4.541265875000001451 ) ) ;
#51680=CARTESIAN_POINT ( 'NONE',  ( 2.449293598294707893E-16, 8.250000000000000000, -4.000000000000001776 ) ) ;
#51681=CARTESIAN_POINT ( 'NONE',  ( -7.347880794884122694E-16, 20.49999999726881583, 4.000000000000001776 ) ) ;
#51682=CARTESIAN_POINT ( 'NONE',  ( -4.541265875000002339, 13.81249999863440614, -5.561446717895856393E-16 ) ) ;
#51689=CARTESIAN_POINT ( 'NONE',  ( -7.347880794884122694E-16, 10.49999999726881406, 4.000000000000001776 ) ) ;
#51691=CARTESIAN_POINT ( 'NONE',  ( -8.342170076843785083E-16, 22.06249999863440792, 4.541265875000002339 ) ) ;
#51695=ORIENTED_EDGE ( 'NONE', *, *, #15669, .F. ) ;
#51746=CARTESIAN_POINT ( 'NONE',  ( -2.828427124746192067, 20.37499999726881228, 2.828427124746190735 ) ) ;
#51763=CARTESIAN_POINT ( 'NONE',  ( -8.342170076843785083E-16, 14.18749999863440792, 4.541265875000002339 ) ) ;
#51774=CARTESIAN_POINT ( 'NONE',  ( 4.000000000000001776, 8.749999997268814056, 0.000000000000000000 ) ) ;
#51781=CARTESIAN_POINT ( 'NONE',  ( -4.541265875000003227, 11.87499999863440969, 1.881053915767121110 ) ) ;
#51783=CARTESIAN_POINT ( 'NONE',  ( 2.449293598294707893E-16, 9.999999997268814056, -4.000000000000001776 ) ) ;
#51828=CARTESIAN_POINT ( 'NONE',  ( -4.541265875000002339, 11.87499999863440969, -1.881053915767121998 ) ) ;
#51839=CARTESIAN_POINT ( 'NONE',  ( -7.347880794884122694E-16, 6.750000000000000000, 4.000000000000001776 ) ) ;
#51856=ORIENTED_EDGE ( 'NONE', *, *, #13168, .F. ) ;
#51858=CARTESIAN_POINT ( 'NONE',  ( -1.881053915767124440, 2.124999998634406584, 4.541265875000001451 ) ) ;
#51875=CARTESIAN_POINT ( 'NONE',  ( 4.541265875000002339, 19.43749999863440436, 0.000000000000000000 ) ) ;
#51902=CYLINDRICAL_SURFACE ( 'NONE', #14036, 4.000000000000001776 ) ;
#51906=FACE_OUTER_BOUND ( 'NONE', #8047, .T. ) ;
#51920=CARTESIAN_POINT ( 'NONE',  ( -4.541265875000002339, 20.74999999863440436, -1.881053915767121998 ) ) ;
#51948=CARTESIAN_POINT ( 'NONE',  ( 1.656854249492381914, 5.812500000000000000, 4.000000000000000888 ) ) ;
#51949=CARTESIAN_POINT ( 'NONE',  ( 2.828427124746190291, 9.624999997268814056, 2.828427124746192067 ) ) ;
#52011=LINE ( 'NONE', #34304, #1051 ) ;
#52012=CARTESIAN_POINT ( 'NONE',  ( 4.000000000000000888, 9.937499999999998224, 1.656854249492384135 ) ) ;
#52013=CARTESIAN_POINT ( 'NONE',  ( -1.881053915767121554, 8.624999998634406140, -4.541265875000002339 ) ) ;
#52046=CARTESIAN_POINT ( 'NONE',  ( 1.656854249492381914, 21.56249999726881583, 4.000000000000000888 ) ) ;
#52048=DIRECTION ( 'NONE',  ( -0.000000000000000000, -1.000000000000000000, -0.000000000000000000 ) ) ;
#52053=( BOUNDED_CURVE ( )  B_SPLINE_CURVE ( 2, ( #71645, #42235, #42608, #7183, #49009, #48635, #53942, #60332, #8660 ),
 .UNSPECIFIED., .F., .F. ) 
 B_SPLINE_CURVE_WITH_KNOTS ( ( 3, 2, 2, 2, 3 ),
 ( 0.7386363636363636465, 0.7443181818181817677, 0.7500000000000000000, 0.7556818181818182323, 0.7613636363636363535 ),
 .UNSPECIFIED. ) 
 CURVE ( )  GEOMETRIC_REPRESENTATION_ITEM ( )  RATIONAL_B_SPLINE_CURVE ( ( 1.000000000000000000, 0.9238795325112867385, 1.000000000000000000, 0.9238795325112867385, 1.000000000000000000, 0.9238795325112867385, 1.000000000000000000, 0.9238795325112867385, 1.000000000000000000 ) ) 
 REPRESENTATION_ITEM ( '' )  );
#52055=VERTEX_POINT ( 'NONE', #17150 ) ;
#52057=CARTESIAN_POINT ( 'NONE',  ( -1.881053915767124440, 12.12499999863440969, 4.541265875000001451 ) ) ;
#52062=CARTESIAN_POINT ( 'NONE',  ( 1.656854249492381248, 10.18750000000000000, -4.000000000000001776 ) ) ;
#52063=CARTESIAN_POINT ( 'NONE',  ( -2.828427124746190735, 22.12499999726881583, -2.828427124746191623 ) ) ;
#52064=CARTESIAN_POINT ( 'NONE',  ( -4.541265875000002339, 11.81249999863440614, -5.561446717895856393E-16 ) ) ;
#52074=CARTESIAN_POINT ( 'NONE',  ( -4.000000000000002665, 10.56250000000000000, 1.656854249492380582 ) ) ;
#52083=CARTESIAN_POINT ( 'NONE',  ( 2.449293598294707893E-16, 8.999999997268814056, -4.000000000000001776 ) ) ;
#52134=LINE ( 'NONE', #52870, #70018 ) ;
#52140=DIRECTION ( 'NONE',  ( -0.000000000000000000, -1.000000000000000000, -0.000000000000000000 ) ) ;
#52145=CARTESIAN_POINT ( 'NONE',  ( 1.881053915767121998, 14.62499999863440969, -4.541265875000002339 ) ) ;
#52156=CARTESIAN_POINT ( 'NONE',  ( 1.656854249492381248, 11.93749999726881406, -4.000000000000001776 ) ) ;
#52157=CARTESIAN_POINT ( 'NONE',  ( -3.211159895383561391, 0.6874999986344068059, -3.211159895383561835 ) ) ;
#52158=ORIENTED_EDGE ( 'NONE', *, *, #72082, .F. ) ;
#52159=VECTOR ( 'NONE', #19268, 1000.000000000000000 ) ;
#52161=DIRECTION ( 'NONE',  ( 0.000000000000000000, 0.000000000000000000, -1.000000000000000000 ) ) ;
#52166=CARTESIAN_POINT ( 'NONE',  ( 2.780723358947928197E-16, 9.562499998634406140, -4.541265875000002339 ) ) ;
#52167=CARTESIAN_POINT ( 'NONE',  ( 2.828427124746191623, 16.12500000000000000, -2.828427124746191623 ) ) ;
#52188=CARTESIAN_POINT ( 'NONE',  ( 0.000000000000000000, 9.032624889217688457E-17, 4.000000000000000000 ) ) ;
#52207=CARTESIAN_POINT ( 'NONE',  ( 3.211159895383560947, 13.31249999863440792, 3.211159895383562723 ) ) ;
#52235=CARTESIAN_POINT ( 'NONE',  ( -4.541265875000002339, 0.9374999986344068059, -5.561446717895856393E-16 ) ) ;
#52247=CARTESIAN_POINT ( 'NONE',  ( -8.342170076843785083E-16, 21.18749999863440792, 4.541265875000002339 ) ) ;
#52292=AXIS2_PLACEMENT_3D ( 'NONE', #11415, #11049, #69129 ) ;
#52294=CARTESIAN_POINT ( 'NONE',  ( 3.211159895383561835, 1.562499998634406806, -3.211159895383561835 ) ) ;
#52306=ORIENTED_EDGE ( 'NONE', *, *, #52704, .F. ) ;
#52327=CARTESIAN_POINT ( 'NONE',  ( 2.828427124746190291, 20.62499999726881583, 2.828427124746192067 ) ) ;
#52332=CARTESIAN_POINT ( 'NONE',  ( 4.000754058696052162, 22.00000000000000000, 0.7008730298822498650 ) ) ;
#52359=ORIENTED_EDGE ( 'NONE', *, *, #43260, .F. ) ;
#52384=CARTESIAN_POINT ( 'NONE',  ( -7.347880794884122694E-16, 9.750000000000000000, 4.000000000000001776 ) ) ;
#52385=CARTESIAN_POINT ( 'NONE',  ( 2.780723358947928197E-16, 10.56249999863440792, -4.541265875000002339 ) ) ;
#52411=ORIENTED_EDGE ( 'NONE', *, *, #32090, .F. ) ;
#52420=ORIENTED_EDGE ( 'NONE', *, *, #62304, .F. ) ;
#52429=CARTESIAN_POINT ( 'NONE',  ( 2.828427124746191623, 13.12500000000000000, -2.828427124746191623 ) ) ;
#52431=CARTESIAN_POINT ( 'NONE',  ( -4.541265875000002339, 10.81249999863440792, -5.561446717895856393E-16 ) ) ;
#52469=( BOUNDED_CURVE ( )  B_SPLINE_CURVE ( 2, ( #50044, #27033, #11180, #68512, #21737, #57206, #73060, #50787, #16072 ),
 .UNSPECIFIED., .F., .F. ) 
 B_SPLINE_CURVE_WITH_KNOTS ( ( 3, 2, 2, 2, 3 ),
 ( 0.07954545454545454419, 0.08522727272727272096, 0.09090909090909091161, 0.09659090909090908839, 0.1022727272727272790 ),
 .UNSPECIFIED. ) 
 CURVE ( )  GEOMETRIC_REPRESENTATION_ITEM ( )  RATIONAL_B_SPLINE_CURVE ( ( 1.000000000000000000, 0.9238795325112867385, 1.000000000000000000, 0.9238795325112867385, 1.000000000000000000, 0.9238795325112867385, 1.000000000000000000, 0.9238795325112867385, 1.000000000000000000 ) ) 
 REPRESENTATION_ITEM ( '' )  );
#52476=VERTEX_POINT ( 'NONE', #56322 ) ;
#52498=CARTESIAN_POINT ( 'NONE',  ( -1.656854249492377029, 3.687500000000000888, 4.000000000000007994 ) ) ;
#52508=CARTESIAN_POINT ( 'NONE',  ( -4.000000000000001776, 8.437500000000000000, -1.656854249492381470 ) ) ;
#52513=CARTESIAN_POINT ( 'NONE',  ( -1.881053915767121776, 16.74999999863440436, -4.541265875000002339 ) ) ;
#52515=ORIENTED_EDGE ( 'NONE', *, *, #71378, .T. ) ;
#52517=CARTESIAN_POINT ( 'NONE',  ( 4.541265875000002339, 1.499999998634407028, -1.881053915767121554 ) ) ;
#52522=CARTESIAN_POINT ( 'NONE',  ( 2.828427124746190291, 14.62499999726881406, 2.828427124746192067 ) ) ;
#52529=CARTESIAN_POINT ( 'NONE',  ( 4.541265875000001451, 15.24999999863440969, 1.881053915767124440 ) ) ;
#52556=CARTESIAN_POINT ( 'NONE',  ( 1.881053915767122664, 3.124999998634407028, 4.541265875000001451 ) ) ;
#52570=AXIS2_PLACEMENT_3D ( 'NONE', #8127, #7395, #1743 ) ;
#52573=CARTESIAN_POINT ( 'NONE',  ( 2.780723358947928197E-16, 10.68749999863440792, -4.541265875000002339 ) ) ;
#52602=CARTESIAN_POINT ( 'NONE',  ( -3.211159895383561391, 1.812499998634406584, -3.211159895383561835 ) ) ;
#52615=CARTESIAN_POINT ( 'NONE',  ( -4.541265875000002339, 21.87499999863441147, -1.881053915767121998 ) ) ;
#52662=CARTESIAN_POINT ( 'NONE',  ( 3.211159895383560947, 21.18749999863440792, 3.211159895383562723 ) ) ;
#52668=DIRECTION ( 'NONE',  ( 0.000000000000000000, 0.000000000000000000, -1.000000000000000000 ) ) ;
#52681=CARTESIAN_POINT ( 'NONE',  ( 0.000000000000000000, 15.99999999999998579, -1.000000000000000000 ) ) ;
#52704=EDGE_CURVE ( 'NONE', #23461, #61992, #41786, .T. ) ;
#52753=CARTESIAN_POINT ( 'NONE',  ( -4.541265875000002339, 8.749999998634406140, -1.881053915767121998 ) ) ;
#52764=CARTESIAN_POINT ( 'NONE',  ( 4.000000000000001776, 8.749999997268814056, 0.000000000000000000 ) ) ;
#52780=CARTESIAN_POINT ( 'NONE',  ( 0.000000000000000000, 0.000000000000000000, -4.000000000000001776 ) ) ;
#52785=DIRECTION ( 'NONE',  ( 0.000000000000000000, 0.000000000000000000, -1.000000000000000000 ) ) ;
#52797=CARTESIAN_POINT ( 'NONE',  ( -1.656854249492381248, 10.31250000000000000, -4.000000000000001776 ) ) ;
#52799=CARTESIAN_POINT ( 'NONE',  ( 3.211159895383561835, 13.43749999863440614, -3.211159895383561835 ) ) ;
#52870=CARTESIAN_POINT ( 'NONE',  ( 4.898587196589415787E-16, 0.000000000000000000, 4.000000000000001776 ) ) ;
#52879=CARTESIAN_POINT ( 'NONE',  ( -1.656854249492371034, 8.687500000000000000, 4.000000000000013323 ) ) ;
#52883=CARTESIAN_POINT ( 'NONE',  ( 4.541265875000001451, 17.37499999863440436, 1.881053915767124440 ) ) ;
#52892=CARTESIAN_POINT ( 'NONE',  ( -4.000000000000001776, 0.5000000000000002220, -4.898587196589415787E-16 ) ) ;
#52893=CARTESIAN_POINT ( 'NONE',  ( 4.000000000000001776, 14.81249999726881406, -1.656854249492381248 ) ) ;
#52894=CARTESIAN_POINT ( 'NONE',  ( 2.449293598294707893E-16, 10.99999999726881406, -4.000000000000001776 ) ) ;
#52900=CARTESIAN_POINT ( 'NONE',  ( -4.541265875000002339, 14.81249999863440792, -5.561446717895856393E-16 ) ) ;
#52901=CARTESIAN_POINT ( 'NONE',  ( 1.656854249492381914, 11.81250000000000000, 4.000000000000000888 ) ) ;
#52918=AXIS2_PLACEMENT_3D ( 'NONE', #18314, #70727, #19046 ) ;
#52928=( BOUNDED_CURVE ( )  B_SPLINE_CURVE ( 2, ( #64622, #6906, #18596, #71366, #70642, #29917, #24244, #47619, #70284 ),
 .UNSPECIFIED., .F., .F. ) 
 B_SPLINE_CURVE_WITH_KNOTS ( ( 3, 2, 2, 2, 3 ),
 ( 0.2159090909090909116, 0.2215909090909090884, 0.2272727272727272652, 0.2329545454545454419, 0.2386363636363636465 ),
 .UNSPECIFIED. ) 
 CURVE ( )  GEOMETRIC_REPRESENTATION_ITEM ( )  RATIONAL_B_SPLINE_CURVE ( ( 1.000000000000000000, 0.9238795325112867385, 1.000000000000000000, 0.9238795325112867385, 1.000000000000000000, 0.9238795325112867385, 1.000000000000000000, 0.9238795325112867385, 1.000000000000000000 ) ) 
 REPRESENTATION_ITEM ( '' )  );
#52931=CARTESIAN_POINT ( 'NONE',  ( 3.211159895383561835, 1.437499998634406806, -3.211159895383561835 ) ) ;
#52942=LINE ( 'NONE', #29555, #22584 ) ;
#52944=CARTESIAN_POINT ( 'NONE',  ( 0.000000000000000000, 0.000000000000000000, 0.000000000000000000 ) ) ;
#52948=CARTESIAN_POINT ( 'NONE',  ( 3.211159895383560947, 18.31249999863440792, 3.211159895383562723 ) ) ;
#52972=CARTESIAN_POINT ( 'NONE',  ( -1.881053915767121776, 4.749999998634407028, -4.541265875000002339 ) ) ;
#52984=CARTESIAN_POINT ( 'NONE',  ( -2.828427124746190735, 1.124999997268813390, -2.828427124746191623 ) ) ;
#52991=CARTESIAN_POINT ( 'NONE',  ( 4.541265875000002339, 1.312499998634406584, 0.000000000000000000 ) ) ;
#53006=CARTESIAN_POINT ( 'NONE',  ( -7.347880794884122694E-16, 6.750000000000000000, 4.000000000000001776 ) ) ;
#53007=EDGE_CURVE ( 'NONE', #35916, #65881, #5745, .T. ) ;
#53021=CYLINDRICAL_SURFACE ( 'NONE', #52918, 4.000000000000001776 ) ;
#53034=CARTESIAN_POINT ( 'NONE',  ( -4.541265875000003227, 2.999999998634407028, 1.881053915767121110 ) ) ;
#53039=ORIENTED_EDGE ( 'NONE', *, *, #55869, .T. ) ;
#53070=CARTESIAN_POINT ( 'NONE',  ( 3.680852415662204891, 22.00000000000001066, 1.883217705396645014 ) ) ;
#53109=FACE_OUTER_BOUND ( 'NONE', #67374, .T. ) ;
#53127=CARTESIAN_POINT ( 'NONE',  ( 1.881053915767122664, 10.12499999863440792, 4.541265875000001451 ) ) ;
#53140=CARTESIAN_POINT ( 'NONE',  ( -1.656854249492405895, 13.06249999726881761, -3.999999999999976463 ) ) ;
#53155=DIRECTION ( 'NONE',  ( -0.000000000000000000, -1.000000000000000000, -0.000000000000000000 ) ) ;
#53163=PLANE ( 'NONE',  #25500 ) ;
#53169=CARTESIAN_POINT ( 'NONE',  ( -2.828427124746192067, 12.62500000000000000, 2.828427124746190735 ) ) ;
#53171=CARTESIAN_POINT ( 'NONE',  ( 1.881053915767122664, 10.12499999863440792, 4.541265875000001451 ) ) ;
#53179=CARTESIAN_POINT ( 'NONE',  ( 1.656854249492381914, 13.56249999726881406, 4.000000000000000888 ) ) ;
#53181=EDGE_CURVE ( 'NONE', #7770, #59197, #23287, .T. ) ;
#53253=CARTESIAN_POINT ( 'NONE',  ( -1.881053915767124440, 18.12499999863441147, 4.541265875000001451 ) ) ;
#53265=CARTESIAN_POINT ( 'NONE',  ( -1.656854249492383691, 15.43749999726881583, 4.000000000000000888 ) ) ;
#53266=CARTESIAN_POINT ( 'NONE',  ( -4.541265875000003227, 0.8749999986344068059, 1.881053915767121110 ) ) ;
#53273=CARTESIAN_POINT ( 'NONE',  ( 3.211159895383561835, 15.43749999863440614, -3.211159895383561835 ) ) ;
#53276=CARTESIAN_POINT ( 'NONE',  ( 2.449293598294707893E-16, 12.25000000000000000, -4.000000000000001776 ) ) ;
#53304=CARTESIAN_POINT ( 'NONE',  ( 4.541265875000001451, 2.249999998634407028, 1.881053915767124440 ) ) ;
#53320=CARTESIAN_POINT ( 'NONE',  ( -3.211159895383562723, 16.06249999863440436, 3.211159895383561391 ) ) ;
#53343=CARTESIAN_POINT ( 'NONE',  ( -3.211159895383561391, 5.812499998634407028, -3.211159895383561835 ) ) ;
#53357=CARTESIAN_POINT ( 'NONE',  ( -4.000000000000001776, 3.187499997268814056, -1.656854249492381470 ) ) ;
#53362=CARTESIAN_POINT ( 'NONE',  ( 2.780723358947928197E-16, 2.562499998634407028, -4.541265875000002339 ) ) ;
#53407=CARTESIAN_POINT ( 'NONE',  ( -3.211159895383562723, 3.062499998634407028, 3.211159895383561391 ) ) ;
#53422=CARTESIAN_POINT ( 'NONE',  ( 4.000000000000001776, 0.7499999972688131678, 0.000000000000000000 ) ) ;
#53454=CARTESIAN_POINT ( 'NONE',  ( -1.881053915767124440, 10.12499999863440792, 4.541265875000001451 ) ) ;
#53466=CARTESIAN_POINT ( 'NONE',  ( -4.310155712710913356, 22.00000000000000000, 1.403903855516097421 ) ) ;
#53485=CARTESIAN_POINT ( 'NONE',  ( 4.000000000000001776, 19.06250000000000000, -1.656854249492381248 ) ) ;
#53494=CARTESIAN_POINT ( 'NONE',  ( 2.449293598294707893E-16, 18.99999999726881228, -4.000000000000001776 ) ) ;
#53495=CARTESIAN_POINT ( 'NONE',  ( -1.881053915767124440, 14.99999999863440969, 4.541265875000001451 ) ) ;
#53512=CARTESIAN_POINT ( 'NONE',  ( 4.000000000000000888, 12.93750000000000355, 1.656854249492384135 ) ) ;
#53522=CARTESIAN_POINT ( 'NONE',  ( 2.828427124746190291, 3.875000000000000000, 2.828427124746192067 ) ) ;
#53539=CARTESIAN_POINT ( 'NONE',  ( -4.000000000000001776, 13.50000000000000000, -4.898587196589415787E-16 ) ) ;
#53541=CARTESIAN_POINT ( 'NONE',  ( 4.541265875000001451, 17.24999999863440792, 1.881053915767124440 ) ) ;
#53549=CARTESIAN_POINT ( 'NONE',  ( 4.000000000000000888, 6.687499997268813168, 1.656854249492384135 ) ) ;
#53607=ORIENTED_EDGE ( 'NONE', *, *, #45966, .F. ) ;
#53608=CARTESIAN_POINT ( 'NONE',  ( 4.000000000000001776, 7.062500000000000000, -1.656854249492381248 ) ) ;
#53623=CARTESIAN_POINT ( 'NONE',  ( -1.881053915767124440, 17.12499999863440436, 4.541265875000001451 ) ) ;
#53627=CARTESIAN_POINT ( 'NONE',  ( -3.211159895383561391, 0.8124999986344069169, -3.211159895383561835 ) ) ;
#53636=CARTESIAN_POINT ( 'NONE',  ( -4.000000000000001776, 16.24999999726881228, -4.898587196589415787E-16 ) ) ;
#53637=CARTESIAN_POINT ( 'NONE',  ( -3.211159895383561391, 3.687499998634407028, -3.211159895383561835 ) ) ;
#53644=CARTESIAN_POINT ( 'NONE',  ( 1.881053915767122664, 14.12499999863440969, 4.541265875000001451 ) ) ;
#53661=CARTESIAN_POINT ( 'NONE',  ( 1.656854249492381248, 8.187500000000000000, -4.000000000000001776 ) ) ;
#53668=CARTESIAN_POINT ( 'NONE',  ( -3.211159895383562723, 1.937499998634406806, 3.211159895383561391 ) ) ;
#53684=( BOUNDED_CURVE ( )  B_SPLINE_CURVE ( 2, ( #74422, #28029, #23478, #46490, #22728, #69511, #17823, #40837, #35195 ),
 .UNSPECIFIED., .F., .F. ) 
 B_SPLINE_CURVE_WITH_KNOTS ( ( 3, 2, 2, 2, 3 ),
 ( 0.7840909090909090606, 0.7897727272727272929, 0.7954545454545454142, 0.8011363636363637575, 0.8068181818181818787 ),
 .UNSPECIFIED. ) 
 CURVE ( )  GEOMETRIC_REPRESENTATION_ITEM ( )  RATIONAL_B_SPLINE_CURVE ( ( 1.000000000000000000, 0.9238795325112867385, 1.000000000000000000, 0.9238795325112867385, 1.000000000000000000, 0.9238795325112867385, 1.000000000000000000, 0.9238795325112852952, 1.000000000000001554 ) ) 
 REPRESENTATION_ITEM ( '' )  );
#53689=CARTESIAN_POINT ( 'NONE',  ( -3.211159895383561391, 16.81249999863440436, -3.211159895383561835 ) ) ;
#53712=CARTESIAN_POINT ( 'NONE',  ( -4.541265875000002339, 4.874999998634406140, -1.881053915767121998 ) ) ;
#53722=EDGE_CURVE ( 'NONE', #61381, #33430, #25897, .T. ) ;
#53724=CARTESIAN_POINT ( 'NONE',  ( -1.656854249492383691, 2.437499997268814056, 4.000000000000000888 ) ) ;
#53730=CARTESIAN_POINT ( 'NONE',  ( 4.541265875000001451, 3.249999998634406584, 1.881053915767124440 ) ) ;
#53774=CARTESIAN_POINT ( 'NONE',  ( 3.211159895383560947, 5.312499998634407028, 3.211159895383562723 ) ) ;
#53801=( BOUNDED_CURVE ( )  B_SPLINE_CURVE ( 2, ( #1282, #42720, #12572, #48008, #12933, #65733, #14035, #2001, #42350 ),
 .UNSPECIFIED., .F., .F. ) 
 B_SPLINE_CURVE_WITH_KNOTS ( ( 3, 2, 2, 2, 3 ),
 ( 0.4886363636363636465, 0.4943181818181818232, 0.5000000000000000000, 0.5056818181818182323, 0.5113636363636363535 ),
 .UNSPECIFIED. ) 
 CURVE ( )  GEOMETRIC_REPRESENTATION_ITEM ( )  RATIONAL_B_SPLINE_CURVE ( ( 1.000000000000000000, 0.9238795325112867385, 1.000000000000000000, 0.9238795325112867385, 1.000000000000000000, 0.9238795325112867385, 1.000000000000000000, 0.9238795325112867385, 1.000000000000000000 ) ) 
 REPRESENTATION_ITEM ( '' )  );
#53820=CARTESIAN_POINT ( 'NONE',  ( 1.881053915767122664, 10.24999999863440792, 4.541265875000001451 ) ) ;
#53834=CARTESIAN_POINT ( 'NONE',  ( -4.195582579073398932, 22.00000000000000355, 1.737867247408543925 ) ) ;
#53861=CARTESIAN_POINT ( 'NONE',  ( 1.881053915767122664, 13.12499999863440969, 4.541265875000001451 ) ) ;
#53866=ADVANCED_FACE ( 'NONE', ( #31572 ), #36864, .T. ) ;
#53902=ORIENTED_EDGE ( 'NONE', *, *, #72950, .F. ) ;
#53904=( BOUNDED_CURVE ( )  B_SPLINE_CURVE ( 2, ( #34644, #18014, #28212, #74611, #23296, #28586, #35015, #22924, #47043 ),
 .UNSPECIFIED., .F., .F. ) 
 B_SPLINE_CURVE_WITH_KNOTS ( ( 3, 2, 2, 2, 3 ),
 ( 0.07954545454545454419, 0.08522727272727272096, 0.09090909090909091161, 0.09659090909090908839, 0.1022727272727272790 ),
 .UNSPECIFIED. ) 
 CURVE ( )  GEOMETRIC_REPRESENTATION_ITEM ( )  RATIONAL_B_SPLINE_CURVE ( ( 1.000000000000000000, 0.9238795325112867385, 1.000000000000000000, 0.9238795325112867385, 1.000000000000000000, 0.9238795325112867385, 1.000000000000000000, 0.9238795325112867385, 1.000000000000000000 ) ) 
 REPRESENTATION_ITEM ( '' )  );
#53906=CARTESIAN_POINT ( 'NONE',  ( -7.347880794884122694E-16, 15.75000000000000000, 4.000000000000001776 ) ) ;
#53907=CARTESIAN_POINT ( 'NONE',  ( -4.541265875000002339, 15.81249999863440436, -5.561446717895856393E-16 ) ) ;
#53917=ADVANCED_FACE ( 'NONE', ( #53109 ), #71176, .T. ) ;
#53922=AXIS2_PLACEMENT_3D ( 'NONE', #58206, #11788, #125 ) ;
#53931=CARTESIAN_POINT ( 'NONE',  ( -2.828427124746190735, 0.3750000000000001665, -2.828427124746191623 ) ) ;
#53933=VECTOR ( 'NONE', #20349, 1000.000000000000000 ) ;
#53942=CARTESIAN_POINT ( 'NONE',  ( -2.828427124746192067, 16.62500000000000000, 2.828427124746190735 ) ) ;
#53944=CARTESIAN_POINT ( 'NONE',  ( -4.000000000000002665, 12.56250000000000000, 1.656854249492380582 ) ) ;
#53946=LINE ( 'NONE', #19970, #9406 ) ;
#53954=CARTESIAN_POINT ( 'NONE',  ( -4.000000000000002665, 14.56250000000000000, 1.656854249492380582 ) ) ;
#53987=CARTESIAN_POINT ( 'NONE',  ( 4.541265875000002339, 15.43749999863440614, 0.000000000000000000 ) ) ;
#53991=CARTESIAN_POINT ( 'NONE',  ( -1.881053915767121554, 4.749999998634407028, -4.541265875000002339 ) ) ;
#53998=CARTESIAN_POINT ( 'NONE',  ( 4.000000000000001776, 1.062500000000000222, -1.656854249492381248 ) ) ;
#53999=CARTESIAN_POINT ( 'NONE',  ( 1.656854249492381914, 12.56249999726881406, 4.000000000000000888 ) ) ;
#54000=CARTESIAN_POINT ( 'NONE',  ( 1.881053915767121998, 4.499999998634407028, -4.541265875000002339 ) ) ;
#54007=CARTESIAN_POINT ( 'NONE',  ( 4.541265875000002339, 15.31249999863440614, 0.000000000000000000 ) ) ;
#54025=VERTEX_POINT ( 'NONE', #71543 ) ;
#54030=CARTESIAN_POINT ( 'NONE',  ( -2.828427124746190735, 5.375000000000000000, -2.828427124746191623 ) ) ;
#54031=CARTESIAN_POINT ( 'NONE',  ( 2.828427124746191623, 8.125000000000000000, -2.828427124746191623 ) ) ;
#54039=CARTESIAN_POINT ( 'NONE',  ( -3.211159895383562723, 3.937499998634406584, 3.211159895383561391 ) ) ;
#54058=CARTESIAN_POINT ( 'NONE',  ( -1.881053915767121554, 16.74999999863440792, -4.541265875000002339 ) ) ;
#54073=CARTESIAN_POINT ( 'NONE',  ( -7.347880794884122694E-16, 17.75000000000000355, 4.000000000000001776 ) ) ;
#54081=CARTESIAN_POINT ( 'NONE',  ( 4.541265875000002339, 6.499999998634407916, -1.881053915767121776 ) ) ;
#54092=CARTESIAN_POINT ( 'NONE',  ( 4.000000000000000888, 3.687499997268813168, 1.656854249492384135 ) ) ;
#54098=CARTESIAN_POINT ( 'NONE',  ( -1.881053915767124440, 2.999999998634407028, 4.541265875000001451 ) ) ;
#54141=( BOUNDED_CURVE ( )  B_SPLINE_CURVE ( 2, ( #13121, #53140, #70486, #30857, #18805, #1827, #24814, #13489, #47829 ),
 .UNSPECIFIED., .F., .F. ) 
 B_SPLINE_CURVE_WITH_KNOTS ( ( 3, 2, 2, 2, 3 ),
 ( 0.5568181818181818787, 0.5625000000000001110, 0.5681818181818183433, 0.5738636363636363535, 0.5795454545454545858 ),
 .UNSPECIFIED. ) 
 CURVE ( )  GEOMETRIC_REPRESENTATION_ITEM ( )  RATIONAL_B_SPLINE_CURVE ( ( 0.9999999999999985567, 0.9238795325112881818, 1.000000000000000000, 0.9238795325112867385, 1.000000000000000000, 0.9238795325112867385, 1.000000000000000000, 0.9238795325112867385, 1.000000000000000000 ) ) 
 REPRESENTATION_ITEM ( '' )  );
#54146=CARTESIAN_POINT ( 'NONE',  ( 1.881053915767122664, 3.249999998634406584, 4.541265875000001451 ) ) ;
#54193=CARTESIAN_POINT ( 'NONE',  ( 4.541265875000002339, 12.43749999863440792, 0.000000000000000000 ) ) ;
#54206=CARTESIAN_POINT ( 'NONE',  ( -3.422326672995520180, 21.99999999999999645, -2.553026752608630101 ) ) ;
#54237=CARTESIAN_POINT ( 'NONE',  ( -8.342170076843785083E-16, 15.06249999863440792, 4.541265875000002339 ) ) ;
#54244=ADVANCED_FACE ( 'NONE', ( #51906 ), #23227, .T. ) ;
#54268=CARTESIAN_POINT ( 'NONE',  ( 2.828427124746191623, 3.874999997268813168, -2.828427124746191623 ) ) ;
#54286=CARTESIAN_POINT ( 'NONE',  ( 1.656854249492381914, 15.81250000000000178, 4.000000000000000888 ) ) ;
#54287=CARTESIAN_POINT ( 'NONE',  ( 3.211159895383560947, 15.18749999863440792, 3.211159895383562723 ) ) ;
#54307=CARTESIAN_POINT ( 'NONE',  ( 0.000000000000000000, 22.00000000000000355, 8.000000000000003553 ) ) ;
#54319=CARTESIAN_POINT ( 'NONE',  ( 2.828427124746190291, 5.624999997268813168, 2.828427124746192067 ) ) ;
#54328=CARTESIAN_POINT ( 'NONE',  ( -1.656854249492381248, 6.312500000000000000, -4.000000000000001776 ) ) ;
#54332=CARTESIAN_POINT ( 'NONE',  ( 2.449293598294707893E-16, 14.25000000000000000, -4.000000000000001776 ) ) ;
#54360=( BOUNDED_CURVE ( )  B_SPLINE_CURVE ( 2, ( #65381, #2381, #42366, #30685, #18257, #24278, #41640, #36352, #54073 ),
 .UNSPECIFIED., .F., .F. ) 
 B_SPLINE_CURVE_WITH_KNOTS ( ( 3, 2, 2, 2, 3 ),
 ( 0.7840909090909090606, 0.7897727272727272929, 0.7954545454545454142, 0.8011363636363637575, 0.8068181818181818787 ),
 .UNSPECIFIED. ) 
 CURVE ( )  GEOMETRIC_REPRESENTATION_ITEM ( )  RATIONAL_B_SPLINE_CURVE ( ( 1.000000000000000000, 0.9238795325112867385, 1.000000000000000000, 0.9238795325112867385, 1.000000000000000000, 0.9238795325112867385, 1.000000000000000000, 0.9238795325112852952, 1.000000000000001554 ) ) 
 REPRESENTATION_ITEM ( '' )  );
#54367=CARTESIAN_POINT ( 'NONE',  ( 1.881053915767122664, 19.24999999863440436, 4.541265875000001451 ) ) ;
#54371=CARTESIAN_POINT ( 'NONE',  ( 4.541265875000002339, 2.437499998634407028, 0.000000000000000000 ) ) ;
#54374=ADVANCED_FACE ( 'NONE', ( #34196 ), #53021, .T. ) ;
#54379=CARTESIAN_POINT ( 'NONE',  ( 4.000000000000001776, 5.062500000000001776, -1.656854249492381248 ) ) ;
#54380=CARTESIAN_POINT ( 'NONE',  ( 1.656854249492381248, 17.93749999726881583, -4.000000000000001776 ) ) ;
#54381=CARTESIAN_POINT ( 'NONE',  ( -1.881053915767124440, 2.999999998634407028, 4.541265875000001451 ) ) ;
#54387=CARTESIAN_POINT ( 'NONE',  ( 4.541265875000001451, 18.24999999863440792, 1.881053915767124440 ) ) ;
#54416=CARTESIAN_POINT ( 'NONE',  ( -4.541265875000002339, 5.812499998634406140, -5.561446717895856393E-16 ) ) ;
#54434=CARTESIAN_POINT ( 'NONE',  ( 1.881053915767122664, 15.24999999863440969, 4.541265875000001451 ) ) ;
#54437=VERTEX_POINT ( 'NONE', #65057 ) ;
#54441=CARTESIAN_POINT ( 'NONE',  ( -4.000000000000001776, 12.24999999726881406, -4.898587196589415787E-16 ) ) ;
#54460=CARTESIAN_POINT ( 'NONE',  ( -3.211159895383562723, 5.062499998634407028, 3.211159895383561391 ) ) ;
#54472=CARTESIAN_POINT ( 'NONE',  ( 2.449293598294707893E-16, 2.999999997268813168, -4.000000000000001776 ) ) ;
#54479=CARTESIAN_POINT ( 'NONE',  ( 4.541265875000001451, 1.249999998634407028, 1.881053915767124440 ) ) ;
#54495=ORIENTED_EDGE ( 'NONE', *, *, #8548, .F. ) ;
#54520=CARTESIAN_POINT ( 'NONE',  ( 2.780723358947928197E-16, 4.687499998634407028, -4.541265875000002339 ) ) ;
#54564=CARTESIAN_POINT ( 'NONE',  ( 4.541265875000001451, 11.37499999863440969, 1.881053915767124440 ) ) ;
#54584=ORIENTED_EDGE ( 'NONE', *, *, #43297, .T. ) ;
#54610=CARTESIAN_POINT ( 'NONE',  ( 4.541265875000001451, 13.24999999863441147, 1.881053915767124440 ) ) ;
#54629=CARTESIAN_POINT ( 'NONE',  ( 2.828427124746190291, 12.87500000000000178, 2.828427124746192067 ) ) ;
#54657=ADVANCED_FACE ( 'NONE', ( #20146 ), #55998, .T. ) ;
#54658=CARTESIAN_POINT ( 'NONE',  ( 2.828427124746190291, 14.87500000000000178, 2.828427124746192067 ) ) ;
#54659=CARTESIAN_POINT ( 'NONE',  ( -4.541265875000003227, 13.87499999863440792, 1.881053915767121110 ) ) ;
#54700=CARTESIAN_POINT ( 'NONE',  ( -4.000000000000002665, 6.562500000000000000, 1.656854249492380582 ) ) ;
#54705=CARTESIAN_POINT ( 'NONE',  ( -2.828427124746192067, 14.62500000000000000, 2.828427124746190735 ) ) ;
#54745=CARTESIAN_POINT ( 'NONE',  ( 4.541265875000002339, 5.437499998634407028, 0.000000000000000000 ) ) ;
#54751=CARTESIAN_POINT ( 'NONE',  ( -7.347880794884122694E-16, 3.750000000000000000, 4.000000000000001776 ) ) ;
#54752=CARTESIAN_POINT ( 'NONE',  ( -4.000000000000001776, 18.18749999726881228, -1.656854249492381470 ) ) ;
#54753=CARTESIAN_POINT ( 'NONE',  ( 3.211159895383560947, 3.187499998634407028, 3.211159895383562723 ) ) ;
#54758=CARTESIAN_POINT ( 'NONE',  ( 3.211159895383561835, 16.43749999863440436, -3.211159895383561835 ) ) ;
#54778=CARTESIAN_POINT ( 'NONE',  ( -7.347880794884122694E-16, 16.75000000000000000, 4.000000000000001776 ) ) ;
#54787=CARTESIAN_POINT ( 'NONE',  ( 3.211159895383561835, 4.437499998634407028, -3.211159895383561835 ) ) ;
#54789=CARTESIAN_POINT ( 'NONE',  ( -2.828427124746190735, 14.12499999726881406, -2.828427124746191623 ) ) ;
#54792=AXIS2_PLACEMENT_3D ( 'NONE', #52188, #70276, #69908 ) ;
#54807=CARTESIAN_POINT ( 'NONE',  ( -3.211159895383562723, 19.06249999863440436, 3.211159895383561391 ) ) ;
#54833=CARTESIAN_POINT ( 'NONE',  ( 3.211159895383561835, 8.562499998634407916, -3.211159895383561835 ) ) ;
#54843=CARTESIAN_POINT ( 'NONE',  ( -1.656854249492381248, 6.062499997268813168, -4.000000000000001776 ) ) ;
#54847=CARTESIAN_POINT ( 'NONE',  ( 1.881053915767122664, 8.124999998634407916, 4.541265875000001451 ) ) ;
#54874=DIRECTION ( 'NONE',  ( -0.000000000000000000, -1.000000000000000000, -0.000000000000000000 ) ) ;
#54892=CARTESIAN_POINT ( 'NONE',  ( 1.881053915767121776, 9.624999998634404363, -4.541265875000002339 ) ) ;
#54913=CARTESIAN_POINT ( 'NONE',  ( -7.347880794884122694E-16, 19.49999999726881228, 4.000000000000001776 ) ) ;
#54939=CARTESIAN_POINT ( 'NONE',  ( 1.881053915767122664, 15.24999999863440969, 4.541265875000001451 ) ) ;
#54949=CARTESIAN_POINT ( 'NONE',  ( 2.828427124746190291, 19.87500000000000000, 2.828427124746192067 ) ) ;
#54985=CARTESIAN_POINT ( 'NONE',  ( -4.541265875000003227, 13.87499999863440969, 1.881053915767121110 ) ) ;
#55021=CARTESIAN_POINT ( 'NONE',  ( 2.449293598294707893E-16, 20.25000000000000000, -4.000000000000001776 ) ) ;
#55032=CARTESIAN_POINT ( 'NONE',  ( 2.828427124746191623, 17.12500000000000000, -2.828427124746191623 ) ) ;
#55033=CARTESIAN_POINT ( 'NONE',  ( -3.211159895383562723, 16.93749999863440436, 3.211159895383561391 ) ) ;
#55036=ADVANCED_FACE ( 'NONE', ( #39743 ), #17774, .F. ) ;
#55116=CARTESIAN_POINT ( 'NONE',  ( -1.881053915767124440, 19.12499999863441147, 4.541265875000001451 ) ) ;
#55119=CARTESIAN_POINT ( 'NONE',  ( 4.541265875000002339, 3.437499998634407028, 0.000000000000000000 ) ) ;
#55126=CARTESIAN_POINT ( 'NONE',  ( -7.347880794884122694E-16, 4.750000000000000000, 4.000000000000001776 ) ) ;
#55127=CARTESIAN_POINT ( 'NONE',  ( 2.828427124746190291, 18.62499999726881583, 2.828427124746192067 ) ) ;
#55128=CARTESIAN_POINT ( 'NONE',  ( 3.211159895383560947, 5.187499998634407028, 3.211159895383562723 ) ) ;
#55134=CARTESIAN_POINT ( 'NONE',  ( 4.541265875000002339, 16.37499999863440436, -1.881053915767121554 ) ) ;
#55166=CARTESIAN_POINT ( 'NONE',  ( 2.780723358947928197E-16, 5.562499998634407028, -4.541265875000002339 ) ) ;
#55185=CARTESIAN_POINT ( 'NONE',  ( -1.881053915767124440, 20.12499999863441147, 4.541265875000001451 ) ) ;
#55208=CARTESIAN_POINT ( 'NONE',  ( 2.780723358947928197E-16, 7.687499998634407028, -4.541265875000002339 ) ) ;
#55216=VECTOR ( 'NONE', #9705, 1000.000000000000000 ) ;
#55219=CARTESIAN_POINT ( 'NONE',  ( -1.656854249492383691, 4.437499997268813168, 4.000000000000000888 ) ) ;
#55225=CARTESIAN_POINT ( 'NONE',  ( -3.211159895383562723, 7.937499998634407028, 3.211159895383561391 ) ) ;
#55256=FACE_OUTER_BOUND ( 'NONE', #12596, .T. ) ;
#55271=CARTESIAN_POINT ( 'NONE',  ( -4.541265875000003227, 7.999999998634407028, 1.881053915767121110 ) ) ;
#55275=CARTESIAN_POINT ( 'NONE',  ( 1.656854249492381914, 0.8125000000000004441, 4.000000000000000888 ) ) ;
#55312=CARTESIAN_POINT ( 'NONE',  ( 4.541265875000002339, 14.43749999863440792, 0.000000000000000000 ) ) ;
#55357=CARTESIAN_POINT ( 'NONE',  ( 4.541265875000002339, 17.31249999863440792, 0.000000000000000000 ) ) ;
#55407=CARTESIAN_POINT ( 'NONE',  ( -1.656854249492381248, 17.31250000000000355, -4.000000000000001776 ) ) ;
#55408=CARTESIAN_POINT ( 'NONE',  ( 4.541265875000002339, 20.37499999863441147, -1.881053915767121776 ) ) ;
#55486=CARTESIAN_POINT ( 'NONE',  ( -4.541265875000002339, 19.87499999863441147, -1.881053915767121998 ) ) ;
#55489=CARTESIAN_POINT ( 'NONE',  ( -3.211159895383562723, 5.062499998634407028, 3.211159895383561391 ) ) ;
#55499=CARTESIAN_POINT ( 'NONE',  ( -7.347880794884122694E-16, 5.750000000000000000, 4.000000000000001776 ) ) ;
#55500=CARTESIAN_POINT ( 'NONE',  ( -1.656854249492381248, 19.06249999726881228, -4.000000000000001776 ) ) ;
#55501=CARTESIAN_POINT ( 'NONE',  ( -4.541265875000002339, 7.749999998634407916, -1.881053915767121998 ) ) ;
#55508=CARTESIAN_POINT ( 'NONE',  ( -1.881053915767124440, 16.99999999863440792, 4.541265875000001451 ) ) ;
#55542=CARTESIAN_POINT ( 'NONE',  ( -3.211159895383561391, 5.687499998634407028, -3.211159895383561835 ) ) ;
#55549=CARTESIAN_POINT ( 'NONE',  ( 4.000000000000001776, 19.81249999726881228, -1.656854249492381248 ) ) ;
#55558=CARTESIAN_POINT ( 'NONE',  ( 4.541265875000002339, 20.43749999863440436, 0.000000000000000000 ) ) ;
#55561=VERTEX_POINT ( 'NONE', #9930 ) ;
#55564=CARTESIAN_POINT ( 'NONE',  ( -4.000000000000002665, 12.31249999726881406, 1.656854249492380582 ) ) ;
#55566=CARTESIAN_POINT ( 'NONE',  ( 0.000000000000000000, 1.806524977843537691E-16, 0.000000000000000000 ) ) ;
#55570=ORIENTED_EDGE ( 'NONE', *, *, #45533, .F. ) ;
#55579=CARTESIAN_POINT ( 'NONE',  ( 4.541265875000002339, 9.437499998634407916, 0.000000000000000000 ) ) ;
#55590=CARTESIAN_POINT ( 'NONE',  ( -2.828427124746190735, 6.124999997268813168, -2.828427124746191623 ) ) ;
#55598=CARTESIAN_POINT ( 'NONE',  ( 1.881053915767122664, 5.124999998634406140, 4.541265875000001451 ) ) ;
#55615=CARTESIAN_POINT ( 'NONE',  ( -7.347880794884122694E-16, 3.499999997268812724, 4.000000000000001776 ) ) ;
#55641=AXIS2_PLACEMENT_3D ( 'NONE', #32474, #4542, #50927 ) ;
#55643=CARTESIAN_POINT ( 'NONE',  ( 2.780723358947928197E-16, 6.687499998634407028, -4.541265875000002339 ) ) ;
#55653=EDGE_CURVE ( 'NONE', #22328, #9782, #12481, .T. ) ;
#55656=ORIENTED_EDGE ( 'NONE', *, *, #45265, .F. ) ;
#55673=VERTEX_POINT ( 'NONE', #12517 ) ;
#55674=CARTESIAN_POINT ( 'NONE',  ( -2.828427124746190735, 4.375000000000000000, -2.828427124746191623 ) ) ;
#55689=CARTESIAN_POINT ( 'NONE',  ( -1.881053915767124440, 16.12499999863440792, 4.541265875000001451 ) ) ;
#55702=DIRECTION ( 'NONE',  ( -0.000000000000000000, -1.000000000000000000, -0.000000000000000000 ) ) ;
#55710=CARTESIAN_POINT ( 'NONE',  ( 2.449293598294707893E-16, 1.999999997268813168, -4.000000000000001776 ) ) ;
#55731=CARTESIAN_POINT ( 'NONE',  ( -3.211159895383561391, 17.68749999863440792, -3.211159895383561835 ) ) ;
#55765=CARTESIAN_POINT ( 'NONE',  ( -1.656854249492381248, 19.31250000000000000, -4.000000000000001776 ) ) ;
#55774=VERTEX_POINT ( 'NONE', #52894 ) ;
#55781=CARTESIAN_POINT ( 'NONE',  ( 1.656854249492381914, 21.81250000000000355, 4.000000000000000888 ) ) ;
#55782=CARTESIAN_POINT ( 'NONE',  ( -4.541265875000002339, 19.81249999863440436, -5.561446717895856393E-16 ) ) ;
#55786=CARTESIAN_POINT ( 'NONE',  ( 4.000000000000000888, 4.687499997268813168, 1.656854249492384135 ) ) ;
#55810=EDGE_CURVE ( 'NONE', #46633, #56773, #71724, .T. ) ;
#55845=VECTOR ( 'NONE', #57954, 1000.000000000000000 ) ;
#55866=CARTESIAN_POINT ( 'NONE',  ( 3.211159895383561835, 9.562499998634406140, -3.211159895383561835 ) ) ;
#55869=EDGE_CURVE ( 'NONE', #57513, #59211, #53904, .T. ) ;
#55872=CARTESIAN_POINT ( 'NONE',  ( 2.828427124746190291, 2.875000000000000000, 2.828427124746192067 ) ) ;
#55873=CARTESIAN_POINT ( 'NONE',  ( 4.000000000000001776, 18.81249999726881228, -1.656854249492381248 ) ) ;
#55874=CARTESIAN_POINT ( 'NONE',  ( -4.541265875000002339, 8.812499998634407916, -5.561446717895856393E-16 ) ) ;
#55881=CARTESIAN_POINT ( 'NONE',  ( 1.881053915767122664, 20.12499999863441147, 4.541265875000001451 ) ) ;
#55915=CARTESIAN_POINT ( 'NONE',  ( -3.211159895383561391, 7.687499998634407028, -3.211159895383561835 ) ) ;
#55934=CARTESIAN_POINT ( 'NONE',  ( 1.881053915767122664, 21.24999999863440436, 4.541265875000001451 ) ) ;
#55945=EDGE_CURVE ( 'NONE', #33430, #25548, #20178, .T. ) ;
#55950=DIRECTION ( 'NONE',  ( 0.000000000000000000, 0.000000000000000000, -1.000000000000000000 ) ) ;
#55956=CARTESIAN_POINT ( 'NONE',  ( -4.541265875000002339, 9.874999998634404363, -1.881053915767121998 ) ) ;
#55966=CARTESIAN_POINT ( 'NONE',  ( 2.828427124746191623, 6.874999997268813168, -2.828427124746191623 ) ) ;
#55972=CARTESIAN_POINT ( 'NONE',  ( -3.211159895383561391, 5.687499998634407028, -3.211159895383561835 ) ) ;
#55983=EDGE_CURVE ( 'NONE', #16346, #46633, #61246, .T. ) ;
#55998=CYLINDRICAL_SURFACE ( 'NONE', #45747, 4.000000000000001776 ) ;
#56014=CARTESIAN_POINT ( 'NONE',  ( 4.541265875000002339, 8.499999998634406140, -1.881053915767121554 ) ) ;
#56017=CARTESIAN_POINT ( 'NONE',  ( -4.000000000000002665, 5.312499997268812280, 1.656854249492380582 ) ) ;
#56021=( BOUNDED_CURVE ( )  B_SPLINE_CURVE ( 2, ( #1158, #59592, #53931, #47515, #24511, #24866, #70180, #65611, #35847 ),
 .UNSPECIFIED., .F., .F. ) 
 B_SPLINE_CURVE_WITH_KNOTS ( ( 3, 2, 2, 2, 3 ),
 ( 0.01136363636363636395, 0.01704545454545454419, 0.02272727272727272790, 0.02840909090909090814, 0.03409090909090908839 ),
 .UNSPECIFIED. ) 
 CURVE ( )  GEOMETRIC_REPRESENTATION_ITEM ( )  RATIONAL_B_SPLINE_CURVE ( ( 1.000000000000000000, 0.9238795325112867385, 1.000000000000000000, 0.9238795325112867385, 1.000000000000000000, 0.9238795325112867385, 1.000000000000000000, 0.9238795325112867385, 1.000000000000000000 ) ) 
 REPRESENTATION_ITEM ( '' )  );
#56059=CARTESIAN_POINT ( 'NONE',  ( 1.881053915767122664, 17.24999999863440792, 4.541265875000001451 ) ) ;
#56101=CARTESIAN_POINT ( 'NONE',  ( -1.881053915767121554, 17.62499999863440436, -4.541265875000002339 ) ) ;
#56113=ORIENTED_EDGE ( 'NONE', *, *, #66528, .T. ) ;
#56151=CARTESIAN_POINT ( 'NONE',  ( -2.828427124746190735, 21.37500000000000000, -2.828427124746191623 ) ) ;
#56152=CARTESIAN_POINT ( 'NONE',  ( 2.780723358947928197E-16, 18.56249999863440436, -4.541265875000002339 ) ) ;
#56214=VERTEX_POINT ( 'NONE', #1144 ) ;
#56215=CYLINDRICAL_SURFACE ( 'NONE', #51247, 4.000000000000001776 ) ;
#56217=DIRECTION ( 'NONE',  ( -0.000000000000000000, -1.000000000000000000, -0.000000000000000000 ) ) ;
#56226=ORIENTED_EDGE ( 'NONE', *, *, #39302, .T. ) ;
#56233=CARTESIAN_POINT ( 'NONE',  ( -4.541265875000002339, 8.937499998634407916, -5.561446717895856393E-16 ) ) ;
#56238=AXIS2_PLACEMENT_3D ( 'NONE', #35895, #72445, #15459 ) ;
#56240=CARTESIAN_POINT ( 'NONE',  ( -7.347880794884122694E-16, 7.750000000000000000, 4.000000000000001776 ) ) ;
#56242=CARTESIAN_POINT ( 'NONE',  ( -4.541265875000003227, 6.874999998634407916, 1.881053915767121110 ) ) ;
#56245=EDGE_CURVE ( 'NONE', #7053, #28042, #56717, .T. ) ;
#56248=CARTESIAN_POINT ( 'NONE',  ( 4.541265875000001451, 22.24999999863440792, 1.881053915767124440 ) ) ;
#56296=CARTESIAN_POINT ( 'NONE',  ( -4.541265875000003227, 21.99999999863440792, 1.881053915767121110 ) ) ;
#56317=CARTESIAN_POINT ( 'NONE',  ( -8.342170076843785083E-16, 8.187499998634406140, 4.541265875000002339 ) ) ;
#56322=CARTESIAN_POINT ( 'NONE',  ( -7.347880794884122694E-16, 4.499999997268813168, 4.000000000000001776 ) ) ;
#56327=CARTESIAN_POINT ( 'NONE',  ( 4.000000000000001776, 11.81249999726881228, -1.656854249492381248 ) ) ;
#56335=CARTESIAN_POINT ( 'NONE',  ( 2.828427124746191623, 12.87499999726881406, -2.828427124746191623 ) ) ;
#56337=CARTESIAN_POINT ( 'NONE',  ( -4.541265875000002339, 6.812499998634407028, -5.561446717895856393E-16 ) ) ;
#56367=CARTESIAN_POINT ( 'NONE',  ( -2.828427124746192067, 7.374999997268813168, 2.828427124746190735 ) ) ;
#56378=CARTESIAN_POINT ( 'NONE',  ( -1.881053915767124440, 10.12499999863440792, 4.541265875000001451 ) ) ;
#56395=CARTESIAN_POINT ( 'NONE',  ( -7.347880794884122694E-16, 14.49999999726881406, 4.000000000000001776 ) ) ;
#56421=CARTESIAN_POINT ( 'NONE',  ( 4.541265875000001451, 14.37499999863440969, 1.881053915767124440 ) ) ;
#56422=VERTEX_POINT ( 'NONE', #28032 ) ;
#56432=DIRECTION ( 'NONE',  ( -0.000000000000000000, -1.000000000000000000, -0.000000000000000000 ) ) ;
#56449=CARTESIAN_POINT ( 'NONE',  ( -3.941655914118860071, 22.00000000000000355, 2.274490667310467451 ) ) ;
#56471=CARTESIAN_POINT ( 'NONE',  ( -3.211159895383561391, 18.68749999863440436, -3.211159895383561835 ) ) ;
#56474=CARTESIAN_POINT ( 'NONE',  ( 2.449293598294707893E-16, 1.250000000000000222, -4.000000000000001776 ) ) ;
#56504=CARTESIAN_POINT ( 'NONE',  ( -7.347880794884122694E-16, 2.750000000000000000, 4.000000000000001776 ) ) ;
#56525=CARTESIAN_POINT ( 'NONE',  ( 2.828427124746190291, 20.87500000000000000, 2.828427124746192067 ) ) ;
#56526=CARTESIAN_POINT ( 'NONE',  ( -8.342170076843785083E-16, 19.06249999863440436, 4.541265875000002339 ) ) ;
#56553=( BOUNDED_CURVE ( )  B_SPLINE_CURVE ( 2, ( #28216, #10868, #16503, #55786, #5215, #15766, #39543, #51225, #74236 ),
 .UNSPECIFIED., .F., .F. ) 
 B_SPLINE_CURVE_WITH_KNOTS ( ( 3, 2, 2, 2, 3 ),
 ( 0.1704545454545454697, 0.1761363636363636742, 0.1818181818181818232, 0.1875000000000000000, 0.1931818181818181768 ),
 .UNSPECIFIED. ) 
 CURVE ( )  GEOMETRIC_REPRESENTATION_ITEM ( )  RATIONAL_B_SPLINE_CURVE ( ( 0.9999999999999996669, 0.9238795325112870716, 1.000000000000000000, 0.9238795325112867385, 1.000000000000000000, 0.9238795325112867385, 1.000000000000000000, 0.9238795325112867385, 1.000000000000000000 ) ) 
 REPRESENTATION_ITEM ( '' )  );
#56569=CARTESIAN_POINT ( 'NONE',  ( 4.000000000000000888, 16.93750000000000000, 1.656854249492384135 ) ) ;
#56591=VERTEX_POINT ( 'NONE', #55615 ) ;
#56612=CARTESIAN_POINT ( 'NONE',  ( -3.211159895383562723, 7.062499998634407028, 3.211159895383561391 ) ) ;
#56618=CARTESIAN_POINT ( 'NONE',  ( 4.000000000000001776, 10.00000000000000000, 0.000000000000000000 ) ) ;
#56619=CARTESIAN_POINT ( 'NONE',  ( -2.828427124746192067, 21.37499999726881583, 2.828427124746190735 ) ) ;
#56620=CARTESIAN_POINT ( 'NONE',  ( -3.211159895383561391, 9.687499998634406140, -3.211159895383561835 ) ) ;
#56627=CARTESIAN_POINT ( 'NONE',  ( -4.541265875000002339, 20.81249999863440436, -5.561446717895856393E-16 ) ) ;
#56666=FACE_OUTER_BOUND ( 'NONE', #66775, .T. ) ;
#56678=( BOUNDED_SURFACE ( )  B_SPLINE_SURFACE ( 1, 2, ( 
 ( #1219, #69868, #46476, #13606, #18915, #41196, #53627, #47942, #41921, #64932, #40821, #12510, #30606, #64575, #63827, #58195, #24198, #52517, #70242, #58927, #18552, #1939, #854, #23839, #24928, #70959, #9085, #61134, #60763, #32481, #66415, #21139, #54371, #71324, #37380, #60012, #67177, #15473, #71692, #44163, #8330, #66797, #3423, #19645, #13967, #38510, #72066, #72458, #55119, #42658, #38133, #26037, #48687, #61512, #65669, #26410, #31340, #72833, #49438, #20384, #32099, #20765, #25299, #9834, #43783, #37010, #9464, #49058, #20011, #53991, #2681, #15100, #25668, #2301, #55489, #43400, #3804, #26802, #48318, #43021, #54745, #66043, #14351, #60382, #49816, #8708, #31723, #3053, #14724, #37764, #4548, #73208, #44910, #21881, #5662, #67915, #40359, #62996, #4183, #68656, #22622, #32861, #68286, #38877, #44535, #46013, #56612, #69034, #45641, #10574, #15844, #57352, #27924, #39247, #61882, #17337, #16583, #28296, #73945, #22246, #74314, #39992, #10205, #5294, #16208, #33985, #21513, #51301, #67546, #50186, #28660, #27169, #39619, #50933, #33604, #33234, #56233, #27543, #63359, #51675, #20, #11320, #62247, #16966, #4927, #50556, #55866, #23007, #10949, #73571, #34353, #45275, #62618, #56980, #31543, #53454, #42481, #53820, #43223, #57727, #59118, #25858, #1773, #2128, #24757, #48138, #69404, #34721, #11685, #42845, #65497, #19837, #19468, #65863, #25120, #54564, #13063, #29039, #70788, #17712, #48880, #71890, #30434, #2871, #40728, #25494, #36838, #52057, #46387, #20203, #30798, #31166, #54193, #63734, #13792, #2500, #6033, #42108, #59844, #48509, #36101, #71146, #392, #71514, #8158, #47767, #7427, #13429, #23375, #7795, #14171, #19103, #65119, #36466, #37205, #59482, #60204, #8528, #66610, #15664, #33422, #44725, #50376, #56421, #55312, #9275, #16038, #44355, #32296, #22069, #26235, #73761, #49639, #61706, #43596, #4743, #32681, #54939, #38705, #20583, #49254, #27736, #21699, #26993, #37580, #60580, #20957, #3620, #31917, #67742, #39069, #55689, #8904, #60957, #14916, #33061, #26616, #9659, #72655, #67366, #4367, #3247, #10027, #73394, #43978, #27360, #62073, #37957, #66990, #56059, #61331, #73023, #38326, #10397, #50747, #21334, #15290, #4003, #72270, #50006, #66239, #14542, #952, #51493, #28854, #10761, #46207, #57550, #45457, #34166, #34914, #22436, #580, #23562, #63933, #5857, #45095, #39436, #28108, #28485, #68107, #11143, #68845, #17158, #51875, #69221, #16401, #57924, #11510, #46573, #22815, #12243, #35280, #6594, #56797, #215, #6232, #29234, #51122, #23194, #33799, #69595, #17907, #34542, #62435, #39799, #68473, #11879, #62805, #63182, #57166, #17531, #52247, #5117, #40548, #40925, #5482, #58292, #29601, #74135, #45832, #63553, #40179, #52615, #16774, #74505, #25023, #30704, #30336, #47312, #41295, #69971, #7699 ),
 ( #7331, #29968, #37109, #60111, #41658, #65770, #52984, #36742, #48042, #64305, #58652, #14072, #42016, #42384, #71051, #12609, #8063, #70691, #18650, #8429, #35637, #19370, #1316, #42753, #65400, #65024, #2036, #53724, #18279, #31446, #24661, #6959, #59023, #70339, #13697, #24301, #54472, #23932, #59752, #53357, #64668, #12969, #36006, #1681, #71419, #47671, #46941, #54092, #19010, #31065, #2403, #13333, #59385, #36369, #25399, #48414, #19746, #38972, #67276, #55219, #60481, #27265, #72559, #9180, #8811, #61978, #61237, #72927, #43882, #66896, #44263, #9929, #31824, #49914, #60859, #3907, #43126, #21237, #37483, #20113, #50283, #71792, #9565, #20863, #3525, #54843, #55590, #15571, #3152, #26899, #38609, #66143, #32199, #61611, #32962, #26140, #15202, #14448, #55966, #32583, #14820, #49161, #26514, #44632, #38232, #4275, #37863, #72168, #20480, #73305, #15944, #43499, #66509, #49540, #21607, #67646, #10303, #33329, #2779, #25766, #48785, #6134, #34451, #74040, #12151, #16305, #63835, #39710, #51774, #33702, #46482, #22720, #45007, #28760, #10670, #39343, #69502, #11785, #17064, #27643, #50650, #11050, #22340, #21978, #34822, #29140, #45736, #73670, #51029, #5024, #23099, #45365, #74412, #68381, #57453, #69130, #68012, #5760, #40458, #16680, #17436, #63457, #56707, #34079, #120, #51398, #63090, #28390, #46111, #57828, #11416, #62711, #28020, #62340, #57075, #40086, #5389, #56327, #68750, #52156, #491, #23471, #17812, #4649, #40829, #24935, #12516, #65310, #13611, #53999, #70604, #35186, #29512, #18187, #18557, #58200, #1225, #58934, #7240, #18922, #36281, #6505, #47952, #1591, #36650, #12878, #2310, #25307, #71331, #46852, #41928, #70968, #19282, #48324, #24576, #23845, #7606, #64211, #69875, #19652, #59660, #64937, #52522, #859, #64582, #52893, #41203, #7976, #30978, #47581, #35548, #29879, #58563, #1946, #24204, #53265, #47215, #13248, #42293, #6867, #59297, #42665, #70248, #65676, #41568, #35914, #30244, #30613, #53636, #20773, #60769, #38142, #15110, #43792, #20394, #37391, #31350, #60019, #72465, #8338, #44544, #43408, #66808, #3430, #49447, #49824, #13975, #3062, #3812, #66051, #44170, #67184, #32868, #61142, #37017, #54380, #71701, #72077, #2689, #54752, #37773, #9095, #9472, #32489, #25675, #26810, #55127, #15481, #66422, #55873, #4189, #50195, #48695, #55500, #72841, #21148, #20019, #38517, #61520, #43029, #9842, #27178, #14359, #14734, #73214, #21522, #60392, #26421, #8718, #31730, #26045, #49065, #32109, #68291, #34729, #62626, #51681, #4934, #44916, #4556, #10957, #6039, #33612, #67923, #16216, #16973, #57734, #46020, #26, #29044, #56619, #10581, #17344, #45647, #27931, #23379, #27551, #400, #50939, #63002, #39256, #73579, #52063, #51310, #11326, #33992, #56986, #34358, #23013, #21887, #39999, #73950, #68662 ) ),
 .UNSPECIFIED., .F., .F., .F. ) 
 B_SPLINE_SURFACE_WITH_KNOTS ( ( 2, 2 ),
 ( 3, 2, 2, 2, 2, 2, 2, 2, 2, 2, 2, 2, 2, 2, 2, 2, 2, 2, 2, 2, 2, 2, 2, 2, 2, 2, 2, 2, 2, 2, 2, 2, 2, 2, 2, 2, 2, 2, 2, 2, 2, 2, 2, 2, 2, 2, 2, 2, 2, 2, 2, 2, 2, 2, 2, 2, 2, 2, 2, 2, 2, 2, 2, 2, 2, 2, 2, 2, 2, 2, 2, 2, 2, 2, 2, 2, 2, 2, 2, 2, 2, 2, 2, 2, 2, 2, 2, 2, 2, 2, 2, 2, 2, 2, 2, 2, 2, 2, 2, 2, 2, 2, 2, 2, 2, 2, 2, 2, 2, 2, 2, 2, 2, 2, 2, 2, 2, 2, 2, 2, 2, 2, 2, 2, 2, 2, 2, 2, 2, 2, 2, 2, 2, 2, 2, 2, 2, 2, 2, 2, 2, 2, 2, 2, 2, 2, 2, 2, 2, 2, 2, 2, 2, 2, 2, 2, 2, 2, 2, 2, 2, 2, 2, 2, 2, 2, 2, 2, 2, 2, 2, 2, 2, 2, 2, 2, 3 ),
 ( 0.000000000000000000, 1.000000000000000000 ),
 ( 0.000000000000000000, 0.005681818181818181976, 0.01136363636363636395, 0.01704545454545454419, 0.02272727272727272790, 0.02840909090909090814, 0.03409090909090908839, 0.03977272727272727210, 0.04545454545454545581, 0.05113636363636363952, 0.05681818181818181629, 0.06250000000000000000, 0.06818181818181817677, 0.07386363636363636742, 0.07954545454545454419, 0.08522727272727272096, 0.09090909090909091161, 0.09659090909090908839, 0.1022727272727272790, 0.1079545454545454558, 0.1136363636363636326, 0.1193181818181818232, 0.1250000000000000000, 0.1306818181818181768, 0.1363636363636363535, 0.1420454545454545581, 0.1477272727272727348, 0.1534090909090909116, 0.1590909090909090884, 0.1647727272727272652, 0.1704545454545454419, 0.1761363636363636465, 0.1818181818181818232, 0.1875000000000000000, 0.1931818181818181768, 0.1988636363636363535, 0.2045454545454545581, 0.2102272727272727348, 0.2159090909090909116, 0.2215909090909090884, 0.2272727272727272652, 0.2329545454545454419, 0.2386363636363636465, 0.2443181818181818232, 0.2500000000000000000, 0.2556818181818181768, 0.2613636363636363535, 0.2670454545454545303, 0.2727272727272727071, 0.2784090909090908839, 0.2840909090909091161, 0.2897727272727272929, 0.2954545454545454697, 0.3011363636363636465, 0.3068181818181818232, 0.3125000000000000000, 0.3181818181818181768, 0.3238636363636363535, 0.3295454545454545303, 0.3352272727272727071, 0.3409090909090908839, 0.3465909090909091161, 0.3522727272727272929, 0.3579545454545454697, 0.3636363636363636465, 0.3693181818181818232, 0.3750000000000000000, 0.3806818181818181768, 0.3863636363636363535, 0.3920454545454545303, 0.3977272727272727071, 0.4034090909090908839, 0.4090909090909091161, 0.4147727272727272929, 0.4204545454545454697, 0.4261363636363636465, 0.4318181818181818232, 0.4375000000000000000, 0.4431818181818181768, 0.4488636363636363535, 0.4545454545454545303, 0.4602272727272727071, 0.4659090909090908839, 0.4715909090909091161, 0.4772727272727272929, 0.4829545454545454697, 0.4886363636363636465, 0.4943181818181818232, 0.5000000000000000000, 0.5056818181818182323, 0.5113636363636363535, 0.5170454545454545858, 0.5227272727272727071, 0.5284090909090909394, 0.5340909090909090606, 0.5397727272727272929, 0.5454545454545454142, 0.5511363636363636465, 0.5568181818181817677, 0.5625000000000000000, 0.5681818181818182323, 0.5738636363636363535, 0.5795454545454545858, 0.5852272727272727071, 0.5909090909090909394, 0.5965909090909090606, 0.6022727272727272929, 0.6079545454545454142, 0.6136363636363636465, 0.6193181818181817677, 0.6250000000000000000, 0.6306818181818182323, 0.6363636363636363535, 0.6420454545454545858, 0.6477272727272727071, 0.6534090909090909394, 0.6590909090909090606, 0.6647727272727272929, 0.6704545454545454142, 0.6761363636363636465, 0.6818181818181817677, 0.6875000000000000000, 0.6931818181818182323, 0.6988636363636363535, 0.7045454545454545858, 0.7102272727272727071, 0.7159090909090909394, 0.7215909090909090606, 0.7272727272727272929, 0.7329545454545454142, 0.7386363636363636465, 0.7443181818181817677, 0.7500000000000000000, 0.7556818181818182323, 0.7613636363636363535, 0.7670454545454545858, 0.7727272727272727071, 0.7784090909090909394, 0.7840909090909090606, 0.7897727272727272929, 0.7954545454545454142, 0.8011363636363636465, 0.8068181818181817677, 0.8125000000000000000, 0.8181818181818182323, 0.8238636363636363535, 0.8295454545454545858, 0.8352272727272727071, 0.8409090909090909394, 0.8465909090909090606, 0.8522727272727272929, 0.8579545454545454142, 0.8636363636363636465, 0.8693181818181817677, 0.8750000000000000000, 0.8806818181818182323, 0.8863636363636363535, 0.8920454545454545858, 0.8977272727272727071, 0.9034090909090909394, 0.9090909090909090606, 0.9147727272727272929, 0.9204545454545454142, 0.9261363636363636465, 0.9318181818181817677, 0.9375000000000000000, 0.9431818181818182323, 0.9488636363636363535, 0.9545454545454545858, 0.9602272727272727071, 0.9659090909090909394, 0.9715909090909090606, 0.9772727272727272929, 0.9829545454545454142, 0.9886363636363636465, 0.9943181818181817677, 1.000000000000000000 ),
 .UNSPECIFIED. ) 
 GEOMETRIC_REPRESENTATION_ITEM ( )  RATIONAL_B_SPLINE_SURFACE ( (
 ( 1.000000000000000000, 0.9238795325112867385, 1.000000000000000000, 0.9238795325112867385, 1.000000000000000000, 0.9238795325112867385, 1.000000000000000000, 0.9238795325112867385, 1.000000000000000000, 0.9238795325112867385, 1.000000000000000000, 0.9238795325112867385, 1.000000000000000000, 0.9238795325112867385, 1.000000000000000000, 0.9238795325112867385, 1.000000000000000000, 0.9238795325112867385, 1.000000000000000000, 0.9238795325112867385, 1.000000000000000000, 0.9238795325112867385, 1.000000000000000000, 0.9238795325112867385, 1.000000000000000000, 0.9238795325112867385, 1.000000000000000000, 0.9238795325112867385, 1.000000000000000000, 0.9238795325112867385, 1.000000000000000000, 0.9238795325112867385, 1.000000000000000000, 0.9238795325112867385, 1.000000000000000000, 0.9238795325112867385, 1.000000000000000000, 0.9238795325112867385, 1.000000000000000000, 0.9238795325112867385, 1.000000000000000000, 0.9238795325112867385, 1.000000000000000000, 0.9238795325112867385, 1.000000000000000000, 0.9238795325112867385, 1.000000000000000000, 0.9238795325112867385, 1.000000000000000000, 0.9238795325112867385, 1.000000000000000000, 0.9238795325112867385, 1.000000000000000000, 0.9238795325112867385, 1.000000000000000000, 0.9238795325112867385, 1.000000000000000000, 0.9238795325112867385, 1.000000000000000000, 0.9238795325112867385, 1.000000000000000000, 0.9238795325112867385, 1.000000000000000000, 0.9238795325112867385, 1.000000000000000000, 0.9238795325112867385, 1.000000000000000000, 0.9238795325112867385, 1.000000000000000000, 0.9238795325112867385, 1.000000000000000000, 0.9238795325112867385, 1.000000000000000000, 0.9238795325112867385, 1.000000000000000000, 0.9238795325112867385, 1.000000000000000000, 0.9238795325112867385, 1.000000000000000000, 0.9238795325112867385, 1.000000000000000000, 0.9238795325112867385, 1.000000000000000000, 0.9238795325112867385, 1.000000000000000000, 0.9238795325112867385, 1.000000000000000000, 0.9238795325112867385, 1.000000000000000000, 0.9238795325112867385, 1.000000000000000000, 0.9238795325112867385, 1.000000000000000000, 0.9238795325112867385, 1.000000000000000000, 0.9238795325112867385, 1.000000000000000000, 0.9238795325112867385, 1.000000000000000000, 0.9238795325112867385, 1.000000000000000000, 0.9238795325112867385, 1.000000000000000000, 0.9238795325112867385, 1.000000000000000000, 0.9238795325112867385, 1.000000000000000000, 0.9238795325112867385, 1.000000000000000000, 0.9238795325112867385, 1.000000000000000000, 0.9238795325112867385, 1.000000000000000000, 0.9238795325112867385, 1.000000000000000000, 0.9238795325112867385, 1.000000000000000000, 0.9238795325112867385, 1.000000000000000000, 0.9238795325112867385, 1.000000000000000000, 0.9238795325112867385, 1.000000000000000000, 0.9238795325112867385, 1.000000000000000000, 0.9238795325112867385, 1.000000000000000000, 0.9238795325112867385, 1.000000000000000000, 0.9238795325112867385, 1.000000000000000000, 0.9238795325112867385, 1.000000000000000000, 0.9238795325112867385, 1.000000000000000000, 0.9238795325112867385, 1.000000000000000000, 0.9238795325112867385, 1.000000000000000000, 0.9238795325112867385, 1.000000000000000000, 0.9238795325112867385, 1.000000000000000000, 0.9238795325112867385, 1.000000000000000000, 0.9238795325112867385, 1.000000000000000000, 0.9238795325112867385, 1.000000000000000000, 0.9238795325112867385, 1.000000000000000000, 0.9238795325112867385, 1.000000000000000000, 0.9238795325112867385, 1.000000000000000000, 0.9238795325112867385, 1.000000000000000000, 0.9238795325112867385, 1.000000000000000000, 0.9238795325112867385, 1.000000000000000000, 0.9238795325112867385, 1.000000000000000000, 0.9238795325112867385, 1.000000000000000000, 0.9238795325112867385, 1.000000000000000000, 0.9238795325112867385, 1.000000000000000000, 0.9238795325112867385, 1.000000000000000000, 0.9238795325112867385, 1.000000000000000000, 0.9238795325112867385, 1.000000000000000000, 0.9238795325112867385, 1.000000000000000000, 0.9238795325112867385, 1.000000000000000000, 0.9238795325112867385, 1.000000000000000000, 0.9238795325112867385, 1.000000000000000000, 0.9238795325112867385, 1.000000000000000000, 0.9238795325112867385, 1.000000000000000000, 0.9238795325112867385, 1.000000000000000000, 0.9238795325112867385, 1.000000000000000000, 0.9238795325112867385, 1.000000000000000000, 0.9238795325112867385, 1.000000000000000000, 0.9238795325112867385, 1.000000000000000000, 0.9238795325112867385, 1.000000000000000000, 0.9238795325112867385, 1.000000000000000000, 0.9238795325112867385, 1.000000000000000000, 0.9238795325112867385, 1.000000000000000000, 0.9238795325112867385, 1.000000000000000000, 0.9238795325112867385, 1.000000000000000000, 0.9238795325112867385, 1.000000000000000000, 0.9238795325112867385, 1.000000000000000000, 0.9238795325112867385, 1.000000000000000000, 0.9238795325112867385, 1.000000000000000000, 0.9238795325112867385, 1.000000000000000000, 0.9238795325112867385, 1.000000000000000000, 0.9238795325112867385, 1.000000000000000000, 0.9238795325112867385, 1.000000000000000000, 0.9238795325112867385, 1.000000000000000000, 0.9238795325112867385, 1.000000000000000000, 0.9238795325112867385, 1.000000000000000000, 0.9238795325112867385, 1.000000000000000000, 0.9238795325112867385, 1.000000000000000000, 0.9238795325112867385, 1.000000000000000000, 0.9238795325112867385, 1.000000000000000000, 0.9238795325112867385, 1.000000000000000000, 0.9238795325112867385, 1.000000000000000000, 0.9238795325112867385, 1.000000000000000000, 0.9238795325112867385, 1.000000000000000000, 0.9238795325112867385, 1.000000000000000000, 0.9238795325112867385, 1.000000000000000000, 0.9238795325112867385, 1.000000000000000000, 0.9238795325112867385, 1.000000000000000000, 0.9238795325112867385, 1.000000000000000000, 0.9238795325112867385, 1.000000000000000000, 0.9238795325112867385, 1.000000000000000000, 0.9238795325112867385, 1.000000000000000000, 0.9238795325112867385, 1.000000000000000000, 0.9238795325112867385, 1.000000000000000000, 0.9238795325112867385, 1.000000000000000000, 0.9238795325112867385, 1.000000000000000000, 0.9238795325112867385, 1.000000000000000000, 0.9238795325112867385, 1.000000000000000000, 0.9238795325112867385, 1.000000000000000000, 0.9238795325112867385, 1.000000000000000000, 0.9238795325112867385, 1.000000000000000000, 0.9238795325112867385, 1.000000000000000000, 0.9238795325112867385, 1.000000000000000000, 0.9238795325112867385, 1.000000000000000000, 0.9238795325112867385, 1.000000000000000000, 0.9238795325112867385, 1.000000000000000000, 0.9238795325112867385, 1.000000000000000000, 0.9238795325112867385, 1.000000000000000000, 0.9238795325112867385, 1.000000000000000000, 0.9238795325112867385, 1.000000000000000000, 0.9238795325112867385, 1.000000000000000000, 0.9238795325112867385, 1.000000000000000000, 0.9238795325112867385, 1.000000000000000000, 0.9238795325112867385, 1.000000000000000000, 0.9238795325112867385, 1.000000000000000000, 0.9238795325112867385, 1.000000000000000000, 0.9238795325112867385, 1.000000000000000000, 0.9238795325112867385, 1.000000000000000000, 0.9238795325112867385, 1.000000000000000000, 0.9238795325112867385, 1.000000000000000000, 0.9238795325112867385, 1.000000000000000000, 0.9238795325112867385, 1.000000000000000000, 0.9238795325112867385, 1.000000000000000000, 0.9238795325112867385, 1.000000000000000000, 0.9238795325112867385, 1.000000000000000000, 0.9238795325112867385, 1.000000000000000000, 0.9238795325112867385, 1.000000000000000000, 0.9238795325112867385, 1.000000000000000000, 0.9238795325112867385, 1.000000000000000000, 0.9238795325112867385, 1.000000000000000000, 0.9238795325112867385, 1.000000000000000000, 0.9238795325112867385, 1.000000000000000000, 0.9238795325112867385, 1.000000000000000000, 0.9238795325112867385, 1.000000000000000000, 0.9238795325112867385, 1.000000000000000000, 0.9238795325112867385, 1.000000000000000000, 0.9238795325112867385, 1.000000000000000000),
 ( 1.000000000000000000, 0.9238795325112867385, 1.000000000000000000, 0.9238795325112867385, 1.000000000000000000, 0.9238795325112867385, 1.000000000000000000, 0.9238795325112867385, 1.000000000000000000, 0.9238795325112867385, 1.000000000000000000, 0.9238795325112867385, 1.000000000000000000, 0.9238795325112867385, 1.000000000000000000, 0.9238795325112867385, 1.000000000000000000, 0.9238795325112867385, 1.000000000000000000, 0.9238795325112867385, 1.000000000000000000, 0.9238795325112867385, 1.000000000000000000, 0.9238795325112867385, 1.000000000000000000, 0.9238795325112867385, 1.000000000000000000, 0.9238795325112867385, 1.000000000000000000, 0.9238795325112867385, 1.000000000000000000, 0.9238795325112867385, 1.000000000000000000, 0.9238795325112867385, 1.000000000000000000, 0.9238795325112867385, 1.000000000000000000, 0.9238795325112867385, 1.000000000000000000, 0.9238795325112867385, 1.000000000000000000, 0.9238795325112867385, 1.000000000000000000, 0.9238795325112867385, 1.000000000000000000, 0.9238795325112867385, 1.000000000000000000, 0.9238795325112867385, 1.000000000000000000, 0.9238795325112867385, 1.000000000000000000, 0.9238795325112867385, 1.000000000000000000, 0.9238795325112867385, 1.000000000000000000, 0.9238795325112867385, 1.000000000000000000, 0.9238795325112867385, 1.000000000000000000, 0.9238795325112867385, 1.000000000000000000, 0.9238795325112867385, 1.000000000000000000, 0.9238795325112867385, 1.000000000000000000, 0.9238795325112867385, 1.000000000000000000, 0.9238795325112867385, 1.000000000000000000, 0.9238795325112867385, 1.000000000000000000, 0.9238795325112867385, 1.000000000000000000, 0.9238795325112867385, 1.000000000000000000, 0.9238795325112867385, 1.000000000000000000, 0.9238795325112867385, 1.000000000000000000, 0.9238795325112867385, 1.000000000000000000, 0.9238795325112867385, 1.000000000000000000, 0.9238795325112867385, 1.000000000000000000, 0.9238795325112867385, 1.000000000000000000, 0.9238795325112867385, 1.000000000000000000, 0.9238795325112867385, 1.000000000000000000, 0.9238795325112867385, 1.000000000000000000, 0.9238795325112867385, 1.000000000000000000, 0.9238795325112867385, 1.000000000000000000, 0.9238795325112867385, 1.000000000000000000, 0.9238795325112867385, 1.000000000000000000, 0.9238795325112867385, 1.000000000000000000, 0.9238795325112867385, 1.000000000000000000, 0.9238795325112867385, 1.000000000000000000, 0.9238795325112867385, 1.000000000000000000, 0.9238795325112867385, 1.000000000000000000, 0.9238795325112867385, 1.000000000000000000, 0.9238795325112867385, 1.000000000000000000, 0.9238795325112867385, 1.000000000000000000, 0.9238795325112867385, 1.000000000000000000, 0.9238795325112867385, 1.000000000000000000, 0.9238795325112867385, 1.000000000000000000, 0.9238795325112867385, 1.000000000000000000, 0.9238795325112867385, 1.000000000000000000, 0.9238795325112867385, 1.000000000000000000, 0.9238795325112867385, 1.000000000000000000, 0.9238795325112867385, 1.000000000000000000, 0.9238795325112867385, 1.000000000000000000, 0.9238795325112867385, 1.000000000000000000, 0.9238795325112867385, 1.000000000000000000, 0.9238795325112867385, 1.000000000000000000, 0.9238795325112867385, 1.000000000000000000, 0.9238795325112867385, 1.000000000000000000, 0.9238795325112867385, 1.000000000000000000, 0.9238795325112867385, 1.000000000000000000, 0.9238795325112867385, 1.000000000000000000, 0.9238795325112867385, 1.000000000000000000, 0.9238795325112867385, 1.000000000000000000, 0.9238795325112867385, 1.000000000000000000, 0.9238795325112867385, 1.000000000000000000, 0.9238795325112867385, 1.000000000000000000, 0.9238795325112867385, 1.000000000000000000, 0.9238795325112867385, 1.000000000000000000, 0.9238795325112867385, 1.000000000000000000, 0.9238795325112867385, 1.000000000000000000, 0.9238795325112867385, 1.000000000000000000, 0.9238795325112867385, 1.000000000000000000, 0.9238795325112867385, 1.000000000000000000, 0.9238795325112867385, 1.000000000000000000, 0.9238795325112867385, 1.000000000000000000, 0.9238795325112867385, 1.000000000000000000, 0.9238795325112867385, 1.000000000000000000, 0.9238795325112867385, 1.000000000000000000, 0.9238795325112867385, 1.000000000000000000, 0.9238795325112867385, 1.000000000000000000, 0.9238795325112867385, 1.000000000000000000, 0.9238795325112867385, 1.000000000000000000, 0.9238795325112867385, 1.000000000000000000, 0.9238795325112867385, 1.000000000000000000, 0.9238795325112867385, 1.000000000000000000, 0.9238795325112867385, 1.000000000000000000, 0.9238795325112867385, 1.000000000000000000, 0.9238795325112867385, 1.000000000000000000, 0.9238795325112867385, 1.000000000000000000, 0.9238795325112867385, 1.000000000000000000, 0.9238795325112867385, 1.000000000000000000, 0.9238795325112867385, 1.000000000000000000, 0.9238795325112867385, 1.000000000000000000, 0.9238795325112867385, 1.000000000000000000, 0.9238795325112867385, 1.000000000000000000, 0.9238795325112867385, 1.000000000000000000, 0.9238795325112867385, 1.000000000000000000, 0.9238795325112867385, 1.000000000000000000, 0.9238795325112867385, 1.000000000000000000, 0.9238795325112867385, 1.000000000000000000, 0.9238795325112867385, 1.000000000000000000, 0.9238795325112867385, 1.000000000000000000, 0.9238795325112867385, 1.000000000000000000, 0.9238795325112867385, 1.000000000000000000, 0.9238795325112867385, 1.000000000000000000, 0.9238795325112867385, 1.000000000000000000, 0.9238795325112867385, 1.000000000000000000, 0.9238795325112867385, 1.000000000000000000, 0.9238795325112867385, 1.000000000000000000, 0.9238795325112867385, 1.000000000000000000, 0.9238795325112867385, 1.000000000000000000, 0.9238795325112867385, 1.000000000000000000, 0.9238795325112867385, 1.000000000000000000, 0.9238795325112867385, 1.000000000000000000, 0.9238795325112867385, 1.000000000000000000, 0.9238795325112867385, 1.000000000000000000, 0.9238795325112867385, 1.000000000000000000, 0.9238795325112867385, 1.000000000000000000, 0.9238795325112867385, 1.000000000000000000, 0.9238795325112867385, 1.000000000000000000, 0.9238795325112867385, 1.000000000000000000, 0.9238795325112867385, 1.000000000000000000, 0.9238795325112867385, 1.000000000000000000, 0.9238795325112867385, 1.000000000000000000, 0.9238795325112867385, 1.000000000000000000, 0.9238795325112867385, 1.000000000000000000, 0.9238795325112867385, 1.000000000000000000, 0.9238795325112867385, 1.000000000000000000, 0.9238795325112867385, 1.000000000000000000, 0.9238795325112867385, 1.000000000000000000, 0.9238795325112867385, 1.000000000000000000, 0.9238795325112867385, 1.000000000000000000, 0.9238795325112867385, 1.000000000000000000, 0.9238795325112867385, 1.000000000000000000, 0.9238795325112867385, 1.000000000000000000, 0.9238795325112867385, 1.000000000000000000, 0.9238795325112867385, 1.000000000000000000, 0.9238795325112867385, 1.000000000000000000, 0.9238795325112867385, 1.000000000000000000, 0.9238795325112867385, 1.000000000000000000, 0.9238795325112867385, 1.000000000000000000, 0.9238795325112867385, 1.000000000000000000, 0.9238795325112867385, 1.000000000000000000, 0.9238795325112867385, 1.000000000000000000, 0.9238795325112867385, 1.000000000000000000, 0.9238795325112867385, 1.000000000000000000, 0.9238795325112867385, 1.000000000000000000, 0.9238795325112867385, 1.000000000000000000, 0.9238795325112867385, 1.000000000000000000, 0.9238795325112867385, 1.000000000000000000, 0.9238795325112867385, 1.000000000000000000, 0.9238795325112867385, 1.000000000000000000, 0.9238795325112867385, 1.000000000000000000, 0.9238795325112867385, 1.000000000000000000, 0.9238795325112867385, 1.000000000000000000, 0.9238795325112867385, 1.000000000000000000, 0.9238795325112867385, 1.000000000000000000, 0.9238795325112867385, 1.000000000000000000, 0.9238795325112867385, 1.000000000000000000, 0.9238795325112867385, 1.000000000000000000, 0.9238795325112867385, 1.000000000000000000, 0.9238795325112867385, 1.000000000000000000) ) ) 
 REPRESENTATION_ITEM ( '' )  SURFACE ( )  );
#56696=( BOUNDED_CURVE ( )  B_SPLINE_CURVE ( 2, ( #1787, #25876, #19119, #18762, #59137, #64777, #42499, #48895, #71908 ),
 .UNSPECIFIED., .F., .F. ) 
 B_SPLINE_CURVE_WITH_KNOTS ( ( 3, 2, 2, 2, 3 ),
 ( 0.6477272727272727071, 0.6534090909090909394, 0.6590909090909091717, 0.6647727272727274039, 0.6704545454545455252 ),
 .UNSPECIFIED. ) 
 CURVE ( )  GEOMETRIC_REPRESENTATION_ITEM ( )  RATIONAL_B_SPLINE_CURVE ( ( 1.000000000000000000, 0.9238795325112867385, 1.000000000000000000, 0.9238795325112867385, 1.000000000000000000, 0.9238795325112867385, 1.000000000000000000, 0.9238795325112852952, 1.000000000000001554 ) ) 
 REPRESENTATION_ITEM ( '' )  );
#56697=CARTESIAN_POINT ( 'NONE',  ( 1.881053915767122664, 11.24999999863441147, 4.541265875000001451 ) ) ;
#56707=CARTESIAN_POINT ( 'NONE',  ( 2.828427124746191623, 10.87499999726881406, -2.828427124746191623 ) ) ;
#56713=CARTESIAN_POINT ( 'NONE',  ( 4.541265875000002339, 10.37499999863440792, -1.881053915767121554 ) ) ;
#56714=CARTESIAN_POINT ( 'NONE',  ( 1.656854249492381248, 0.1875000000000001943, -4.000000000000001776 ) ) ;
#56717=LINE ( 'NONE', #5773, #40970 ) ;
#56728=ORIENTED_EDGE ( 'NONE', *, *, #41486, .F. ) ;
#56754=CARTESIAN_POINT ( 'NONE',  ( 2.780723358947928197E-16, 13.68749999863440614, -4.541265875000002339 ) ) ;
#56773=VERTEX_POINT ( 'NONE', #6158 ) ;
#56783=CARTESIAN_POINT ( 'NONE',  ( -8.342170076843785083E-16, 1.187499998634406806, 4.541265875000002339 ) ) ;
#56797=CARTESIAN_POINT ( 'NONE',  ( -3.211159895383562723, 20.06249999863440436, 3.211159895383561391 ) ) ;
#56841=CARTESIAN_POINT ( 'NONE',  ( -3.211159895383562723, 17.93749999863440792, 3.211159895383561391 ) ) ;
#56844=CARTESIAN_POINT ( 'NONE',  ( 2.449293598294707893E-16, 11.99999999726881406, -4.000000000000001776 ) ) ;
#56865=CARTESIAN_POINT ( 'NONE',  ( 2.449293598294707893E-16, 16.25000000000000000, -4.000000000000001776 ) ) ;
#56898=CARTESIAN_POINT ( 'NONE',  ( 4.000000000000001776, 21.00000000000000000, 0.000000000000000000 ) ) ;
#56900=CARTESIAN_POINT ( 'NONE',  ( -8.342170076843785083E-16, 18.06249999863440792, 4.541265875000002339 ) ) ;
#56933=CARTESIAN_POINT ( 'NONE',  ( 4.000000000000000888, 16.68749999726881583, 1.656854249492384135 ) ) ;
#56955=VECTOR ( 'NONE', #7111, 1000.000000000000000 ) ;
#56980=CARTESIAN_POINT ( 'NONE',  ( -4.541265875000003227, 9.999999998634407916, 1.881053915767121110 ) ) ;
#56985=CARTESIAN_POINT ( 'NONE',  ( 4.000000000000000888, 7.937500000000000888, 1.656854249492384135 ) ) ;
#56986=CARTESIAN_POINT ( 'NONE',  ( -2.828427124746192067, 22.37499999726881583, 2.828427124746190735 ) ) ;
#56987=CARTESIAN_POINT ( 'NONE',  ( 3.211159895383560947, 6.187499998634407028, 3.211159895383562723 ) ) ;
#56995=CARTESIAN_POINT ( 'NONE',  ( -3.211159895383562723, 21.93749999863440792, 3.211159895383561391 ) ) ;
#57012=CARTESIAN_POINT ( 'NONE',  ( 4.898587196589415787E-16, 0.000000000000000000, 4.000000000000001776 ) ) ;
#57048=ORIENTED_EDGE ( 'NONE', *, *, #12218, .F. ) ;
#57065=CARTESIAN_POINT ( 'NONE',  ( 2.780723358947928197E-16, 13.68749999863440614, -4.541265875000002339 ) ) ;
#57075=CARTESIAN_POINT ( 'NONE',  ( 2.828427124746190291, 11.62499999726881406, 2.828427124746192067 ) ) ;
#57081=CARTESIAN_POINT ( 'NONE',  ( -1.881053915767121554, 9.624999998634404363, -4.541265875000002339 ) ) ;
#57125=CARTESIAN_POINT ( 'NONE',  ( -1.881053915767124440, 14.12499999863440969, 4.541265875000001451 ) ) ;
#57154=CARTESIAN_POINT ( 'NONE',  ( 4.541265875000002339, 0.4374999986344068059, 0.000000000000000000 ) ) ;
#57166=CARTESIAN_POINT ( 'NONE',  ( -3.211159895383562723, 21.06249999863440792, 3.211159895383561391 ) ) ;
#57205=ORIENTED_EDGE ( 'NONE', *, *, #73800, .F. ) ;
#57206=CARTESIAN_POINT ( 'NONE',  ( 4.000000000000001776, 2.062500000000000000, -1.656854249492381248 ) ) ;
#57213=CARTESIAN_POINT ( 'NONE',  ( 4.541265875000001451, 22.24999999863440792, 1.881053915767124440 ) ) ;
#57223=AXIS2_PLACEMENT_3D ( 'NONE', #8751, #13643, #1975 ) ;
#57256=EDGE_LOOP ( 'NONE', ( #67350, #11239, #45162, #71714 ) ) ;
#57271=CARTESIAN_POINT ( 'NONE',  ( 4.000000000000001776, 20.00000000000000000, 0.000000000000000000 ) ) ;
#57284=ADVANCED_FACE ( 'NONE', ( #62648 ), #6445, .T. ) ;
#57308=DIRECTION ( 'NONE',  ( -0.000000000000000000, -1.000000000000000000, -0.000000000000000000 ) ) ;
#57310=CARTESIAN_POINT ( 'NONE',  ( 4.541265875000002339, 10.31249999863440792, 0.000000000000000000 ) ) ;
#57352=CARTESIAN_POINT ( 'NONE',  ( 4.541265875000001451, 7.374999998634408804, 1.881053915767124440 ) ) ;
#57354=AXIS2_PLACEMENT_3D ( 'NONE', #63097, #11422, #34459 ) ;
#57358=CARTESIAN_POINT ( 'NONE',  ( 4.000000000000001776, 7.062500000000000000, -1.656854249492381248 ) ) ;
#57360=CARTESIAN_POINT ( 'NONE',  ( 2.780723358947928197E-16, 11.56249999863440614, -4.541265875000002339 ) ) ;
#57369=CARTESIAN_POINT ( 'NONE',  ( -1.881053915767124440, 20.99999999863440792, 4.541265875000001451 ) ) ;
#57387=EDGE_CURVE ( 'NONE', #45255, #57513, #29074, .T. ) ;
#57441=CARTESIAN_POINT ( 'NONE',  ( -3.211159895383561391, 12.81249999863440792, -3.211159895383561835 ) ) ;
#57453=CARTESIAN_POINT ( 'NONE',  ( -2.828427124746192067, 10.37499999726881406, 2.828427124746190735 ) ) ;
#57463=CARTESIAN_POINT ( 'NONE',  ( -1.881053915767121554, 11.62499999863440969, -4.541265875000002339 ) ) ;
#57482=EDGE_CURVE ( 'NONE', #23575, #52476, #19221, .T. ) ;
#57497=ORIENTED_EDGE ( 'NONE', *, *, #55810, .T. ) ;
#57509=CARTESIAN_POINT ( 'NONE',  ( -4.541265875000002339, 10.87499999863440792, -1.881053915767121998 ) ) ;
#57513=VERTEX_POINT ( 'NONE', #36216 ) ;
#57537=CARTESIAN_POINT ( 'NONE',  ( -4.541265875000002339, 1.937499998634406806, -5.561446717895856393E-16 ) ) ;
#57549=CARTESIAN_POINT ( 'NONE',  ( 4.000000000000000888, 2.937500000000000000, 1.656854249492384135 ) ) ;
#57550=CARTESIAN_POINT ( 'NONE',  ( 4.541265875000001451, 18.37499999863441147, 1.881053915767124440 ) ) ;
#57576=CARTESIAN_POINT ( 'NONE',  ( 0.000000000000000000, 0.000000000000000000, -4.000000000000001776 ) ) ;
#57592=CARTESIAN_POINT ( 'NONE',  ( 4.541265875000001451, 2.374999998634407028, 1.881053915767124440 ) ) ;
#57599=CARTESIAN_POINT ( 'NONE',  ( 2.828427124746191623, 15.87499999726881406, -2.828427124746191623 ) ) ;
#57615=VERTEX_POINT ( 'NONE', #35849 ) ;
#57645=( GEOMETRIC_REPRESENTATION_CONTEXT ( 3 ) GLOBAL_UNCERTAINTY_ASSIGNED_CONTEXT ( ( #29498 ) ) GLOBAL_UNIT_ASSIGNED_CONTEXT ( ( #16824, #33846, #40600 ) ) REPRESENTATION_CONTEXT ( 'NONE', 'WORKASPACE' ) );
#57649=CARTESIAN_POINT ( 'NONE',  ( -1.881053915767121554, 3.624999998634406584, -4.541265875000002339 ) ) ;
#57666=CARTESIAN_POINT ( 'NONE',  ( 4.000000000000001776, 21.06250000000000000, -1.656854249492381248 ) ) ;
#57683=CARTESIAN_POINT ( 'NONE',  ( -7.347880794884122694E-16, 15.75000000000000000, 4.000000000000001776 ) ) ;
#57685=CARTESIAN_POINT ( 'NONE',  ( 4.541265875000001451, 9.249999998634406140, 1.881053915767124440 ) ) ;
#57713=CYLINDRICAL_SURFACE ( 'NONE', #40756, 4.000000000000001776 ) ;
#57717=CARTESIAN_POINT ( 'NONE',  ( 4.000000000000000888, 21.68749999726881583, 1.656854249492384135 ) ) ;
#57727=CARTESIAN_POINT ( 'NONE',  ( 4.541265875000001451, 10.37499999863440792, 1.881053915767124440 ) ) ;
#57733=CARTESIAN_POINT ( 'NONE',  ( -4.000000000000002665, 11.56249999999999822, 1.656854249492380804 ) ) ;
#57734=CARTESIAN_POINT ( 'NONE',  ( -2.828427124746190735, 21.12499999726881583, -2.828427124746191623 ) ) ;
#57735=CARTESIAN_POINT ( 'NONE',  ( 4.541265875000002339, 10.37499999863440969, -1.881053915767121776 ) ) ;
#57746=CARTESIAN_POINT ( 'NONE',  ( 4.541265875000001451, 21.24999999863440436, 1.881053915767124440 ) ) ;
#57749=VERTEX_POINT ( 'NONE', #48627 ) ;
#57773=( BOUNDED_CURVE ( )  B_SPLINE_CURVE ( 2, ( #73383, #50737, #43968, #67730, #32668, #33411, #10385, #4732, #14906 ),
 .UNSPECIFIED., .F., .F. ) 
 B_SPLINE_CURVE_WITH_KNOTS ( ( 3, 2, 2, 2, 3 ),
 ( 0.3295454545454545303, 0.3352272727272727071, 0.3409090909090908839, 0.3465909090909091161, 0.3522727272727272929 ),
 .UNSPECIFIED. ) 
 CURVE ( )  GEOMETRIC_REPRESENTATION_ITEM ( )  RATIONAL_B_SPLINE_CURVE ( ( 1.000000000000000000, 0.9238795325112867385, 1.000000000000000000, 0.9238795325112867385, 1.000000000000000000, 0.9238795325112867385, 1.000000000000000000, 0.9238795325112867385, 1.000000000000000000 ) ) 
 REPRESENTATION_ITEM ( '' )  );
#57803=CARTESIAN_POINT ( 'NONE',  ( -2.828427124746192067, 3.625000000000000000, 2.828427124746190735 ) ) ;
#57810=ORIENTED_EDGE ( 'NONE', *, *, #47564, .F. ) ;
#57817=CARTESIAN_POINT ( 'NONE',  ( -4.541265875000002339, 13.93749999863440614, -5.561446717895856393E-16 ) ) ;
#57828=CARTESIAN_POINT ( 'NONE',  ( -4.000000000000002665, 11.31249999726881583, 1.656854249492380804 ) ) ;
#57831=LINE ( 'NONE', #41206, #2125 ) ;
#57836=CARTESIAN_POINT ( 'NONE',  ( 1.881053915767121776, 11.49999999863440792, -4.541265875000002339 ) ) ;
#57858=PLANE ( 'NONE',  #54792 ) ;
#57879=CARTESIAN_POINT ( 'NONE',  ( -1.881053915767124440, 12.12499999863440969, 4.541265875000001451 ) ) ;
#57882=CARTESIAN_POINT ( 'NONE',  ( 2.449293598294707893E-16, 7.999999997268813168, -4.000000000000001776 ) ) ;
#57906=ORIENTED_EDGE ( 'NONE', *, *, #63812, .F. ) ;
#57908=CARTESIAN_POINT ( 'NONE',  ( -4.541265875000003227, 1.999999998634407028, 1.881053915767121110 ) ) ;
#57924=CARTESIAN_POINT ( 'NONE',  ( 1.881053915767121776, 19.62499999863441147, -4.541265875000002339 ) ) ;
#57934=VERTEX_POINT ( 'NONE', #51689 ) ;
#57954=DIRECTION ( 'NONE',  ( -0.000000000000000000, -1.000000000000000000, -0.000000000000000000 ) ) ;
#57963=EDGE_LOOP ( 'NONE', ( #20964, #18425, #29384, #13158 ) ) ;
#57972=CARTESIAN_POINT ( 'NONE',  ( -1.881053915767121554, 0.7499999986344069169, -4.541265875000002339 ) ) ;
#57991=DIRECTION ( 'NONE',  ( 0.000000000000000000, 0.000000000000000000, -1.000000000000000000 ) ) ;
#58061=CARTESIAN_POINT ( 'NONE',  ( -4.541265875000003227, 9.874999998634404363, 1.881053915767121110 ) ) ;
#58103=CARTESIAN_POINT ( 'NONE',  ( 2.449293598294707893E-16, 12.25000000000000000, -4.000000000000001776 ) ) ;
#58105=CARTESIAN_POINT ( 'NONE',  ( 4.541265875000002339, 11.31249999863440614, 0.000000000000000000 ) ) ;
#58123=ORIENTED_EDGE ( 'NONE', *, *, #64067, .F. ) ;
#58167=VECTOR ( 'NONE', #53155, 1000.000000000000000 ) ;
#58191=CARTESIAN_POINT ( 'NONE',  ( -4.541265875000002339, 16.93749999863440436, -5.561446717895856393E-16 ) ) ;
#58195=CARTESIAN_POINT ( 'NONE',  ( 4.541265875000001451, 1.374999998634407250, 1.881053915767124440 ) ) ;
#58200=CARTESIAN_POINT ( 'NONE',  ( 1.656854249492381248, 12.93749999726881583, -4.000000000000001776 ) ) ;
#58201=CARTESIAN_POINT ( 'NONE',  ( 3.211159895383560947, 1.187499998634406806, 3.211159895383562723 ) ) ;
#58206=CARTESIAN_POINT ( 'NONE',  ( 0.000000000000000000, 0.000000000000000000, 0.000000000000000000 ) ) ;
#58210=CARTESIAN_POINT ( 'NONE',  ( 3.211159895383561835, 8.437499998634407916, -3.211159895383561835 ) ) ;
#58214=( BOUNDED_CURVE ( )  B_SPLINE_CURVE ( 2, ( #47897, #19594, #13555, #7554, #30561, #53944, #70917, #30922, #72021 ),
 .UNSPECIFIED., .F., .F. ) 
 B_SPLINE_CURVE_WITH_KNOTS ( ( 3, 2, 2, 2, 3 ),
 ( 0.5568181818181818787, 0.5625000000000001110, 0.5681818181818183433, 0.5738636363636363535, 0.5795454545454545858 ),
 .UNSPECIFIED. ) 
 CURVE ( )  GEOMETRIC_REPRESENTATION_ITEM ( )  RATIONAL_B_SPLINE_CURVE ( ( 0.9999999999999985567, 0.9238795325112881818, 1.000000000000000000, 0.9238795325112867385, 1.000000000000000000, 0.9238795325112867385, 1.000000000000000000, 0.9238795325112867385, 1.000000000000000000 ) ) 
 REPRESENTATION_ITEM ( '' )  );
#58215=ORIENTED_EDGE ( 'NONE', *, *, #33059, .F. ) ;
#58238=( BOUNDED_CURVE ( )  B_SPLINE_CURVE ( 2, ( #50603, #34402, #22670, #5342, #50981, #40039, #45689, #33653, #73 ),
 .UNSPECIFIED., .F., .F. ) 
 B_SPLINE_CURVE_WITH_KNOTS ( ( 3, 2, 2, 2, 3 ),
 ( 0.4886363636363636465, 0.4943181818181818232, 0.5000000000000000000, 0.5056818181818182323, 0.5113636363636363535 ),
 .UNSPECIFIED. ) 
 CURVE ( )  GEOMETRIC_REPRESENTATION_ITEM ( )  RATIONAL_B_SPLINE_CURVE ( ( 1.000000000000000000, 0.9238795325112867385, 1.000000000000000000, 0.9238795325112867385, 1.000000000000000000, 0.9238795325112867385, 1.000000000000000000, 0.9238795325112867385, 1.000000000000000000 ) ) 
 REPRESENTATION_ITEM ( '' )  );
#58241=CARTESIAN_POINT ( 'NONE',  ( -8.342170076843785083E-16, 3.062499998634406584, 4.541265875000002339 ) ) ;
#58255=CARTESIAN_POINT ( 'NONE',  ( -4.541265875000002339, 11.93749999863440614, -5.561446717895856393E-16 ) ) ;
#58257=CARTESIAN_POINT ( 'NONE',  ( -2.828427124746192067, 4.374999997268814056, 2.828427124746190735 ) ) ;
#58281=CARTESIAN_POINT ( 'NONE',  ( -3.211159895383561391, 2.812499998634407028, -3.211159895383561835 ) ) ;
#58292=CARTESIAN_POINT ( 'NONE',  ( 4.541265875000002339, 21.49999999863440792, -1.881053915767121554 ) ) ;
#58340=CARTESIAN_POINT ( 'NONE',  ( 2.780723358947928197E-16, 21.56249999863440792, -4.541265875000002339 ) ) ;
#58343=CARTESIAN_POINT ( 'NONE',  ( -4.000000000000001776, 1.500000000000000222, -4.898587196589415787E-16 ) ) ;
#58356=CARTESIAN_POINT ( 'NONE',  ( -1.656854249492381248, 6.062499997268813168, -4.000000000000001776 ) ) ;
#58361=ORIENTED_EDGE ( 'NONE', *, *, #48180, .F. ) ;
#58426=CARTESIAN_POINT ( 'NONE',  ( -3.211159895383561391, 10.68749999863440792, -3.211159895383561835 ) ) ;
#58459=DIRECTION ( 'NONE',  ( -0.000000000000000000, -1.000000000000000000, -0.000000000000000000 ) ) ;
#58469=CARTESIAN_POINT ( 'NONE',  ( -1.656854249492381248, 13.31250000000000000, -4.000000000000001776 ) ) ;
#58471=CARTESIAN_POINT ( 'NONE',  ( 3.211159895383561835, 11.43749999863440614, -3.211159895383561835 ) ) ;
#58542=CIRCLE ( 'NONE', #68169, 7.141428428542858420 ) ;
#58549=CARTESIAN_POINT ( 'NONE',  ( -7.347880794884122694E-16, 8.750000000000000000, 4.000000000000001776 ) ) ;
#58552=CARTESIAN_POINT ( 'NONE',  ( -1.881053915767121776, 15.74999999863440436, -4.541265875000002339 ) ) ;
#58562=CARTESIAN_POINT ( 'NONE',  ( 1.656854249492381248, 0.1875000000000001943, -4.000000000000001776 ) ) ;
#58563=CARTESIAN_POINT ( 'NONE',  ( -4.000000000000001776, 15.24999999726881406, -4.898587196589415787E-16 ) ) ;
#58564=VERTEX_POINT ( 'NONE', #48341 ) ;
#58569=CARTESIAN_POINT ( 'NONE',  ( -4.541265875000002339, 13.74999999863440969, -1.881053915767121998 ) ) ;
#58583=( GEOMETRIC_REPRESENTATION_CONTEXT ( 3 ) GLOBAL_UNCERTAINTY_ASSIGNED_CONTEXT ( ( #29235 ) ) GLOBAL_UNIT_ASSIGNED_CONTEXT ( ( #30986, #36288, #1953 ) ) REPRESENTATION_CONTEXT ( 'NONE', 'WORKASPACE' ) );
#58584=ORIENTED_EDGE ( 'NONE', *, *, #29591, .T. ) ;
#58592=DIRECTION ( 'NONE',  ( 0.000000000000000000, 0.000000000000000000, -1.000000000000000000 ) ) ;
#58597=CARTESIAN_POINT ( 'NONE',  ( -4.541265875000002339, 0.7499999986344069169, -1.881053915767121998 ) ) ;
#58615=CARTESIAN_POINT ( 'NONE',  ( -8.342170076843785083E-16, 18.18749999863440792, 4.541265875000002339 ) ) ;
#58639=CARTESIAN_POINT ( 'NONE',  ( -1.881053915767124440, 3.124999998634407028, 4.541265875000001451 ) ) ;
#58642=EDGE_CURVE ( 'NONE', #30848, #36205, #36301, .T. ) ;
#58652=CARTESIAN_POINT ( 'NONE',  ( -2.828427124746192067, 1.374999997268813168, 2.828427124746190735 ) ) ;
#58660=VECTOR ( 'NONE', #13727, 1000.000000000000000 ) ;
#58664=( BOUNDED_CURVE ( )  B_SPLINE_CURVE ( 2, ( #38286, #61291, #9618, #34128, #543, #23153, #58257, #40885, #46539 ),
 .UNSPECIFIED., .F., .F. ) 
 B_SPLINE_CURVE_WITH_KNOTS ( ( 3, 2, 2, 2, 3 ),
 ( 0.1477272727272727348, 0.1534090909090909116, 0.1590909090909091161, 0.1647727272727272929, 0.1704545454545454697 ),
 .UNSPECIFIED. ) 
 CURVE ( )  GEOMETRIC_REPRESENTATION_ITEM ( )  RATIONAL_B_SPLINE_CURVE ( ( 1.000000000000000000, 0.9238795325112867385, 1.000000000000000000, 0.9238795325112867385, 1.000000000000000000, 0.9238795325112867385, 1.000000000000000000, 0.9238795325112864054, 1.000000000000000444 ) ) 
 REPRESENTATION_ITEM ( '' )  );
#58666=LINE ( 'NONE', #13346, #19532 ) ;
#58679=CARTESIAN_POINT ( 'NONE',  ( -4.000000000000001776, 17.18749999726881583, -1.656854249492381470 ) ) ;
#58700=CARTESIAN_POINT ( 'NONE',  ( 4.541265875000002339, 5.499999998634407028, -1.881053915767121554 ) ) ;
#58727=CARTESIAN_POINT ( 'NONE',  ( -7.347880794884122694E-16, 9.750000000000000000, 4.000000000000001776 ) ) ;
#58773=VERTEX_POINT ( 'NONE', #9861 ) ;
#58792=CARTESIAN_POINT ( 'NONE',  ( 4.541265875000002339, 11.31249999863440614, 0.000000000000000000 ) ) ;
#58800=CARTESIAN_POINT ( 'NONE',  ( 4.898587196589415787E-16, 0.000000000000000000, 4.000000000000001776 ) ) ;
#58819=CARTESIAN_POINT ( 'NONE',  ( -7.347880794884122694E-16, 16.49999999726881228, 4.000000000000001776 ) ) ;
#58836=CARTESIAN_POINT ( 'NONE',  ( 1.656854249492381248, 11.18749999999999822, -4.000000000000001776 ) ) ;
#58838=CARTESIAN_POINT ( 'NONE',  ( -3.211159895383562723, 9.937499998634406140, 3.211159895383561391 ) ) ;
#58841=ORIENTED_EDGE ( 'NONE', *, *, #43343, .F. ) ;
#58884=ORIENTED_EDGE ( 'NONE', *, *, #43297, .F. ) ;
#58896=EDGE_CURVE ( 'NONE', #56422, #45848, #50585, .T. ) ;
#58910=CARTESIAN_POINT ( 'NONE',  ( -1.656854249492383468, 16.43749999726881228, 4.000000000000000888 ) ) ;
#58923=CARTESIAN_POINT ( 'NONE',  ( -4.541265875000003227, 17.99999999863440792, 1.881053915767121110 ) ) ;
#58927=CARTESIAN_POINT ( 'NONE',  ( 1.881053915767121776, 1.624999998634407028, -4.541265875000002339 ) ) ;
#58934=CARTESIAN_POINT ( 'NONE',  ( -1.656854249492381248, 13.06249999726881406, -4.000000000000001776 ) ) ;
#58935=CARTESIAN_POINT ( 'NONE',  ( -4.541265875000002339, 0.7499999986344069169, -1.881053915767121998 ) ) ;
#58941=CARTESIAN_POINT ( 'NONE',  ( 3.211159895383561835, 14.43749999863440792, -3.211159895383561835 ) ) ;
#58968=CARTESIAN_POINT ( 'NONE',  ( -4.541265875000003227, 2.874999998634407028, 1.881053915767121110 ) ) ;
#58984=( BOUNDED_CURVE ( )  B_SPLINE_CURVE ( 2, ( #21989, #62720, #63099, #56714, #34831 ),
 .UNSPECIFIED., .F., .F. ) 
 B_SPLINE_CURVE_WITH_KNOTS ( ( 3, 2, 3 ),
 ( 0.000000000000000000, 0.005681818181818181976, 0.01136363636363636395 ),
 .UNSPECIFIED. ) 
 CURVE ( )  GEOMETRIC_REPRESENTATION_ITEM ( )  RATIONAL_B_SPLINE_CURVE ( ( 1.000000000000000000, 0.9238795325112867385, 1.000000000000000000, 0.9238795325112867385, 1.000000000000000000 ) ) 
 REPRESENTATION_ITEM ( '' )  );
#58988=CARTESIAN_POINT ( 'NONE',  ( -1.881053915767124440, 17.12499999863440436, 4.541265875000001451 ) ) ;
#58989=CARTESIAN_POINT ( 'NONE',  ( 1.656854249492369036, 10.93749999726881583, -4.000000000000014211 ) ) ;
#58991=ORIENTED_EDGE ( 'NONE', *, *, #8579, .F. ) ;
#59002=EDGE_LOOP ( 'NONE', ( #6049, #67617, #42284, #24917 ) ) ;
#59011=EDGE_LOOP ( 'NONE', ( #15877, #26055, #32767, #19089 ) ) ;
#59013=CARTESIAN_POINT ( 'NONE',  ( -4.541265875000003227, 3.999999998634406584, 1.881053915767121110 ) ) ;
#59023=CARTESIAN_POINT ( 'NONE',  ( 4.000000000000001776, 2.749999997268813168, 0.000000000000000000 ) ) ;
#59030=CARTESIAN_POINT ( 'NONE',  ( 3.211159895383560947, 4.187499998634407028, 3.211159895383562723 ) ) ;
#59072=CARTESIAN_POINT ( 'NONE',  ( -4.541265875000002339, 5.874999998634407028, -1.881053915767121998 ) ) ;
#59118=CARTESIAN_POINT ( 'NONE',  ( 4.541265875000002339, 10.43749999863440792, 0.000000000000000000 ) ) ;
#59137=CARTESIAN_POINT ( 'NONE',  ( -4.000000000000001776, 15.24999999726881406, -4.898587196589415787E-16 ) ) ;
#59139=ORIENTED_EDGE ( 'NONE', *, *, #45265, .T. ) ;
#59164=CARTESIAN_POINT ( 'NONE',  ( -4.541265875000002339, 13.81249999863440614, -5.561446717895856393E-16 ) ) ;
#59197=VERTEX_POINT ( 'NONE', #54307 ) ;
#59206=CARTESIAN_POINT ( 'NONE',  ( -7.347880794884122694E-16, 10.75000000000000000, 4.000000000000001776 ) ) ;
#59208=CARTESIAN_POINT ( 'NONE',  ( 4.541265875000002339, 17.31249999863440792, 0.000000000000000000 ) ) ;
#59211=VERTEX_POINT ( 'NONE', #2618 ) ;
#59215=CARTESIAN_POINT ( 'NONE',  ( 4.000000000000000888, 13.68749999726881583, 1.656854249492384135 ) ) ;
#59251=ORIENTED_EDGE ( 'NONE', *, *, #27773, .T. ) ;
#59287=CARTESIAN_POINT ( 'NONE',  ( -3.211159895383561391, 18.81249999863440436, -3.211159895383561835 ) ) ;
#59296=CARTESIAN_POINT ( 'NONE',  ( -4.000000000000002665, 1.562500000000000666, 1.656854249492380804 ) ) ;
#59297=CARTESIAN_POINT ( 'NONE',  ( 4.000000000000001776, 15.74999999726881406, 0.000000000000000000 ) ) ;
#59298=CARTESIAN_POINT ( 'NONE',  ( 3.211159895383561835, 5.437499998634407028, -3.211159895383561835 ) ) ;
#59306=CARTESIAN_POINT ( 'NONE',  ( -4.541265875000002339, 13.81249999863440614, -5.561446717895856393E-16 ) ) ;
#59313=( BOUNDED_CURVE ( )  B_SPLINE_CURVE ( 2, ( #51839, #22780, #185, #65280, #45802, #53608, #1920, #24908, #47924 ),
 .UNSPECIFIED., .F., .F. ) 
 B_SPLINE_CURVE_WITH_KNOTS ( ( 3, 2, 2, 2, 3 ),
 ( 0.3068181818181818232, 0.3125000000000000000, 0.3181818181818181768, 0.3238636363636363535, 0.3295454545454545303 ),
 .UNSPECIFIED. ) 
 CURVE ( )  GEOMETRIC_REPRESENTATION_ITEM ( )  RATIONAL_B_SPLINE_CURVE ( ( 1.000000000000000000, 0.9238795325112867385, 1.000000000000000000, 0.9238795325112867385, 1.000000000000000000, 0.9238795325112867385, 1.000000000000000000, 0.9238795325112867385, 1.000000000000000000 ) ) 
 REPRESENTATION_ITEM ( '' )  );
#59335=CARTESIAN_POINT ( 'NONE',  ( -1.881053915767121554, 1.624999998634407028, -4.541265875000002339 ) ) ;
#59352=CARTESIAN_POINT ( 'NONE',  ( -1.881053915767121554, 15.74999999863440614, -4.541265875000002339 ) ) ;
#59375=CARTESIAN_POINT ( 'NONE',  ( 3.211159895383560947, 5.312499998634407028, 3.211159895383562723 ) ) ;
#59385=CARTESIAN_POINT ( 'NONE',  ( 2.449293598294707893E-16, 3.999999997268813168, -4.000000000000001776 ) ) ;
#59391=CARTESIAN_POINT ( 'NONE',  ( -4.541265875000002339, 2.812499998634407028, -5.561446717895856393E-16 ) ) ;
#59412=CYLINDRICAL_SURFACE ( 'NONE', #49558, 4.000000000000001776 ) ;
#59436=CARTESIAN_POINT ( 'NONE',  ( 4.541265875000002339, 4.437499998634407028, 0.000000000000000000 ) ) ;
#59472=CARTESIAN_POINT ( 'NONE',  ( -1.062900648031719353, 21.99999999999998934, 4.384117386624189372 ) ) ;
#59482=CARTESIAN_POINT ( 'NONE',  ( -4.541265875000002339, 13.87499999863440969, -1.881053915767121998 ) ) ;
#59522=CARTESIAN_POINT ( 'NONE',  ( 4.541265875000002339, 12.37499999863440969, -1.881053915767121554 ) ) ;
#59561=CARTESIAN_POINT ( 'NONE',  ( 0.000000000000000000, 0.000000000000000000, -4.000000000000001776 ) ) ;
#59568=CARTESIAN_POINT ( 'NONE',  ( 1.656854249492381914, 17.81250000000000355, 4.000000000000000888 ) ) ;
#59569=CARTESIAN_POINT ( 'NONE',  ( -4.541265875000002339, 17.74999999863440792, -1.881053915767121998 ) ) ;
#59592=CARTESIAN_POINT ( 'NONE',  ( -1.656854249492381248, 0.3125000000000002220, -4.000000000000001776 ) ) ;
#59614=CARTESIAN_POINT ( 'NONE',  ( -7.347880794884122694E-16, 14.75000000000000178, 4.000000000000001776 ) ) ;
#59647=CARTESIAN_POINT ( 'NONE',  ( -1.881053915767121776, 18.74999999863440436, -4.541265875000002339 ) ) ;
#59659=FACE_OUTER_BOUND ( 'NONE', #61113, .T. ) ;
#59660=CARTESIAN_POINT ( 'NONE',  ( -7.347880794884122694E-16, 14.49999999726881406, 4.000000000000001776 ) ) ;
#59661=CARTESIAN_POINT ( 'NONE',  ( -3.211159895383562723, 4.937499998634407028, 3.211159895383561391 ) ) ;
#59665=EDGE_CURVE ( 'NONE', #31861, #56591, #53946, .T. ) ;
#59670=CARTESIAN_POINT ( 'NONE',  ( 1.881053915767122664, 15.12499999863441147, 4.541265875000001451 ) ) ;
#59676=LINE ( 'NONE', #13990, #12881 ) ;
#59699=CARTESIAN_POINT ( 'NONE',  ( -4.541265875000002339, 3.812499998634407028, -5.561446717895856393E-16 ) ) ;
#59717=CARTESIAN_POINT ( 'NONE',  ( -3.211159895383561391, 15.81249999863440436, -3.211159895383561835 ) ) ;
#59741=CARTESIAN_POINT ( 'NONE',  ( -1.881053915767124440, 6.124999998634407916, 4.541265875000001451 ) ) ;
#59752=CARTESIAN_POINT ( 'NONE',  ( -2.828427124746190735, 3.124999997268813168, -2.828427124746191623 ) ) ;
#59759=CARTESIAN_POINT ( 'NONE',  ( -1.881053915767121554, 2.624999998634406584, -4.541265875000002339 ) ) ;
#59800=CARTESIAN_POINT ( 'NONE',  ( 1.881053915767121776, 4.624999998634407028, -4.541265875000002339 ) ) ;
#59811=DIRECTION ( 'NONE',  ( 0.000000000000000000, 0.000000000000000000, -1.000000000000000000 ) ) ;
#59829=ORIENTED_EDGE ( 'NONE', *, *, #45586, .F. ) ;
#59835=DIRECTION ( 'NONE',  ( -0.000000000000000000, -1.000000000000000000, -0.000000000000000000 ) ) ;
#59841=EDGE_CURVE ( 'NONE', #27667, #8238, #1049, .T. ) ;
#59844=CARTESIAN_POINT ( 'NONE',  ( -3.211159895383561391, 12.81249999863440792, -3.211159895383561835 ) ) ;
#59855=CARTESIAN_POINT ( 'NONE',  ( 0.000000000000000000, 15.99999999999998579, 0.000000000000000000 ) ) ;
#59858=CARTESIAN_POINT ( 'NONE',  ( -4.352425261977313831, 21.99999999999996803, -0.6811922050314749288 ) ) ;
#59887=CARTESIAN_POINT ( 'NONE',  ( 4.541265875000002339, 14.37499999863440969, -1.881053915767121554 ) ) ;
#59894=LINE ( 'NONE', #8208, #37569 ) ;
#59907=CARTESIAN_POINT ( 'NONE',  ( 4.000000000000001776, 13.06250000000000000, -1.656854249492381248 ) ) ;
#59924=ORIENTED_EDGE ( 'NONE', *, *, #30634, .T. ) ;
#59932=CARTESIAN_POINT ( 'NONE',  ( 1.656854249492381248, 15.18750000000000000, -4.000000000000001776 ) ) ;
#59933=CARTESIAN_POINT ( 'NONE',  ( 2.780723358947928197E-16, 14.56249999863440792, -4.541265875000002339 ) ) ;
#59970=CARTESIAN_POINT ( 'NONE',  ( -4.000000000000001776, 6.437500000000000888, -1.656854249492381470 ) ) ;
#60009=CARTESIAN_POINT ( 'NONE',  ( 4.541265875000001451, 19.37499999863440792, 1.881053915767124440 ) ) ;
#60012=CARTESIAN_POINT ( 'NONE',  ( 1.881053915767121776, 2.624999998634407028, -4.541265875000002339 ) ) ;
#60018=CARTESIAN_POINT ( 'NONE',  ( 4.000000000000000888, 5.937500000000000000, 1.656854249492384135 ) ) ;
#60019=CARTESIAN_POINT ( 'NONE',  ( 4.000000000000001776, 16.81249999726881228, -1.656854249492381248 ) ) ;
#60020=CARTESIAN_POINT ( 'NONE',  ( 4.541265875000002339, 4.374999998634407028, -1.881053915767121776 ) ) ;
#60026=CARTESIAN_POINT ( 'NONE',  ( 4.541265875000002339, 19.37499999863440792, -1.881053915767121554 ) ) ;
#60047=CARTESIAN_POINT ( 'NONE',  ( -2.828427124746192067, 3.374999997268813612, 2.828427124746190735 ) ) ;
#60053=CARTESIAN_POINT ( 'NONE',  ( -4.541265875000003227, 7.874999998634407028, 1.881053915767121110 ) ) ;
#60074=CARTESIAN_POINT ( 'NONE',  ( -1.881053915767121554, 17.74999999863440792, -4.541265875000002339 ) ) ;
#60100=CARTESIAN_POINT ( 'NONE',  ( -4.541265875000002339, 4.937499998634407916, -5.561446717895856393E-16 ) ) ;
#60104=DIRECTION ( 'NONE',  ( 0.000000000000000000, 0.000000000000000000, -1.000000000000000000 ) ) ;
#60109=ADVANCED_FACE ( 'NONE', ( #25246 ), #48263, .T. ) ;
#60111=CARTESIAN_POINT ( 'NONE',  ( 1.656854249492381248, 0.9374999972688131678, -4.000000000000001776 ) ) ;
#60115=CARTESIAN_POINT ( 'NONE',  ( -8.342170076843785083E-16, 2.062499998634406584, 4.541265875000002339 ) ) ;
#60116=AXIS2_PLACEMENT_3D ( 'NONE', #45864, #46237, #40959 ) ;
#60149=EDGE_LOOP ( 'NONE', ( #55570, #5750, #70815, #22741 ) ) ;
#60157=ADVANCED_FACE ( 'NONE', ( #49767, #9786 ), #32807, .F. ) ;
#60160=CARTESIAN_POINT ( 'NONE',  ( 4.541265875000002339, 5.437499998634407028, 0.000000000000000000 ) ) ;
#60168=CARTESIAN_POINT ( 'NONE',  ( 4.000000000000001776, 1.806524977843537691E-16, 0.000000000000000000 ) ) ;
#60191=CARTESIAN_POINT ( 'NONE',  ( 1.656854249492356157, 20.93749999726881228, -4.000000000000026645 ) ) ;
#60194=CARTESIAN_POINT ( 'NONE',  ( -0.3671489098107383886, 21.99999999999999645, 4.453226760635411452 ) ) ;
#60204=CARTESIAN_POINT ( 'NONE',  ( -4.541265875000002339, 13.93749999863440614, -5.561446717895856393E-16 ) ) ;
#60225=CARTESIAN_POINT ( 'NONE',  ( -4.000000000000002665, 2.312499997268813168, 1.656854249492380582 ) ) ;
#60247=CARTESIAN_POINT ( 'NONE',  ( 1.881053915767121776, 15.49999999863440792, -4.541265875000002339 ) ) ;
#60279=CARTESIAN_POINT ( 'NONE',  ( -1.656854249492393238, 11.06249999726881406, -3.999999999999989786 ) ) ;
#60295=CARTESIAN_POINT ( 'NONE',  ( 4.000000000000000888, 15.93750000000000000, 1.656854249492384135 ) ) ;
#60296=CARTESIAN_POINT ( 'NONE',  ( 4.541265875000002339, 14.31249999863440792, 0.000000000000000000 ) ) ;
#60332=CARTESIAN_POINT ( 'NONE',  ( -1.656854249492383468, 16.68750000000000000, 4.000000000000000888 ) ) ;
#60340=VERTEX_POINT ( 'NONE', #7374 ) ;
#60378=CARTESIAN_POINT ( 'NONE',  ( 4.541265875000002339, 20.49999999863440436, -1.881053915767121776 ) ) ;
#60382=CARTESIAN_POINT ( 'NONE',  ( 1.881053915767121776, 5.624999998634407028, -4.541265875000002339 ) ) ;
#60391=CARTESIAN_POINT ( 'NONE',  ( -4.000000000000001776, 3.437500000000000000, -1.656854249492381470 ) ) ;
#60392=CARTESIAN_POINT ( 'NONE',  ( 2.828427124746191623, 19.87499999726881228, -2.828427124746191623 ) ) ;
#60393=CARTESIAN_POINT ( 'NONE',  ( 4.541265875000002339, 2.312499998634407028, 0.000000000000000000 ) ) ;
#60399=CARTESIAN_POINT ( 'NONE',  ( 2.780723358947928197E-16, 17.56249999863440792, -4.541265875000002339 ) ) ;
#60424=CARTESIAN_POINT ( 'NONE',  ( -4.000000000000001776, 3.249999997268813612, -4.898587196589415787E-16 ) ) ;
#60430=CARTESIAN_POINT ( 'NONE',  ( -4.541265875000003227, 6.874999998634407916, 1.881053915767121110 ) ) ;
#60445=CARTESIAN_POINT ( 'NONE',  ( -4.541265875000002339, 21.87499999863441147, -1.881053915767121998 ) ) ;
#60470=CARTESIAN_POINT ( 'NONE',  ( -4.541265875000002339, 8.874999998634407916, -1.881053915767121998 ) ) ;
#60481=CARTESIAN_POINT ( 'NONE',  ( -7.347880794884122694E-16, 4.499999997268813168, 4.000000000000001776 ) ) ;
#60490=CARTESIAN_POINT ( 'NONE',  ( 4.541265875000002339, 5.374999998634406140, -1.881053915767121554 ) ) ;
#60498=CARTESIAN_POINT ( 'NONE',  ( 0.000000000000000000, 0.000000000000000000, 0.000000000000000000 ) ) ;
#60520=DIRECTION ( 'NONE',  ( 0.000000000000000000, 0.000000000000000000, -1.000000000000000000 ) ) ;
#60535=CARTESIAN_POINT ( 'NONE',  ( 1.881053915767122664, 9.249999998634406140, 4.541265875000001451 ) ) ;
#60542=FACE_OUTER_BOUND ( 'NONE', #57256, .T. ) ;
#60549=CARTESIAN_POINT ( 'NONE',  ( 0.000000000000000000, 0.000000000000000000, -4.000000000000001776 ) ) ;
#60580=CARTESIAN_POINT ( 'NONE',  ( -1.881053915767121554, 15.74999999863440614, -4.541265875000002339 ) ) ;
#60626=CARTESIAN_POINT ( 'NONE',  ( -3.211159895383562723, 13.93749999863440614, 3.211159895383561391 ) ) ;
#60658=DIRECTION ( 'NONE',  ( -0.000000000000000000, -1.000000000000000000, -0.000000000000000000 ) ) ;
#60678=CARTESIAN_POINT ( 'NONE',  ( 4.000000000000001776, 17.00000000000000000, 0.000000000000000000 ) ) ;
#60679=CARTESIAN_POINT ( 'NONE',  ( -4.541265875000002339, 16.74999999863440436, -1.881053915767121998 ) ) ;
#60746=CARTESIAN_POINT ( 'NONE',  ( -7.347880794884122694E-16, 8.499999997268814056, 4.000000000000001776 ) ) ;
#60763=CARTESIAN_POINT ( 'NONE',  ( -8.342170076843785083E-16, 2.187499998634407028, 4.541265875000002339 ) ) ;
#60768=CARTESIAN_POINT ( 'NONE',  ( 1.656854249492381914, 2.812500000000000000, 4.000000000000000888 ) ) ;
#60769=CARTESIAN_POINT ( 'NONE',  ( -2.828427124746192067, 16.37499999726881228, 2.828427124746190735 ) ) ;
#60770=CARTESIAN_POINT ( 'NONE',  ( -3.211159895383562723, 3.937499998634406584, 3.211159895383561391 ) ) ;
#60775=CARTESIAN_POINT ( 'NONE',  ( -4.541265875000003227, 19.87499999863440792, 1.881053915767121110 ) ) ;
#60786=CARTESIAN_POINT ( 'NONE',  ( -4.000000000000001776, 21.24999999726881583, -4.898587196589415787E-16 ) ) ;
#60804=CARTESIAN_POINT ( 'NONE',  ( 1.881053915767121776, 5.499999998634407028, -4.541265875000002339 ) ) ;
#60813=CARTESIAN_POINT ( 'NONE',  ( 1.656854249492381248, 19.93749999726881228, -4.000000000000001776 ) ) ;
#60824=CARTESIAN_POINT ( 'NONE',  ( -4.541265875000002339, 20.93749999863440436, -5.561446717895856393E-16 ) ) ;
#60850=CARTESIAN_POINT ( 'NONE',  ( 3.211159895383560947, 8.312499998634407916, 3.211159895383562723 ) ) ;
#60859=CARTESIAN_POINT ( 'NONE',  ( -2.828427124746192067, 5.374999997268813168, 2.828427124746190735 ) ) ;
#60863=CARTESIAN_POINT ( 'NONE',  ( -8.342170076843785083E-16, 8.062499998634406140, 4.541265875000002339 ) ) ;
#60865=CARTESIAN_POINT ( 'NONE',  ( 2.449293598294707893E-16, 13.25000000000000000, -4.000000000000001776 ) ) ;
#60908=CARTESIAN_POINT ( 'NONE',  ( 1.881053915767121776, 6.624999998634407916, -4.541265875000002339 ) ) ;
#60912=CARTESIAN_POINT ( 'NONE',  ( -1.656854249492383468, 5.437499997268813168, 4.000000000000000888 ) ) ;
#60913=ORIENTED_EDGE ( 'NONE', *, *, #39325, .F. ) ;
#60957=CARTESIAN_POINT ( 'NONE',  ( 1.881053915767122664, 16.24999999863440436, 4.541265875000001451 ) ) ;
#60967=DIRECTION ( 'NONE',  ( -1.000000000000000000, -0.000000000000000000, 0.000000000000000000 ) ) ;
#60998=CARTESIAN_POINT ( 'NONE',  ( 3.211159895383560947, 20.18749999863440436, 3.211159895383562723 ) ) ;
#61023=DIRECTION ( 'NONE',  ( 0.000000000000000000, 0.000000000000000000, -1.000000000000000000 ) ) ;
#61032=CARTESIAN_POINT ( 'NONE',  ( -7.347880794884122694E-16, 19.75000000000000000, 4.000000000000001776 ) ) ;
#61050=CARTESIAN_POINT ( 'NONE',  ( -4.000000000000001776, 14.50000000000000000, -4.898587196589415787E-16 ) ) ;
#61051=CARTESIAN_POINT ( 'NONE',  ( 1.881053915767122664, 21.12499999863441147, 4.541265875000001451 ) ) ;
#61113=EDGE_LOOP ( 'NONE', ( #29433, #46998, #40979, #9487, #50236, #5937, #35350, #23800, #34642, #24384, #50043, #45269, #19120, #16166, #46007, #71977, #8578, #16220, #33227, #63666, #13022, #16869, #59924, #28534, #33616, #37689, #48474, #13987, #10855, #65827, #44340, #41471, #38166, #5978, #30844, #22269, #36283, #25469, #32073, #70395, #37783, #4567, #9995, #16510, #72041, #19295, #43421, #32008 ) ) ;
#61131=CARTESIAN_POINT ( 'NONE',  ( -4.541265875000002339, 20.93749999863440436, -5.561446717895856393E-16 ) ) ;
#61134=CARTESIAN_POINT ( 'NONE',  ( -1.881053915767124440, 2.124999998634406584, 4.541265875000001451 ) ) ;
#61141=CARTESIAN_POINT ( 'NONE',  ( -4.000000000000001776, 5.500000000000000000, -4.898587196589415787E-16 ) ) ;
#61142=CARTESIAN_POINT ( 'NONE',  ( 4.000000000000001776, 17.81249999726881938, -1.656854249492381248 ) ) ;
#61143=CARTESIAN_POINT ( 'NONE',  ( 4.541265875000002339, 9.374999998634404363, -1.881053915767121776 ) ) ;
#61146=VERTEX_POINT ( 'NONE', #67142 ) ;
#61151=CARTESIAN_POINT ( 'NONE',  ( -1.881053915767121554, 18.62499999863440792, -4.541265875000002339 ) ) ;
#61185=CARTESIAN_POINT ( 'NONE',  ( 4.541265875000002339, 7.312499998634407028, 0.000000000000000000 ) ) ;
#61193=CARTESIAN_POINT ( 'NONE',  ( 4.000000000000000888, 19.68749999726881228, 1.656854249492384135 ) ) ;
#61202=CARTESIAN_POINT ( 'NONE',  ( -4.541265875000003227, 19.99999999863440436, 1.881053915767121110 ) ) ;
#61208=EDGE_CURVE ( 'NONE', #45464, #33515, #3435, .T. ) ;
#61227=CARTESIAN_POINT ( 'NONE',  ( 4.541265875000002339, 8.437499998634407916, 0.000000000000000000 ) ) ;
#61237=CARTESIAN_POINT ( 'NONE',  ( 2.828427124746191623, 4.874999997268813168, -2.828427124746191623 ) ) ;
#61242=CARTESIAN_POINT ( 'NONE',  ( -1.881053915767121554, 5.624999998634407028, -4.541265875000002339 ) ) ;
#61246=LINE ( 'NONE', #37872, #63844 ) ;
#61287=CARTESIAN_POINT ( 'NONE',  ( 4.541265875000002339, 9.437499998634407916, 0.000000000000000000 ) ) ;
#61291=CARTESIAN_POINT ( 'NONE',  ( -1.656854249492381248, 4.062499997268813168, -4.000000000000001776 ) ) ;
#61331=CARTESIAN_POINT ( 'NONE',  ( 3.211159895383560947, 17.31249999863440792, 3.211159895383562723 ) ) ;
#61332=ORIENTED_EDGE ( 'NONE', *, *, #46382, .T. ) ;
#61375=CARTESIAN_POINT ( 'NONE',  ( 1.881053915767122664, 17.12499999863440436, 4.541265875000001451 ) ) ;
#61381=VERTEX_POINT ( 'NONE', #42542 ) ;
#61427=CARTESIAN_POINT ( 'NONE',  ( -7.347880794884122694E-16, 21.75000000000000355, 4.000000000000001776 ) ) ;
#61428=CARTESIAN_POINT ( 'NONE',  ( -3.211159895383561391, 18.68749999863440436, -3.211159895383561835 ) ) ;
#61451=CARTESIAN_POINT ( 'NONE',  ( 2.449293598294707893E-16, 14.25000000000000000, -4.000000000000001776 ) ) ;
#61493=CARTESIAN_POINT ( 'NONE',  ( -7.347880794884122694E-16, 18.49999999726881583, 4.000000000000001776 ) ) ;
#61512=CARTESIAN_POINT ( 'NONE',  ( -1.881053915767121554, 3.749999998634407028, -4.541265875000002339 ) ) ;
#61518=CARTESIAN_POINT ( 'NONE',  ( -4.000000000000002665, 4.562500000000000888, 1.656854249492380804 ) ) ;
#61520=CARTESIAN_POINT ( 'NONE',  ( -2.828427124746192067, 19.37499999726881228, 2.828427124746190735 ) ) ;
#61521=CARTESIAN_POINT ( 'NONE',  ( -3.211159895383562723, 5.937499998634407028, 3.211159895383561391 ) ) ;
#61528=CARTESIAN_POINT ( 'NONE',  ( 1.881053915767121776, 19.49999999863440436, -4.541265875000002339 ) ) ;
#61542=VECTOR ( 'NONE', #28165, 1000.000000000000000 ) ;
#61561=CARTESIAN_POINT ( 'NONE',  ( -3.211159895383562723, 5.937499998634407028, 3.211159895383561391 ) ) ;
#61579=CARTESIAN_POINT ( 'NONE',  ( -4.541265875000002339, 20.87499999863441147, -1.881053915767121998 ) ) ;
#61598=CARTESIAN_POINT ( 'NONE',  ( 1.881053915767121998, 9.624999998634404363, -4.541265875000002339 ) ) ;
#61611=CARTESIAN_POINT ( 'NONE',  ( 1.656854249492381914, 6.562499997268813168, 4.000000000000000888 ) ) ;
#61621=CARTESIAN_POINT ( 'NONE',  ( 1.881053915767122664, 7.124999998634407916, 4.541265875000001451 ) ) ;
#61625=DIRECTION ( 'NONE',  ( 0.8660254037844400399, 0.4999999999999976130, 0.000000000000000000 ) ) ;
#61641=LINE ( 'NONE', #3936, #72457 ) ;
#61663=CARTESIAN_POINT ( 'NONE',  ( -8.342170076843785083E-16, 8.187499998634406140, 4.541265875000002339 ) ) ;
#61666=CARTESIAN_POINT ( 'NONE',  ( -4.000000000000001776, 5.249999997268813168, -4.898587196589415787E-16 ) ) ;
#61706=CARTESIAN_POINT ( 'NONE',  ( -4.541265875000003227, 14.99999999863440969, 1.881053915767121110 ) ) ;
#61750=FACE_OUTER_BOUND ( 'NONE', #6190, .T. ) ;
#61751=CARTESIAN_POINT ( 'NONE',  ( 2.780723358947928197E-16, 17.56249999863440792, -4.541265875000002339 ) ) ;
#61760=DIRECTION ( 'NONE',  ( -0.000000000000000000, -1.000000000000000000, -0.000000000000000000 ) ) ;
#61783=CARTESIAN_POINT ( 'NONE',  ( 2.449293598294707893E-16, 0.9999999972688131678, -4.000000000000001776 ) ) ;
#61795=VERTEX_POINT ( 'NONE', #28922 ) ;
#61801=CARTESIAN_POINT ( 'NONE',  ( 4.000000000000001776, 21.06250000000000000, -1.656854249492381248 ) ) ;
#61802=CARTESIAN_POINT ( 'NONE',  ( -1.881053915767124440, 17.99999999863440792, 4.541265875000001451 ) ) ;
#61828=ORIENTED_EDGE ( 'NONE', *, *, #33400, .F. ) ;
#61835=CARTESIAN_POINT ( 'NONE',  ( 2.449293598294707893E-16, 17.99999999726881583, -4.000000000000001776 ) ) ;
#61882=CARTESIAN_POINT ( 'NONE',  ( 3.211159895383561835, 7.562499998634407028, -3.211159895383561835 ) ) ;
#61888=CARTESIAN_POINT ( 'NONE',  ( -4.000000000000001776, 9.500000000000000000, -4.898587196589415787E-16 ) ) ;
#61890=CARTESIAN_POINT ( 'NONE',  ( 2.780723358947928197E-16, 9.562499998634406140, -4.541265875000002339 ) ) ;
#61897=CARTESIAN_POINT ( 'NONE',  ( 4.541265875000002339, 21.31249999863440792, 0.000000000000000000 ) ) ;
#61930=ADVANCED_FACE ( 'NONE', ( #34975 ), #17971, .T. ) ;
#61943=CARTESIAN_POINT ( 'NONE',  ( 2.780723358947928197E-16, 18.68749999863440436, -4.541265875000002339 ) ) ;
#61965=CARTESIAN_POINT ( 'NONE',  ( -1.881053915767124440, 9.124999998634407916, 4.541265875000001451 ) ) ;
#61978=CARTESIAN_POINT ( 'NONE',  ( 4.000000000000001776, 4.812499997268813168, -1.656854249492381248 ) ) ;
#61985=CARTESIAN_POINT ( 'NONE',  ( 2.828427124746190291, 12.62499999726881406, 2.828427124746192067 ) ) ;
#61986=CARTESIAN_POINT ( 'NONE',  ( -3.211159895383561391, 6.687499998634407028, -3.211159895383561835 ) ) ;
#61987=EDGE_CURVE ( 'NONE', #8238, #49926, #40023, .T. ) ;
#61988=CARTESIAN_POINT ( 'NONE',  ( -1.656854249492383468, 13.68750000000000000, 4.000000000000000888 ) ) ;
#61992=VERTEX_POINT ( 'NONE', #14139 ) ;
#62022=CARTESIAN_POINT ( 'NONE',  ( 2.449293598294707893E-16, 15.99999999726881406, -4.000000000000001776 ) ) ;
#62029=CARTESIAN_POINT ( 'NONE',  ( -3.211159895383562723, 10.06249999863440614, 3.211159895383561391 ) ) ;
#62033=ORIENTED_EDGE ( 'NONE', *, *, #55983, .T. ) ;
#62044=CARTESIAN_POINT ( 'NONE',  ( 4.000000000000001776, 14.74999999726881406, 0.000000000000000000 ) ) ;
#62073=CARTESIAN_POINT ( 'NONE',  ( -3.211159895383562723, 17.06249999863440792, 3.211159895383561391 ) ) ;
#62097=CARTESIAN_POINT ( 'NONE',  ( -2.290346072756624274, 21.99999999999999289, 3.966738362316490907 ) ) ;
#62111=DIRECTION ( 'NONE',  ( 0.000000000000000000, 0.000000000000000000, -1.000000000000000000 ) ) ;
#62115=CARTESIAN_POINT ( 'NONE',  ( 4.541265875000002339, 18.37499999863441147, -1.881053915767121554 ) ) ;
#62160=VERTEX_POINT ( 'NONE', #53422 ) ;
#62165=CARTESIAN_POINT ( 'NONE',  ( -4.000000000000001776, 18.50000000000000000, -4.898587196589415787E-16 ) ) ;
#62167=CARTESIAN_POINT ( 'NONE',  ( -1.881053915767121776, 19.62499999863441147, -4.541265875000002339 ) ) ;
#62244=ORIENTED_EDGE ( 'NONE', *, *, #68890, .F. ) ;
#62247=CARTESIAN_POINT ( 'NONE',  ( 3.211159895383560947, 9.312499998634407916, 3.211159895383562723 ) ) ;
#62253=CARTESIAN_POINT ( 'NONE',  ( -1.656854249492381248, 6.312500000000000888, -4.000000000000001776 ) ) ;
#62255=CARTESIAN_POINT ( 'NONE',  ( -1.881053915767121776, 7.624999998634407916, -4.541265875000002339 ) ) ;
#62264=CARTESIAN_POINT ( 'NONE',  ( -8.342170076843785083E-16, 21.06249999863440792, 4.541265875000002339 ) ) ;
#62304=EDGE_CURVE ( 'NONE', #8230, #42656, #3902, .T. ) ;
#62326=CARTESIAN_POINT ( 'NONE',  ( 0.000000000000000000, 0.000000000000000000, -4.000000000000001776 ) ) ;
#62332=CARTESIAN_POINT ( 'NONE',  ( 1.881053915767122664, 12.24999999863440792, 4.541265875000001451 ) ) ;
#62340=CARTESIAN_POINT ( 'NONE',  ( 1.656854249492381914, 11.56249999726881583, 4.000000000000000888 ) ) ;
#62347=CARTESIAN_POINT ( 'NONE',  ( 2.780723358947928197E-16, 11.56249999863440614, -4.541265875000002339 ) ) ;
#62354=CARTESIAN_POINT ( 'NONE',  ( -4.000000000000001776, 18.50000000000000000, -4.898587196589415787E-16 ) ) ;
#62392=CARTESIAN_POINT ( 'NONE',  ( -4.541265875000003227, 12.99999999863440969, 1.881053915767121110 ) ) ;
#62424=CARTESIAN_POINT ( 'NONE',  ( 2.780723358947928197E-16, 0.6874999986344068059, -4.541265875000002339 ) ) ;
#62435=CARTESIAN_POINT ( 'NONE',  ( 2.780723358947928197E-16, 20.68749999863440436, -4.541265875000002339 ) ) ;
#62453=ORIENTED_EDGE ( 'NONE', *, *, #36131, .T. ) ;
#62479=CARTESIAN_POINT ( 'NONE',  ( -4.541265875000002339, 18.74999999863440436, -1.881053915767121998 ) ) ;
#62516=EDGE_LOOP ( 'NONE', ( #73818, #36663, #63565 ) ) ;
#62536=CARTESIAN_POINT ( 'NONE',  ( -4.000000000000001776, 20.43750000000000000, -1.656854249492381470 ) ) ;
#62537=CARTESIAN_POINT ( 'NONE',  ( 1.881053915767121998, 21.49999999863440792, -4.541265875000002339 ) ) ;
#62560=CARTESIAN_POINT ( 'NONE',  ( 0.000000000000000000, 0.000000000000000000, 0.000000000000000000 ) ) ;
#62570=CARTESIAN_POINT ( 'NONE',  ( 2.449293598294707893E-16, 10.25000000000000000, -4.000000000000001776 ) ) ;
#62610=ORIENTED_EDGE ( 'NONE', *, *, #20794, .F. ) ;
#62618=CARTESIAN_POINT ( 'NONE',  ( -4.541265875000002339, 9.937499998634406140, -5.561446717895856393E-16 ) ) ;
#62625=CARTESIAN_POINT ( 'NONE',  ( 1.656854249492381914, 8.812500000000000000, 4.000000000000000888 ) ) ;
#62626=CARTESIAN_POINT ( 'NONE',  ( -1.656854249492383691, 20.43749999726881228, 4.000000000000000888 ) ) ;
#62627=CARTESIAN_POINT ( 'NONE',  ( -1.881053915767121776, 8.624999998634407916, -4.541265875000002339 ) ) ;
#62648=FACE_OUTER_BOUND ( 'NONE', #20589, .T. ) ;
#62664=DIRECTION ( 'NONE',  ( -0.000000000000000000, -1.000000000000000000, -0.000000000000000000 ) ) ;
#62700=CARTESIAN_POINT ( 'NONE',  ( -4.541265875000003227, 13.99999999863440792, 1.881053915767121110 ) ) ;
#62711=CARTESIAN_POINT ( 'NONE',  ( -1.656854249492383691, 11.43749999726881406, 4.000000000000000888 ) ) ;
#62712=CARTESIAN_POINT ( 'NONE',  ( 4.000000000000001776, 18.06250000000000000, -1.656854249492381248 ) ) ;
#62719=CARTESIAN_POINT ( 'NONE',  ( -4.541265875000002339, 8.749999998634406140, -1.881053915767121998 ) ) ;
#62720=CARTESIAN_POINT ( 'NONE',  ( 4.000000000000001776, 0.06250000000000018041, -1.656854249492381248 ) ) ;
#62753=CARTESIAN_POINT ( 'NONE',  ( 0.000000000000000000, 25.94987437106619765, 1.000000000000000000 ) ) ;
#62759=CARTESIAN_POINT ( 'NONE',  ( -3.211159895383562723, 13.06249999863440792, 3.211159895383561391 ) ) ;
#62805=CARTESIAN_POINT ( 'NONE',  ( -4.541265875000002339, 20.93749999863440436, -5.561446717895856393E-16 ) ) ;
#62814=VERTEX_POINT ( 'NONE', #61493 ) ;
#62850=CARTESIAN_POINT ( 'NONE',  ( -1.881053915767124440, 1.124999998634406584, 4.541265875000001451 ) ) ;
#62861=CIRCLE ( 'NONE', #26672, 4.000000000000002665 ) ;
#62878=CARTESIAN_POINT ( 'NONE',  ( -7.347880794884122694E-16, 6.499999997268813168, 4.000000000000001776 ) ) ;
#62884=VERTEX_POINT ( 'NONE', #19996 ) ;
#62893=EDGE_LOOP ( 'NONE', ( #17076, #3527, #42635, #19755 ) ) ;
#62911=CARTESIAN_POINT ( 'NONE',  ( -7.347880794884122694E-16, 19.75000000000000000, 4.000000000000001776 ) ) ;
#62948=CARTESIAN_POINT ( 'NONE',  ( 2.828427124746191623, 17.87499999726881583, -2.828427124746191623 ) ) ;
#62949=CARTESIAN_POINT ( 'NONE',  ( 3.211159895383560947, 10.18749999863440614, 3.211159895383562723 ) ) ;
#62996=CARTESIAN_POINT ( 'NONE',  ( 4.541265875000002339, 6.499999998634407028, -1.881053915767121554 ) ) ;
#63001=CARTESIAN_POINT ( 'NONE',  ( 2.449293598294707893E-16, 7.250000000000000000, -4.000000000000001776 ) ) ;
#63002=CARTESIAN_POINT ( 'NONE',  ( 1.656854249492381248, 21.93749999726881228, -4.000000000000001776 ) ) ;
#63003=CARTESIAN_POINT ( 'NONE',  ( 1.881053915767122664, 12.12499999863440792, 4.541265875000001451 ) ) ;
#63010=CARTESIAN_POINT ( 'NONE',  ( -4.000000000000001776, 10.43750000000000000, -1.656854249492381470 ) ) ;
#63080=CARTESIAN_POINT ( 'NONE',  ( -3.211159895383562723, 11.06249999863440792, 3.211159895383561391 ) ) ;
#63090=CARTESIAN_POINT ( 'NONE',  ( -2.828427124746190735, 11.12499999726881406, -2.828427124746191623 ) ) ;
#63097=CARTESIAN_POINT ( 'NONE',  ( 0.000000000000000000, 0.000000000000000000, 0.000000000000000000 ) ) ;
#63098=CARTESIAN_POINT ( 'NONE',  ( 1.881053915767121776, 8.499999998634406140, -4.541265875000002339 ) ) ;
#63099=CARTESIAN_POINT ( 'NONE',  ( 2.828427124746191623, 0.1250000000000001943, -2.828427124746191623 ) ) ;
#63142=CARTESIAN_POINT ( 'NONE',  ( -8.342170076843785083E-16, 11.18749999863440792, 4.541265875000002339 ) ) ;
#63172=CARTESIAN_POINT ( 'NONE',  ( 1.881053915767121998, 1.624999998634407028, -4.541265875000002339 ) ) ;
#63182=CARTESIAN_POINT ( 'NONE',  ( -4.541265875000003227, 20.99999999863440792, 1.881053915767121110 ) ) ;
#63225=CARTESIAN_POINT ( 'NONE',  ( 3.211159895383560947, 2.312499998634407028, 3.211159895383562723 ) ) ;
#63232=CARTESIAN_POINT ( 'NONE',  ( -7.071067811865484387, 22.99999999999999645, -1.000000000000000000 ) ) ;
#63245=EDGE_CURVE ( 'NONE', #30314, #57513, #42429, .T. ) ;
#63279=CARTESIAN_POINT ( 'NONE',  ( 1.881053915767121776, 2.499999998634407028, -4.541265875000002339 ) ) ;
#63297=CARTESIAN_POINT ( 'NONE',  ( 2.828427124746191623, 21.12500000000000000, -2.828427124746191623 ) ) ;
#63318=CARTESIAN_POINT ( 'NONE',  ( 2.780723358947928197E-16, 8.562499998634407916, -4.541265875000002339 ) ) ;
#63359=CARTESIAN_POINT ( 'NONE',  ( -3.211159895383562723, 9.062499998634407916, 3.211159895383561391 ) ) ;
#63364=CARTESIAN_POINT ( 'NONE',  ( -7.347880794884122694E-16, 8.750000000000000000, 4.000000000000001776 ) ) ;
#63366=CARTESIAN_POINT ( 'NONE',  ( -4.541265875000003227, 11.87499999863440792, 1.881053915767121110 ) ) ;
#63374=( BOUNDED_CURVE ( )  B_SPLINE_CURVE ( 2, ( #2061, #1710, #19772, #58679, #31477, #71079, #18678, #24687, #41687 ),
 .UNSPECIFIED., .F., .F. ) 
 B_SPLINE_CURVE_WITH_KNOTS ( ( 3, 2, 2, 2, 3 ),
 ( 0.7386363636363636465, 0.7443181818181817677, 0.7500000000000000000, 0.7556818181818182323, 0.7613636363636363535 ),
 .UNSPECIFIED. ) 
 CURVE ( )  GEOMETRIC_REPRESENTATION_ITEM ( )  RATIONAL_B_SPLINE_CURVE ( ( 1.000000000000000000, 0.9238795325112867385, 1.000000000000000000, 0.9238795325112867385, 1.000000000000000000, 0.9238795325112867385, 1.000000000000000000, 0.9238795325112867385, 1.000000000000000000 ) ) 
 REPRESENTATION_ITEM ( '' )  );
#63441=LINE ( 'NONE', #62326, #20793 ) ;
#63447=CARTESIAN_POINT ( 'NONE',  ( 1.881053915767122664, 14.24999999863440969, 4.541265875000001451 ) ) ;
#63457=CARTESIAN_POINT ( 'NONE',  ( 4.000000000000001776, 10.81249999726881406, -1.656854249492381248 ) ) ;
#63458=CARTESIAN_POINT ( 'NONE',  ( 2.780723358947928197E-16, 1.562499998634406584, -4.541265875000002339 ) ) ;
#63468=CARTESIAN_POINT ( 'NONE',  ( -1.881053915767124440, 11.99999999863440969, 4.541265875000001451 ) ) ;
#63469=CARTESIAN_POINT ( 'NONE',  ( 4.000000000000001776, 16.06250000000000000, -1.656854249492381248 ) ) ;
#63514=CARTESIAN_POINT ( 'NONE',  ( 4.541265875000002339, 13.43749999863440792, 0.000000000000000000 ) ) ;
#63530=CARTESIAN_POINT ( 'NONE',  ( 2.449293598294707893E-16, 19.25000000000000000, -4.000000000000001776 ) ) ;
#63541=CARTESIAN_POINT ( 'NONE',  ( 3.211159895383561835, 2.562499998634407028, -3.211159895383561835 ) ) ;
#63553=CARTESIAN_POINT ( 'NONE',  ( -1.881053915767121554, 21.74999999863440436, -4.541265875000002339 ) ) ;
#63565=ORIENTED_EDGE ( 'NONE', *, *, #71378, .F. ) ;
#63594=MECHANICAL_DESIGN_GEOMETRIC_PRESENTATION_REPRESENTATION('',(#74482),#57645);
#63595=CARTESIAN_POINT ( 'NONE',  ( -2.828427124746192067, 11.62500000000000000, 2.828427124746190735 ) ) ;
#63598=CARTESIAN_POINT ( 'NONE',  ( -3.211159895383561391, 21.68749999863440792, -3.211159895383561835 ) ) ;
#63606=CARTESIAN_POINT ( 'NONE',  ( 2.449293598294707893E-16, 15.99999999726881406, -4.000000000000001776 ) ) ;
#63666=ORIENTED_EDGE ( 'NONE', *, *, #50082, .T. ) ;
#63669=ORIENTED_EDGE ( 'NONE', *, *, #8568, .F. ) ;
#63689=CARTESIAN_POINT ( 'NONE',  ( -3.211159895383561391, 8.687499998634407916, -3.211159895383561835 ) ) ;
#63713=( BOUNDED_CURVE ( )  B_SPLINE_CURVE ( 2, ( #40444, #30231, #35533, #52508, #29865, #47203, #41550, #52879, #58549 ),
 .UNSPECIFIED., .F., .F. ) 
 B_SPLINE_CURVE_WITH_KNOTS ( ( 3, 2, 2, 2, 3 ),
 ( 0.3750000000000000000, 0.3806818181818181768, 0.3863636363636363535, 0.3920454545454545858, 0.3977272727272727626 ),
 .UNSPECIFIED. ) 
 CURVE ( )  GEOMETRIC_REPRESENTATION_ITEM ( )  RATIONAL_B_SPLINE_CURVE ( ( 1.000000000000000000, 0.9238795325112867385, 1.000000000000000000, 0.9238795325112867385, 1.000000000000000000, 0.9238795325112867385, 1.000000000000000000, 0.9238795325112859613, 1.000000000000000666 ) ) 
 REPRESENTATION_ITEM ( '' )  );
#63716=ORIENTED_EDGE ( 'NONE', *, *, #49425, .T. ) ;
#63734=CARTESIAN_POINT ( 'NONE',  ( 4.541265875000002339, 12.49999999863440969, -1.881053915767121554 ) ) ;
#63736=ADVANCED_FACE ( 'NONE', ( #39068 ), #43977, .T. ) ;
#63740=CARTESIAN_POINT ( 'NONE',  ( 4.000000000000000888, 10.93750000000000000, 1.656854249492384135 ) ) ;
#63742=CARTESIAN_POINT ( 'NONE',  ( 4.541265875000001451, 11.24999999863441147, 1.881053915767124440 ) ) ;
#63777=LINE ( 'NONE', #1169, #4845 ) ;
#63812=EDGE_CURVE ( 'NONE', #31431, #43256, #71953, .T. ) ;
#63818=DIRECTION ( 'NONE',  ( 0.000000000000000000, 0.000000000000000000, -1.000000000000000000 ) ) ;
#63823=CARTESIAN_POINT ( 'NONE',  ( -4.541265875000003227, 12.99999999863440969, 1.881053915767121110 ) ) ;
#63827=CARTESIAN_POINT ( 'NONE',  ( 3.211159895383560947, 1.312499998634406806, 3.211159895383562723 ) ) ;
#63834=CARTESIAN_POINT ( 'NONE',  ( -1.656854249492383691, 1.687500000000000222, 4.000000000000000888 ) ) ;
#63835=CARTESIAN_POINT ( 'NONE',  ( 2.828427124746190291, 8.624999997268814056, 2.828427124746192067 ) ) ;
#63836=CARTESIAN_POINT ( 'NONE',  ( 4.541265875000002339, 0.3124999986344066949, 0.000000000000000000 ) ) ;
#63843=CARTESIAN_POINT ( 'NONE',  ( -4.541265875000003227, 9.874999998634404363, 1.881053915767121110 ) ) ;
#63844=VECTOR ( 'NONE', #61625, 1000.000000000000000 ) ;
#63888=CARTESIAN_POINT ( 'NONE',  ( 4.541265875000001451, 12.37499999863440969, 1.881053915767124440 ) ) ;
#63893=ORIENTED_EDGE ( 'NONE', *, *, #18092, .F. ) ;
#63918=CARTESIAN_POINT ( 'NONE',  ( -4.541265875000002339, 1.874999998634406806, -1.881053915767121998 ) ) ;
#63932=CARTESIAN_POINT ( 'NONE',  ( -4.000000000000001776, 15.50000000000000000, -4.898587196589415787E-16 ) ) ;
#63933=CARTESIAN_POINT ( 'NONE',  ( -3.211159895383561391, 18.81249999863440436, -3.211159895383561835 ) ) ;
#63980=CARTESIAN_POINT ( 'NONE',  ( 3.211159895383560947, 1.312499998634406806, 3.211159895383562723 ) ) ;
#64002=EDGE_CURVE ( 'NONE', #45255, #282, #30975, .T. ) ;
#64067=EDGE_CURVE ( 'NONE', #61795, #46255, #23721, .T. ) ;
#64073=CARTESIAN_POINT ( 'NONE',  ( -4.541265875000003227, 11.87499999863440969, 1.881053915767121110 ) ) ;
#64097=ORIENTED_EDGE ( 'NONE', *, *, #17153, .F. ) ;
#64100=CARTESIAN_POINT ( 'NONE',  ( -7.347880794884122694E-16, 21.49999999726881583, 4.000000000000001776 ) ) ;
#64104=CARTESIAN_POINT ( 'NONE',  ( 0.000000000000000000, 0.000000000000000000, 0.000000000000000000 ) ) ;
#64114=AXIS2_PLACEMENT_3D ( 'NONE', #52681, #1015, #64369 ) ;
#64115=CARTESIAN_POINT ( 'NONE',  ( -2.828427124746190735, 12.37500000000000000, -2.828427124746191623 ) ) ;
#64117=CARTESIAN_POINT ( 'NONE',  ( -8.342170076843785083E-16, 13.06249999863440792, 4.541265875000002339 ) ) ;
#64124=CARTESIAN_POINT ( 'NONE',  ( -7.347880794884122694E-16, 6.499999997268813168, 4.000000000000001776 ) ) ;
#64131=ORIENTED_EDGE ( 'NONE', *, *, #73268, .F. ) ;
#64132=ORIENTED_EDGE ( 'NONE', *, *, #40779, .F. ) ;
#64171=DIRECTION ( 'NONE',  ( -0.000000000000000000, -1.000000000000000000, -0.000000000000000000 ) ) ;
#64188=CARTESIAN_POINT ( 'NONE',  ( 2.449293598294707893E-16, 14.99999999726881406, -4.000000000000001776 ) ) ;
#64202=CARTESIAN_POINT ( 'NONE',  ( -1.881053915767121776, 17.74999999863440792, -4.541265875000002339 ) ) ;
#64206=FACE_OUTER_BOUND ( 'NONE', #2379, .T. ) ;
#64210=CARTESIAN_POINT ( 'NONE',  ( 4.000000000000001776, 2.062500000000000000, -1.656854249492381248 ) ) ;
#64211=CARTESIAN_POINT ( 'NONE',  ( -4.000000000000002665, 14.31249999726881406, 1.656854249492380804 ) ) ;
#64215=FACE_OUTER_BOUND ( 'NONE', #19573, .T. ) ;
#64218=CARTESIAN_POINT ( 'NONE',  ( 3.211159895383561835, 13.43749999863440614, -3.211159895383561835 ) ) ;
#64219=CARTESIAN_POINT ( 'NONE',  ( 4.000000000000000888, 11.93750000000000000, 1.656854249492384135 ) ) ;
#64245=CARTESIAN_POINT ( 'NONE',  ( -3.211159895383561391, 1.687499998634406584, -3.211159895383561835 ) ) ;
#64250=( BOUNDED_CURVE ( )  B_SPLINE_CURVE ( 2, ( #6274, #69638, #23976, #17200, #46983, #46245, #63595, #70016, #69265 ),
 .UNSPECIFIED., .F., .F. ) 
 B_SPLINE_CURVE_WITH_KNOTS ( ( 3, 2, 2, 2, 3 ),
 ( 0.5113636363636363535, 0.5170454545454545858, 0.5227272727272727071, 0.5284090909090909394, 0.5340909090909090606 ),
 .UNSPECIFIED. ) 
 CURVE ( )  GEOMETRIC_REPRESENTATION_ITEM ( )  RATIONAL_B_SPLINE_CURVE ( ( 1.000000000000000000, 0.9238795325112867385, 1.000000000000000000, 0.9238795325112867385, 1.000000000000000000, 0.9238795325112867385, 1.000000000000000000, 0.9238795325112867385, 1.000000000000000000 ) ) 
 REPRESENTATION_ITEM ( '' )  );
#64263=CARTESIAN_POINT ( 'NONE',  ( -3.211159895383562723, 18.06249999863440792, 3.211159895383561391 ) ) ;
#64280=ORIENTED_EDGE ( 'NONE', *, *, #13625, .T. ) ;
#64291=CARTESIAN_POINT ( 'NONE',  ( -8.342170076843785083E-16, 3.187499998634407028, 4.541265875000002339 ) ) ;
#64304=CARTESIAN_POINT ( 'NONE',  ( 4.000000000000000888, 8.937500000000001776, 1.656854249492384135 ) ) ;
#64305=CARTESIAN_POINT ( 'NONE',  ( -4.000000000000002665, 1.312499997268813390, 1.656854249492380804 ) ) ;
#64351=CARTESIAN_POINT ( 'NONE',  ( -3.211159895383562723, 21.93749999863440792, 3.211159895383561391 ) ) ;
#64369=DIRECTION ( 'NONE',  ( -1.000000000000000000, 0.000000000000000000, 0.000000000000000000 ) ) ;
#64378=CARTESIAN_POINT ( 'NONE',  ( 4.000000000000001776, 9.812499997268814056, -1.656854249492381248 ) ) ;
#64392=CARTESIAN_POINT ( 'NONE',  ( 3.856379400883930941, 21.99999999999998934, 1.388370628458741596 ) ) ;
#64395=EDGE_LOOP ( 'NONE', ( #11841, #42160, #36708, #18474 ) ) ;
#64403=ORIENTED_EDGE ( 'NONE', *, *, #65047, .T. ) ;
#64415=CARTESIAN_POINT ( 'NONE',  ( -3.834411065495477722, 22.00000000000000000, -1.980039758230538016 ) ) ;
#64445=CARTESIAN_POINT ( 'NONE',  ( -1.881053915767121554, 9.624999998634404363, -4.541265875000002339 ) ) ;
#64458=CARTESIAN_POINT ( 'NONE',  ( 1.656854249492381248, 8.937499997268814056, -4.000000000000001776 ) ) ;
#64463=CARTESIAN_POINT ( 'NONE',  ( -7.347880794884122694E-16, 12.49999999726881406, 4.000000000000001776 ) ) ;
#64475=CARTESIAN_POINT ( 'NONE',  ( 4.270632937500002058, 0.5937499979516099868, 0.000000000000000000 ) ) ;
#64488=ADVANCED_FACE ( 'NONE', ( #51028 ), #6133, .T. ) ;
#64489=CARTESIAN_POINT ( 'NONE',  ( -2.828427124746192067, 11.62500000000000000, 2.828427124746190735 ) ) ;
#64491=CARTESIAN_POINT ( 'NONE',  ( 4.541265875000002339, 12.31249999863440792, 0.000000000000000000 ) ) ;
#64532=CARTESIAN_POINT ( 'NONE',  ( 0.000000000000000000, 15.99999999999998579, 1.000000000000000000 ) ) ;
#64571=CARTESIAN_POINT ( 'NONE',  ( -3.211159895383561391, 17.81249999863440792, -3.211159895383561835 ) ) ;
#64575=CARTESIAN_POINT ( 'NONE',  ( 1.881053915767122664, 1.249999998634407028, 4.541265875000001451 ) ) ;
#64581=CARTESIAN_POINT ( 'NONE',  ( 2.828427124746191623, 0.1250000000000001943, -2.828427124746191623 ) ) ;
#64582=CARTESIAN_POINT ( 'NONE',  ( 4.000000000000001776, 14.74999999726881406, 0.000000000000000000 ) ) ;
#64583=CARTESIAN_POINT ( 'NONE',  ( -1.881053915767124440, 0.9999999986344065839, 4.541265875000001451 ) ) ;
#64590=CARTESIAN_POINT ( 'NONE',  ( 1.881053915767121776, 13.49999999863440969, -4.541265875000002339 ) ) ;
#64619=CARTESIAN_POINT ( 'NONE',  ( 1.881053915767122664, 1.124999998634406584, 4.541265875000001451 ) ) ;
#64622=CARTESIAN_POINT ( 'NONE',  ( -7.347880794884122694E-16, 4.750000000000000000, 4.000000000000001776 ) ) ;
#64635=CARTESIAN_POINT ( 'NONE',  ( -3.211159895383562723, 15.06249999863440792, 3.211159895383561391 ) ) ;
#64658=CARTESIAN_POINT ( 'NONE',  ( -4.541265875000003227, 5.999999998634406140, 1.881053915767121110 ) ) ;
#64668=CARTESIAN_POINT ( 'NONE',  ( -4.000000000000001776, 3.249999997268813612, -4.898587196589415787E-16 ) ) ;
#64676=CARTESIAN_POINT ( 'NONE',  ( -1.881053915767121554, 1.624999998634407028, -4.541265875000002339 ) ) ;
#64689=ADVANCED_FACE ( 'NONE', ( #59659 ), #13125, .F. ) ;
#64721=CARTESIAN_POINT ( 'NONE',  ( -1.881053915767121554, 5.749999998634407028, -4.541265875000002339 ) ) ;
#64754=CARTESIAN_POINT ( 'NONE',  ( 3.454596936255384776, 22.00000000000000711, 2.354823634152921841 ) ) ;
#64762=AXIS2_PLACEMENT_3D ( 'NONE', #39308, #33290, #27983 ) ;
#64777=CARTESIAN_POINT ( 'NONE',  ( -4.000000000000002665, 15.31249999726881406, 1.656854249492380582 ) ) ;
#64780=VECTOR ( 'NONE', #62664, 1000.000000000000000 ) ;
#64781=EDGE_CURVE ( 'NONE', #43772, #21170, #5005, .T. ) ;
#64789=DIRECTION ( 'NONE',  ( -0.000000000000000000, -1.000000000000000000, -0.000000000000000000 ) ) ;
#64805=CARTESIAN_POINT ( 'NONE',  ( 3.211159895383561835, 12.43749999863440792, -3.211159895383561835 ) ) ;
#64848=CARTESIAN_POINT ( 'NONE',  ( -1.656854249492383691, 12.68750000000000178, 4.000000000000000888 ) ) ;
#64850=CARTESIAN_POINT ( 'NONE',  ( 4.541265875000002339, 17.37499999863440436, -1.881053915767121776 ) ) ;
#64889=DIRECTION ( 'NONE',  ( -0.000000000000000000, -1.000000000000000000, -0.000000000000000000 ) ) ;
#64915=CARTESIAN_POINT ( 'NONE',  ( -7.347880794884122694E-16, 3.750000000000000000, 4.000000000000001776 ) ) ;
#64928=CARTESIAN_POINT ( 'NONE',  ( -8.342170076843785083E-16, 18.18749999863440792, 4.541265875000002339 ) ) ;
#64932=CARTESIAN_POINT ( 'NONE',  ( -4.541265875000003227, 0.9999999986344068059, 1.881053915767121110 ) ) ;
#64936=CARTESIAN_POINT ( 'NONE',  ( 2.449293598294707893E-16, 1.250000000000000222, -4.000000000000001776 ) ) ;
#64937=CARTESIAN_POINT ( 'NONE',  ( 1.656854249492381914, 14.56249999726881228, 4.000000000000000888 ) ) ;
#64939=ORIENTED_EDGE ( 'NONE', *, *, #68863, .F. ) ;
#64945=CARTESIAN_POINT ( 'NONE',  ( 1.881053915767122664, 13.12499999863440969, 4.541265875000001451 ) ) ;
#64949=ORIENTED_EDGE ( 'NONE', *, *, #57387, .T. ) ;
#64971=CARTESIAN_POINT ( 'NONE',  ( -1.881053915767124440, 1.999999998634406806, 4.541265875000001451 ) ) ;
#64990=CARTESIAN_POINT ( 'NONE',  ( 2.780723358947928197E-16, 14.68749999863440792, -4.541265875000002339 ) ) ;
#65014=CARTESIAN_POINT ( 'NONE',  ( -4.541265875000003227, 2.999999998634407028, 1.881053915767121110 ) ) ;
#65023=CARTESIAN_POINT ( 'NONE',  ( -7.347880794884122694E-16, 8.750000000000000000, 4.000000000000001776 ) ) ;
#65024=CARTESIAN_POINT ( 'NONE',  ( -4.000000000000002665, 2.312499997268813168, 1.656854249492380804 ) ) ;
#65030=CARTESIAN_POINT ( 'NONE',  ( 3.211159895383560947, 1.187499998634406806, 3.211159895383562723 ) ) ;
#65047=EDGE_CURVE ( 'NONE', #58564, #25107, #30425, .T. ) ;
#65057=CARTESIAN_POINT ( 'NONE',  ( 2.449293598294707893E-16, 4.999999997268813168, -4.000000000000001776 ) ) ;
#65071=CARTESIAN_POINT ( 'NONE',  ( 1.881053915767122664, 6.249999998634407916, 4.541265875000001451 ) ) ;
#65084=ADVANCED_FACE ( 'NONE', ( #13422 ), #48131, .T. ) ;
#65119=CARTESIAN_POINT ( 'NONE',  ( 2.780723358947928197E-16, 13.68749999863440614, -4.541265875000002339 ) ) ;
#65120=ORIENTED_EDGE ( 'NONE', *, *, #56245, .F. ) ;
#65142=CARTESIAN_POINT ( 'NONE',  ( -2.828427124746190735, 9.124999997268814056, -2.828427124746191623 ) ) ;
#65144=ORIENTED_EDGE ( 'NONE', *, *, #53181, .F. ) ;
#65163=CARTESIAN_POINT ( 'NONE',  ( 2.780723358947928197E-16, 14.56249999863440792, -4.541265875000002339 ) ) ;
#65168=ORIENTED_EDGE ( 'NONE', *, *, #33789, .T. ) ;
#65202=VECTOR ( 'NONE', #13043, 1000.000000000000000 ) ;
#65212=CARTESIAN_POINT ( 'NONE',  ( -1.656854249492383691, 13.68750000000000000, 4.000000000000000888 ) ) ;
#65213=CARTESIAN_POINT ( 'NONE',  ( -1.881053915767124440, 15.99999999863440614, 4.541265875000001451 ) ) ;
#65221=CARTESIAN_POINT ( 'NONE',  ( 4.000000000000001776, 13.74999999726881583, 0.000000000000000000 ) ) ;
#65247=CARTESIAN_POINT ( 'NONE',  ( 0.000000000000000000, 0.000000000000000000, 0.000000000000000000 ) ) ;
#65280=CARTESIAN_POINT ( 'NONE',  ( 4.000000000000000888, 6.937500000000000000, 1.656854249492384135 ) ) ;
#65297=CARTESIAN_POINT ( 'NONE',  ( 4.541265875000002339, 18.49999999863440436, -1.881053915767121776 ) ) ;
#65310=CARTESIAN_POINT ( 'NONE',  ( -1.656854249492383691, 12.43749999726881406, 4.000000000000000888 ) ) ;
#65311=CARTESIAN_POINT ( 'NONE',  ( 3.211159895383561835, 3.437499998634407028, -3.211159895383561835 ) ) ;
#65317=CARTESIAN_POINT ( 'NONE',  ( -1.881053915767121554, 12.62499999863441147, -4.541265875000002339 ) ) ;
#65348=CARTESIAN_POINT ( 'NONE',  ( -4.541265875000002339, 2.812499998634407028, -5.561446717895856393E-16 ) ) ;
#65366=CARTESIAN_POINT ( 'NONE',  ( 4.541265875000001451, 16.37499999863440436, 1.881053915767124440 ) ) ;
#65381=CARTESIAN_POINT ( 'NONE',  ( 2.449293598294707893E-16, 17.25000000000000000, -4.000000000000001776 ) ) ;
#65389=CARTESIAN_POINT ( 'NONE',  ( -3.211159895383561391, 3.812499998634407028, -3.211159895383561835 ) ) ;
#65400=CARTESIAN_POINT ( 'NONE',  ( -4.000000000000001776, 2.249999997268813612, -4.898587196589415787E-16 ) ) ;
#65406=CARTESIAN_POINT ( 'NONE',  ( 3.211159895383561835, 0.4374999986344066949, -3.211159895383561835 ) ) ;
#65441=AXIS2_PLACEMENT_3D ( 'NONE', #44368, #55702, #9290 ) ;
#65450=CARTESIAN_POINT ( 'NONE',  ( -3.211159895383561391, 2.812499998634407028, -3.211159895383561835 ) ) ;
#65463=DIRECTION ( 'NONE',  ( 1.000000000000000000, -0.000000000000000000, -0.000000000000000000 ) ) ;
#65497=CARTESIAN_POINT ( 'NONE',  ( -3.211159895383562723, 11.06249999863440792, 3.211159895383561391 ) ) ;
#65508=CARTESIAN_POINT ( 'NONE',  ( 4.000000000000001776, 20.06250000000000000, -1.656854249492381248 ) ) ;
#65542=CARTESIAN_POINT ( 'NONE',  ( 4.541265875000002339, 13.37499999863440792, -1.881053915767121554 ) ) ;
#65568=CARTESIAN_POINT ( 'NONE',  ( -7.347880794884122694E-16, 3.499999997268812724, 4.000000000000001776 ) ) ;
#65586=CARTESIAN_POINT ( 'NONE',  ( -1.656854249492381248, 15.31249999999999822, -4.000000000000001776 ) ) ;
#65587=CARTESIAN_POINT ( 'NONE',  ( 3.211159895383560947, 14.18749999863440792, 3.211159895383562723 ) ) ;
#65611=CARTESIAN_POINT ( 'NONE',  ( -1.656854249492383468, 0.6875000000000004441, 4.000000000000000888 ) ) ;
#65620=DIRECTION ( 'NONE',  ( 0.000000000000000000, 0.000000000000000000, -1.000000000000000000 ) ) ;
#65665=CARTESIAN_POINT ( 'NONE',  ( -4.541265875000003227, 14.99999999863440969, 1.881053915767121110 ) ) ;
#65669=CARTESIAN_POINT ( 'NONE',  ( -3.211159895383561391, 3.812499998634407028, -3.211159895383561835 ) ) ;
#65675=CARTESIAN_POINT ( 'NONE',  ( -2.828427124746192067, 4.625000000000000000, 2.828427124746190735 ) ) ;
#65676=CARTESIAN_POINT ( 'NONE',  ( 1.656854249492381248, 15.93749999726881228, -4.000000000000001776 ) ) ;
#65677=CARTESIAN_POINT ( 'NONE',  ( 4.541265875000002339, 5.312499998634407028, 0.000000000000000000 ) ) ;
#65684=CARTESIAN_POINT ( 'NONE',  ( -4.541265875000003227, 15.87499999863440436, 1.881053915767121110 ) ) ;
#65712=CARTESIAN_POINT ( 'NONE',  ( -3.211159895383561391, 2.687499998634407028, -3.211159895383561835 ) ) ;
#65725=CARTESIAN_POINT ( 'NONE',  ( -7.347880794884122694E-16, 9.499999997268814056, 4.000000000000001776 ) ) ;
#65732=CARTESIAN_POINT ( 'NONE',  ( 1.881053915767122664, 16.24999999863440436, 4.541265875000001451 ) ) ;
#65733=CARTESIAN_POINT ( 'NONE',  ( 4.000000000000001776, 11.06250000000000000, -1.656854249492381248 ) ) ;
#65757=CARTESIAN_POINT ( 'NONE',  ( 3.211159895383561835, 6.562499998634407028, -3.211159895383561835 ) ) ;
#65762=CARTESIAN_POINT ( 'NONE',  ( 0.000000000000000000, 0.000000000000000000, 0.000000000000000000 ) ) ;
#65770=CARTESIAN_POINT ( 'NONE',  ( -1.656854249492381248, 1.062499997268813168, -4.000000000000001776 ) ) ;
#65775=CARTESIAN_POINT ( 'NONE',  ( -4.541265875000003227, 3.874999998634407028, 1.881053915767121110 ) ) ;
#65817=CARTESIAN_POINT ( 'NONE',  ( 1.881053915767121776, 3.624999998634407028, -4.541265875000002339 ) ) ;
#65827=ORIENTED_EDGE ( 'NONE', *, *, #1308, .T. ) ;
#65838=ORIENTED_EDGE ( 'NONE', *, *, #25648, .T. ) ;
#65863=CARTESIAN_POINT ( 'NONE',  ( 1.881053915767122664, 11.24999999863440792, 4.541265875000001451 ) ) ;
#65877=CARTESIAN_POINT ( 'NONE',  ( -2.044767169047288391, 21.99999999999996447, -3.615591841833113662 ) ) ;
#65881=VERTEX_POINT ( 'NONE', #2603 ) ;
#65899=LINE ( 'NONE', #3284, #45822 ) ;
#65907=CARTESIAN_POINT ( 'NONE',  ( 3.211159895383560947, 16.18749999863440436, 3.211159895383562723 ) ) ;
#65919=ORIENTED_EDGE ( 'NONE', *, *, #19639, .F. ) ;
#65937=ORIENTED_EDGE ( 'NONE', *, *, #65047, .F. ) ;
#65941=CARTESIAN_POINT ( 'NONE',  ( -1.656854249492383468, 19.68750000000000000, 4.000000000000000888 ) ) ;
#65945=EDGE_CURVE ( 'NONE', #52476, #54437, #56553, .T. ) ;
#65958=CARTESIAN_POINT ( 'NONE',  ( -1.656854249492383691, 17.68750000000000000, 4.000000000000000888 ) ) ;
#65959=CARTESIAN_POINT ( 'NONE',  ( 4.541265875000002339, 14.37499999863440969, -1.881053915767121776 ) ) ;
#66040=CARTESIAN_POINT ( 'NONE',  ( 4.541265875000002339, 21.49999999863440792, -1.881053915767121776 ) ) ;
#66043=CARTESIAN_POINT ( 'NONE',  ( 4.541265875000002339, 5.499999998634407028, -1.881053915767121554 ) ) ;
#66050=CARTESIAN_POINT ( 'NONE',  ( -7.347880794884122694E-16, 2.750000000000000000, 4.000000000000001776 ) ) ;
#66051=CARTESIAN_POINT ( 'NONE',  ( 1.656854249492381914, 17.56249999726881938, 4.000000000000000888 ) ) ;
#66052=CARTESIAN_POINT ( 'NONE',  ( -8.342170076843785083E-16, 4.062499998634407028, 4.541265875000002339 ) ) ;
#66058=CARTESIAN_POINT ( 'NONE',  ( -4.541265875000002339, 19.74999999863440792, -1.881053915767121998 ) ) ;
#66086=CARTESIAN_POINT ( 'NONE',  ( -4.541265875000003227, 4.874999998634406140, 1.881053915767121110 ) ) ;
#66105=CARTESIAN_POINT ( 'NONE',  ( -4.541265875000002339, 18.93749999863440436, -5.561446717895856393E-16 ) ) ;
#66131=CARTESIAN_POINT ( 'NONE',  ( -4.541265875000003227, 7.999999998634407028, 1.881053915767121110 ) ) ;
#66143=CARTESIAN_POINT ( 'NONE',  ( -1.656854249492383691, 6.437499997268812280, 4.000000000000000888 ) ) ;
#66147=CARTESIAN_POINT ( 'NONE',  ( 1.881053915767121776, 7.499999998634408804, -4.541265875000002339 ) ) ;
#66151=CARTESIAN_POINT ( 'NONE',  ( -4.000000000000001776, 13.50000000000000000, -4.898587196589415787E-16 ) ) ;
#66192=CARTESIAN_POINT ( 'NONE',  ( 4.541265875000001451, 3.374999998634406584, 1.881053915767124440 ) ) ;
#66239=CARTESIAN_POINT ( 'NONE',  ( -4.541265875000002339, 17.93749999863440792, -5.561446717895856393E-16 ) ) ;
#66256=VERTEX_POINT ( 'NONE', #72182 ) ;
#66261=CARTESIAN_POINT ( 'NONE',  ( -1.656854249492383468, 2.437499997268814056, 4.000000000000000888 ) ) ;
#66265=CARTESIAN_POINT ( 'NONE',  ( 4.898587196589415787E-16, 0.000000000000000000, 4.000000000000001776 ) ) ;
#66282=CARTESIAN_POINT ( 'NONE',  ( 4.541265875000001451, 15.24999999863440969, 1.881053915767124440 ) ) ;
#66316=CARTESIAN_POINT ( 'NONE',  ( 4.000000000000001776, 0.7499999972688131678, 0.000000000000000000 ) ) ;
#66317=CARTESIAN_POINT ( 'NONE',  ( -7.347880794884122694E-16, 11.49999999726881406, 4.000000000000001776 ) ) ;
#66332=CARTESIAN_POINT ( 'NONE',  ( -1.656854249492381248, 16.31250000000000000, -4.000000000000001776 ) ) ;
#66333=CARTESIAN_POINT ( 'NONE',  ( 3.211159895383561835, 15.43749999863440614, -3.211159895383561835 ) ) ;
#66411=CARTESIAN_POINT ( 'NONE',  ( -1.881053915767124440, 20.12499999863441147, 4.541265875000001451 ) ) ;
#66413=ORIENTED_EDGE ( 'NONE', *, *, #73268, .T. ) ;
#66415=CARTESIAN_POINT ( 'NONE',  ( 3.211159895383560947, 2.312499998634407028, 3.211159895383562723 ) ) ;
#66421=CARTESIAN_POINT ( 'NONE',  ( 4.000000000000000888, 3.937500000000000000, 1.656854249492384135 ) ) ;
#66422=CARTESIAN_POINT ( 'NONE',  ( 4.000000000000001776, 18.74999999726881583, 0.000000000000000000 ) ) ;
#66423=CARTESIAN_POINT ( 'NONE',  ( -8.342170076843785083E-16, 5.062499998634407028, 4.541265875000002339 ) ) ;
#66430=CARTESIAN_POINT ( 'NONE',  ( 1.881053915767121776, 16.49999999863440436, -4.541265875000002339 ) ) ;
#66455=CARTESIAN_POINT ( 'NONE',  ( -1.656854249492383468, 3.437499997268814056, 4.000000000000000888 ) ) ;
#66461=CARTESIAN_POINT ( 'NONE',  ( 2.780723358947928197E-16, 6.562499998634407028, -4.541265875000002339 ) ) ;
#66470=EDGE_CURVE ( 'NONE', #68294, #51031, #48766, .T. ) ;
#66479=CARTESIAN_POINT ( 'NONE',  ( 1.881053915767122664, 22.24999999863440792, 4.541265875000001451 ) ) ;
#66500=CARTESIAN_POINT ( 'NONE',  ( -1.881053915767121776, 10.74999999863440969, -4.541265875000002339 ) ) ;
#66509=CARTESIAN_POINT ( 'NONE',  ( 4.000000000000001776, 7.749999997268813168, 0.000000000000000000 ) ) ;
#66515=CARTESIAN_POINT ( 'NONE',  ( 3.211159895383560947, 6.187499998634407028, 3.211159895383562723 ) ) ;
#66528=EDGE_CURVE ( 'NONE', #22328, #22922, #43249, .T. ) ;
#66563=CARTESIAN_POINT ( 'NONE',  ( 1.881053915767122664, 8.249999998634406140, 4.541265875000001451 ) ) ;
#66581=DIRECTION ( 'NONE',  ( -0.000000000000000000, -1.000000000000000000, -0.000000000000000000 ) ) ;
#66609=DIRECTION ( 'NONE',  ( -0.000000000000000000, -1.000000000000000000, -0.000000000000000000 ) ) ;
#66610=CARTESIAN_POINT ( 'NONE',  ( -3.211159895383562723, 14.06249999863440614, 3.211159895383561391 ) ) ;
#66637=DIRECTION ( 'NONE',  ( 0.000000000000000000, 0.000000000000000000, -1.000000000000000000 ) ) ;
#66644=CARTESIAN_POINT ( 'NONE',  ( 4.898587196589415787E-16, 0.000000000000000000, 4.000000000000001776 ) ) ;
#66656=CARTESIAN_POINT ( 'NONE',  ( 4.541265875000002339, 18.31249999863440792, 0.000000000000000000 ) ) ;
#66682=DIRECTION ( 'NONE',  ( -0.000000000000000000, -1.000000000000000000, -0.000000000000000000 ) ) ;
#66712=CARTESIAN_POINT ( 'NONE',  ( -2.828427124746192067, 14.62500000000000000, 2.828427124746190735 ) ) ;
#66713=CARTESIAN_POINT ( 'NONE',  ( 3.211159895383561835, 18.43749999863440436, -3.211159895383561835 ) ) ;
#66743=CARTESIAN_POINT ( 'NONE',  ( 1.656854249492381914, 5.562499997268813168, 4.000000000000000888 ) ) ;
#66775=EDGE_LOOP ( 'NONE', ( #70533, #3330, #7753, #43102 ) ) ;
#66793=CARTESIAN_POINT ( 'NONE',  ( 4.541265875000002339, 20.43749999863440436, 0.000000000000000000 ) ) ;
#66797=CARTESIAN_POINT ( 'NONE',  ( -4.541265875000003227, 2.999999998634407028, 1.881053915767121110 ) ) ;
#66806=CARTESIAN_POINT ( 'NONE',  ( 2.449293598294707893E-16, 5.250000000000000000, -4.000000000000001776 ) ) ;
#66808=CARTESIAN_POINT ( 'NONE',  ( -2.828427124746190735, 17.12499999726881583, -2.828427124746191623 ) ) ;
#66809=CARTESIAN_POINT ( 'NONE',  ( 4.541265875000002339, 2.374999998634407028, -1.881053915767121776 ) ) ;
#66815=CARTESIAN_POINT ( 'NONE',  ( 1.881053915767122664, 18.12499999863440792, 4.541265875000001451 ) ) ;
#66826=CARTESIAN_POINT ( 'NONE',  ( -7.347880794884122694E-16, 21.49999999726881583, 4.000000000000001776 ) ) ;
#66846=CARTESIAN_POINT ( 'NONE',  ( 1.881053915767122664, 7.124999998634407916, 4.541265875000001451 ) ) ;
#66861=CARTESIAN_POINT ( 'NONE',  ( -8.342170076843785083E-16, 19.18749999863440436, 4.541265875000002339 ) ) ;
#66886=CARTESIAN_POINT ( 'NONE',  ( -4.541265875000002339, 6.937499998634407916, -5.561446717895856393E-16 ) ) ;
#66896=CARTESIAN_POINT ( 'NONE',  ( -1.656854249492381248, 5.062499997268813168, -4.000000000000001776 ) ) ;
#66903=CARTESIAN_POINT ( 'NONE',  ( -4.541265875000003227, 4.874999998634406140, 1.881053915767121110 ) ) ;
#66923=CARTESIAN_POINT ( 'NONE',  ( 4.541265875000002339, 0.3124999986344066949, 0.000000000000000000 ) ) ;
#66944=CARTESIAN_POINT ( 'NONE',  ( 2.780723358947928197E-16, 7.687499998634407028, -4.541265875000002339 ) ) ;
#66983=ORIENTED_EDGE ( 'NONE', *, *, #50786, .T. ) ;
#66990=CARTESIAN_POINT ( 'NONE',  ( -8.342170076843785083E-16, 17.18749999863440792, 4.541265875000002339 ) ) ;
#66996=CIRCLE ( 'NONE', #44109, 4.000000000000000000 ) ;
#67035=DIRECTION ( 'NONE',  ( 0.000000000000000000, 0.000000000000000000, -1.000000000000000000 ) ) ;
#67036=CARTESIAN_POINT ( 'NONE',  ( -3.211159895383561391, 16.68749999863440436, -3.211159895383561835 ) ) ;
#67062=FACE_OUTER_BOUND ( 'NONE', #10133, .T. ) ;
#67071=CARTESIAN_POINT ( 'NONE',  ( -2.828427124746190735, 11.12499999726881406, -2.828427124746191623 ) ) ;
#67090=CARTESIAN_POINT ( 'NONE',  ( -2.828427124746190735, 17.37500000000000000, -2.828427124746191623 ) ) ;
#67091=CARTESIAN_POINT ( 'NONE',  ( -4.541265875000002339, 21.74999999863440792, -1.881053915767121998 ) ) ;
#67142=CARTESIAN_POINT ( 'NONE',  ( 2.449293598294707893E-16, 7.999999997268813168, -4.000000000000001776 ) ) ;
#67174=CARTESIAN_POINT ( 'NONE',  ( -8.342170076843785083E-16, 21.18749999863440792, 4.541265875000002339 ) ) ;
#67177=CARTESIAN_POINT ( 'NONE',  ( 2.780723358947928197E-16, 2.687499998634407028, -4.541265875000002339 ) ) ;
#67183=CARTESIAN_POINT ( 'NONE',  ( 2.828427124746191623, 2.125000000000000000, -2.828427124746191623 ) ) ;
#67184=CARTESIAN_POINT ( 'NONE',  ( 4.000000000000000888, 17.68749999726881228, 1.656854249492384135 ) ) ;
#67185=CARTESIAN_POINT ( 'NONE',  ( 1.881053915767122664, 7.124999998634407916, 4.541265875000001451 ) ) ;
#67192=CARTESIAN_POINT ( 'NONE',  ( -3.211159895383561391, 18.68749999863440436, -3.211159895383561835 ) ) ;
#67224=CARTESIAN_POINT ( 'NONE',  ( 4.541265875000002339, 6.312499998634407028, 0.000000000000000000 ) ) ;
#67242=CARTESIAN_POINT ( 'NONE',  ( -3.211159895383561391, 21.81249999863440792, -3.211159895383561835 ) ) ;
#67265=CARTESIAN_POINT ( 'NONE',  ( 4.541265875000002339, 7.437499998634407028, 0.000000000000000000 ) ) ;
#67276=CARTESIAN_POINT ( 'NONE',  ( -2.828427124746192067, 4.374999997268814056, 2.828427124746190735 ) ) ;
#67281=CARTESIAN_POINT ( 'NONE',  ( 3.211159895383561835, 4.437499998634407028, -3.211159895383561835 ) ) ;
#67284=CARTESIAN_POINT ( 'NONE',  ( -4.000000000000001776, 21.43750000000000000, -1.656854249492381470 ) ) ;
#67285=ORIENTED_EDGE ( 'NONE', *, *, #43343, .T. ) ;
#67324=CARTESIAN_POINT ( 'NONE',  ( -1.881053915767121554, 7.749999998634407916, -4.541265875000002339 ) ) ;
#67332=CYLINDRICAL_SURFACE ( 'NONE', #6202, 4.000000000000001776 ) ;
#67343=ORIENTED_EDGE ( 'NONE', *, *, #41486, .T. ) ;
#67350=ORIENTED_EDGE ( 'NONE', *, *, #28295, .F. ) ;
#67351=DIRECTION ( 'NONE',  ( 0.000000000000000000, 0.000000000000000000, -1.000000000000000000 ) ) ;
#67366=CARTESIAN_POINT ( 'NONE',  ( 1.881053915767121776, 16.62499999863440436, -4.541265875000002339 ) ) ;
#67374=EDGE_LOOP ( 'NONE', ( #40446, #25697, #66983, #9972 ) ) ;
#67386=CARTESIAN_POINT ( 'NONE',  ( -2.828427124746192067, 2.374999997268813612, 2.828427124746190735 ) ) ;
#67411=CARTESIAN_POINT ( 'NONE',  ( 4.541265875000002339, 16.37499999863440436, -1.881053915767121554 ) ) ;
#67443=CARTESIAN_POINT ( 'NONE',  ( -1.656854249492383468, 2.687500000000000444, 4.000000000000000888 ) ) ;
#67462=CARTESIAN_POINT ( 'NONE',  ( -7.347880794884122694E-16, 20.75000000000000000, 4.000000000000001776 ) ) ;
#67464=CARTESIAN_POINT ( 'NONE',  ( 4.541265875000001451, 18.24999999863440792, 1.881053915767124440 ) ) ;
#67543=CARTESIAN_POINT ( 'NONE',  ( -4.541265875000002339, 21.93749999863440792, -5.561446717895856393E-16 ) ) ;
#67546=CARTESIAN_POINT ( 'NONE',  ( 4.541265875000002339, 8.437499998634407916, 0.000000000000000000 ) ) ;
#67553=CARTESIAN_POINT ( 'NONE',  ( -2.828427124746190735, 9.375000000000000000, -2.828427124746191623 ) ) ;
#67555=CARTESIAN_POINT ( 'NONE',  ( 4.541265875000002339, 9.312499998634407916, 0.000000000000000000 ) ) ;
#67562=CARTESIAN_POINT ( 'NONE',  ( -4.541265875000003227, 18.87499999863441147, 1.881053915767121110 ) ) ;
#67614=CARTESIAN_POINT ( 'NONE',  ( -4.541265875000002339, 19.87499999863440792, -1.881053915767121998 ) ) ;
#67617=ORIENTED_EDGE ( 'NONE', *, *, #73198, .F. ) ;
#67637=CARTESIAN_POINT ( 'NONE',  ( 4.541265875000001451, 9.374999998634407916, 1.881053915767124440 ) ) ;
#67646=CARTESIAN_POINT ( 'NONE',  ( 1.656854249492381248, 7.937499997268813168, -4.000000000000001776 ) ) ;
#67647=CARTESIAN_POINT ( 'NONE',  ( 1.656854249492406783, 17.81250000000000711, 3.999999999999976019 ) ) ;
#67653=CARTESIAN_POINT ( 'NONE',  ( -1.881053915767124440, 4.999999998634406140, 4.541265875000001451 ) ) ;
#67669=ORIENTED_EDGE ( 'NONE', *, *, #21898, .T. ) ;
#67698=CARTESIAN_POINT ( 'NONE',  ( -4.541265875000002339, 8.937499998634407916, -5.561446717895856393E-16 ) ) ;
#67701=CARTESIAN_POINT ( 'NONE',  ( -7.347880794884122694E-16, 0.7500000000000002220, 4.000000000000001776 ) ) ;
#67725=ORIENTED_EDGE ( 'NONE', *, *, #7136, .F. ) ;
#67730=CARTESIAN_POINT ( 'NONE',  ( -4.000000000000001776, 7.437500000000000888, -1.656854249492381470 ) ) ;
#67742=CARTESIAN_POINT ( 'NONE',  ( -4.541265875000003227, 15.99999999863440614, 1.881053915767121110 ) ) ;
#67750=EDGE_LOOP ( 'NONE', ( #14329, #10108, #50335, #32397 ) ) ;
#67785=CARTESIAN_POINT ( 'NONE',  ( 3.211159895383560947, 18.18749999863440792, 3.211159895383562723 ) ) ;
#67820=CARTESIAN_POINT ( 'NONE',  ( -2.828427124746190735, 20.37500000000000000, -2.828427124746191623 ) ) ;
#67821=ORIENTED_EDGE ( 'NONE', *, *, #7604, .F. ) ;
#67833=CARTESIAN_POINT ( 'NONE',  ( 4.541265875000002339, 0.3124999986344066949, 0.000000000000000000 ) ) ;
#67834=CARTESIAN_POINT ( 'NONE',  ( 4.541265875000002339, 21.37499999863441147, -1.881053915767121776 ) ) ;
#67915=CARTESIAN_POINT ( 'NONE',  ( 4.541265875000001451, 6.374999998634407028, 1.881053915767124440 ) ) ;
#67922=CARTESIAN_POINT ( 'NONE',  ( -1.656854249492383691, 9.687500000000000000, 4.000000000000000888 ) ) ;
#67923=CARTESIAN_POINT ( 'NONE',  ( 1.656854249492381248, 20.93749999726881228, -4.000000000000001776 ) ) ;
#67924=CARTESIAN_POINT ( 'NONE',  ( 3.211159895383561835, 8.437499998634407916, -3.211159895383561835 ) ) ;
#67933=CARTESIAN_POINT ( 'NONE',  ( -1.656854249492393238, 10.31249999999999822, -3.999999999999989786 ) ) ;
#67954=CARTESIAN_POINT ( 'NONE',  ( -7.347880794884122694E-16, 20.49999999726881583, 4.000000000000001776 ) ) ;
#67992=CARTESIAN_POINT ( 'NONE',  ( 0.000000000000000000, 15.99999999999998579, 0.000000000000000000 ) ) ;
#67999=CARTESIAN_POINT ( 'NONE',  ( 4.541265875000002339, 14.49999999863440969, -1.881053915767121776 ) ) ;
#68012=CARTESIAN_POINT ( 'NONE',  ( -7.347880794884122694E-16, 10.49999999726881406, 4.000000000000001776 ) ) ;
#68020=CARTESIAN_POINT ( 'NONE',  ( 4.541265875000001451, 11.24999999863440792, 1.881053915767124440 ) ) ;
#68032=CIRCLE ( 'NONE', #69224, 9.949874371066211864 ) ;
#68066=CARTESIAN_POINT ( 'NONE',  ( -3.211159895383562723, 7.062499998634407028, 3.211159895383561391 ) ) ;
#68069=CARTESIAN_POINT ( 'NONE',  ( -4.000000000000001776, 5.187499997268813168, -1.656854249492381470 ) ) ;
#68075=ADVANCED_FACE ( 'NONE', ( #17165 ), #40184, .F. ) ;
#68078=EDGE_LOOP ( 'NONE', ( #65937, #15098, #39355, #66413 ) ) ;
#68107=CARTESIAN_POINT ( 'NONE',  ( -8.342170076843785083E-16, 19.18749999863440436, 4.541265875000002339 ) ) ;
#68118=CYLINDRICAL_SURFACE ( 'NONE', #2687, 4.000000000000001776 ) ;
#68150=CARTESIAN_POINT ( 'NONE',  ( -3.211159895383561391, 19.68749999863440436, -3.211159895383561835 ) ) ;
#68169=AXIS2_PLACEMENT_3D ( 'NONE', #5103, #27722, #67351 ) ;
#68186=CARTESIAN_POINT ( 'NONE',  ( -7.347880794884122694E-16, 1.499999997268813168, 4.000000000000001776 ) ) ;
#68203=CARTESIAN_POINT ( 'NONE',  ( -4.000000000000002665, 18.56250000000000000, 1.656854249492380804 ) ) ;
#68204=CARTESIAN_POINT ( 'NONE',  ( 4.541265875000002339, 19.37499999863440792, -1.881053915767121776 ) ) ;
#68234=CIRCLE ( 'NONE', #52570, 10.00000000000001243 ) ;
#68286=CARTESIAN_POINT ( 'NONE',  ( -3.211159895383561391, 6.812499998634407028, -3.211159895383561835 ) ) ;
#68290=CARTESIAN_POINT ( 'NONE',  ( -4.000000000000002665, 7.562500000000000000, 1.656854249492380804 ) ) ;
#68291=CARTESIAN_POINT ( 'NONE',  ( -4.000000000000002665, 20.31249999726881583, 1.656854249492380804 ) ) ;
#68292=CARTESIAN_POINT ( 'NONE',  ( 4.541265875000001451, 9.249999998634407916, 1.881053915767124440 ) ) ;
#68294=VERTEX_POINT ( 'NONE', #12616 ) ;
#68318=CARTESIAN_POINT ( 'NONE',  ( 0.000000000000000000, 0.000000000000000000, 0.000000000000000000 ) ) ;
#68358=CARTESIAN_POINT ( 'NONE',  ( -4.000000000000001776, 20.18749999726881228, -1.656854249492381470 ) ) ;
#68371=CARTESIAN_POINT ( 'NONE',  ( -1.881053915767121776, 13.74999999863440969, -4.541265875000002339 ) ) ;
#68381=CARTESIAN_POINT ( 'NONE',  ( -4.000000000000002665, 10.31249999726881406, 1.656854249492380804 ) ) ;
#68388=CARTESIAN_POINT ( 'NONE',  ( -1.881053915767124440, 8.999999998634406140, 4.541265875000001451 ) ) ;
#68428=CARTESIAN_POINT ( 'NONE',  ( 1.881053915767122664, 12.24999999863440969, 4.541265875000001451 ) ) ;
#68470=EDGE_CURVE ( 'NONE', #57749, #28680, #74392, .T. ) ;
#68473=CARTESIAN_POINT ( 'NONE',  ( -3.211159895383561391, 20.81249999863440436, -3.211159895383561835 ) ) ;
#68474=ORIENTED_EDGE ( 'NONE', *, *, #33953, .T. ) ;
#68512=CARTESIAN_POINT ( 'NONE',  ( 4.000000000000000888, 1.937500000000000222, 1.656854249492384135 ) ) ;
#68519=CARTESIAN_POINT ( 'NONE',  ( -3.211159895383561391, 1.812499998634406584, -3.211159895383561835 ) ) ;
#68522=CARTESIAN_POINT ( 'NONE',  ( -4.000000000000001776, 1.437500000000000444, -1.656854249492381470 ) ) ;
#68537=PLANE ( 'NONE',  #21940 ) ;
#68575=CARTESIAN_POINT ( 'NONE',  ( -4.000000000000002665, 19.56250000000000000, 1.656854249492380804 ) ) ;
#68602=VECTOR ( 'NONE', #12772, 1000.000000000000000 ) ;
#68610=CARTESIAN_POINT ( 'NONE',  ( 2.828427124746190291, 16.62499999726881583, 2.828427124746192067 ) ) ;
#68612=CARTESIAN_POINT ( 'NONE',  ( -1.881053915767124440, 8.999999998634406140, 4.541265875000001451 ) ) ;
#68656=CARTESIAN_POINT ( 'NONE',  ( 1.881053915767121776, 6.624999998634407916, -4.541265875000002339 ) ) ;
#68661=CARTESIAN_POINT ( 'NONE',  ( -1.656854249492383691, 6.687500000000000888, 4.000000000000000888 ) ) ;
#68662=CARTESIAN_POINT ( 'NONE',  ( 4.000000000000001776, 22.74999999726881228, 0.000000000000000000 ) ) ;
#68663=CARTESIAN_POINT ( 'NONE',  ( -1.881053915767124440, 8.999999998634407916, 4.541265875000001451 ) ) ;
#68672=CARTESIAN_POINT ( 'NONE',  ( -4.000000000000001776, 10.50000000000000000, -4.898587196589415787E-16 ) ) ;
#68687=DIRECTION ( 'NONE',  ( -0.000000000000000000, -1.000000000000000000, -0.000000000000000000 ) ) ;
#68740=CARTESIAN_POINT ( 'NONE',  ( -4.541265875000002339, 12.93749999863440792, -5.561446717895856393E-16 ) ) ;
#68750=CARTESIAN_POINT ( 'NONE',  ( 2.828427124746191623, 11.87499999726881406, -2.828427124746191623 ) ) ;
#68760=CARTESIAN_POINT ( 'NONE',  ( 4.541265875000001451, 9.249999998634406140, 1.881053915767124440 ) ) ;
#68802=CARTESIAN_POINT ( 'NONE',  ( 4.541265875000001451, 11.37499999863440969, 1.881053915767124440 ) ) ;
#68830=CARTESIAN_POINT ( 'NONE',  ( 3.211159895383560947, 1.312499998634406806, 3.211159895383562723 ) ) ;
#68834=EDGE_CURVE ( 'NONE', #16346, #52055, #58984, .T. ) ;
#68845=CARTESIAN_POINT ( 'NONE',  ( 3.211159895383560947, 19.31249999863440436, 3.211159895383562723 ) ) ;
#68852=EDGE_CURVE ( 'NONE', #13303, #57934, #45962, .T. ) ;
#68863=EDGE_CURVE ( 'NONE', #43256, #28738, #35829, .T. ) ;
#68866=ORIENTED_EDGE ( 'NONE', *, *, #33789, .F. ) ;
#68890=EDGE_CURVE ( 'NONE', #27854, #62814, #53684, .T. ) ;
#68893=CARTESIAN_POINT ( 'NONE',  ( -8.342170076843785083E-16, 2.187499998634407028, 4.541265875000002339 ) ) ;
#68899=ORIENTED_EDGE ( 'NONE', *, *, #43260, .T. ) ;
#68900=LINE ( 'NONE', #28163, #1449 ) ;
#68949=CARTESIAN_POINT ( 'NONE',  ( 4.541265875000002339, 1.374999998634407250, -1.881053915767121554 ) ) ;
#68961=VECTOR ( 'NONE', #39868, 1000.000000000000000 ) ;
#68977=DIRECTION ( 'NONE',  ( -0.000000000000000000, -1.000000000000000000, -0.000000000000000000 ) ) ;
#68987=CARTESIAN_POINT ( 'NONE',  ( -1.881053915767121554, 11.62499999863440969, -4.541265875000002339 ) ) ;
#69015=CARTESIAN_POINT ( 'NONE',  ( 0.000000000000000000, 0.000000000000000000, 0.000000000000000000 ) ) ;
#69028=EDGE_CURVE ( 'NONE', #4559, #2415, #30531, .T. ) ;
#69034=CARTESIAN_POINT ( 'NONE',  ( -1.881053915767124440, 7.124999998634407916, 4.541265875000001451 ) ) ;
#69040=CARTESIAN_POINT ( 'NONE',  ( -1.656854249492383691, 8.687500000000000000, 4.000000000000000888 ) ) ;
#69042=CARTESIAN_POINT ( 'NONE',  ( 2.780723358947928197E-16, 10.56249999863440792, -4.541265875000002339 ) ) ;
#69118=CARTESIAN_POINT ( 'NONE',  ( 4.541265875000001451, 11.37499999863440969, 1.881053915767124440 ) ) ;
#69129=DIRECTION ( 'NONE',  ( 0.000000000000000000, 0.000000000000000000, -1.000000000000000000 ) ) ;
#69130=CARTESIAN_POINT ( 'NONE',  ( -1.656854249492383691, 10.43749999726881228, 4.000000000000000888 ) ) ;
#69131=CARTESIAN_POINT ( 'NONE',  ( -3.211159895383562723, 0.9374999986344068059, 3.211159895383561391 ) ) ;
#69136=CARTESIAN_POINT ( 'NONE',  ( -8.342170076843785083E-16, 11.06249999863440792, 4.541265875000002339 ) ) ;
#69138=CARTESIAN_POINT ( 'NONE',  ( 2.828427124746190291, 15.87500000000000000, 2.828427124746192067 ) ) ;
#69158=CYLINDRICAL_SURFACE ( 'NONE', #41477, 4.000000000000001776 ) ;
#69180=CARTESIAN_POINT ( 'NONE',  ( -3.211159895383561391, 12.81249999863440792, -3.211159895383561835 ) ) ;
#69220=CARTESIAN_POINT ( 'NONE',  ( -7.347880794884122694E-16, 2.750000000000000000, 4.000000000000001776 ) ) ;
#69221=CARTESIAN_POINT ( 'NONE',  ( 4.541265875000002339, 19.49999999863440436, -1.881053915767121554 ) ) ;
#69224=AXIS2_PLACEMENT_3D ( 'NONE', #72200, #36770, #71081 ) ;
#69260=ORIENTED_EDGE ( 'NONE', *, *, #16870, .F. ) ;
#69265=CARTESIAN_POINT ( 'NONE',  ( -7.347880794884122694E-16, 11.75000000000000000, 4.000000000000001776 ) ) ;
#69268=CARTESIAN_POINT ( 'NONE',  ( -4.541265875000002339, 20.81249999863440436, -5.561446717895856393E-16 ) ) ;
#69287=CARTESIAN_POINT ( 'NONE',  ( -4.000000000000001776, 6.187499997268813168, -1.656854249492381470 ) ) ;
#69360=CARTESIAN_POINT ( 'NONE',  ( -3.211159895383562723, 9.937499998634406140, 3.211159895383561391 ) ) ;
#69404=CARTESIAN_POINT ( 'NONE',  ( -3.211159895383561391, 10.81249999863440792, -3.211159895383561835 ) ) ;
#69409=CARTESIAN_POINT ( 'NONE',  ( 4.000000000000001776, 14.00000000000000000, 0.000000000000000000 ) ) ;
#69411=CARTESIAN_POINT ( 'NONE',  ( 4.541265875000002339, 12.37499999863440969, -1.881053915767121776 ) ) ;
#69419=CARTESIAN_POINT ( 'NONE',  ( 1.881053915767121776, 20.49999999863440436, -4.541265875000002339 ) ) ;
#69485=EDGE_CURVE ( 'NONE', #52055, #29918, #56021, .T. ) ;
#69486=DIRECTION ( 'NONE',  ( 1.000000000000000000, -0.000000000000000000, 0.000000000000000000 ) ) ;
#69492=CARTESIAN_POINT ( 'NONE',  ( 2.780723358947928197E-16, 14.68749999863440792, -4.541265875000002339 ) ) ;
#69501=CARTESIAN_POINT ( 'NONE',  ( -1.656854249492381248, 0.3125000000000001110, -4.000000000000001776 ) ) ;
#69502=CARTESIAN_POINT ( 'NONE',  ( -4.000000000000001776, 9.249999997268814056, -4.898587196589415787E-16 ) ) ;
#69503=CARTESIAN_POINT ( 'NONE',  ( -4.541265875000002339, 1.812499998634406584, -5.561446717895856393E-16 ) ) ;
#69510=CARTESIAN_POINT ( 'NONE',  ( -3.211159895383562723, 8.937499998634407916, 3.211159895383561391 ) ) ;
#69511=CARTESIAN_POINT ( 'NONE',  ( -4.000000000000002665, 18.31249999726881938, 1.656854249492380582 ) ) ;
#69554=CARTESIAN_POINT ( 'NONE',  ( -8.342170076843785083E-16, 13.18749999863440792, 4.541265875000002339 ) ) ;
#69583=CARTESIAN_POINT ( 'NONE',  ( 3.211159895383561835, 1.562499998634406806, -3.211159895383561835 ) ) ;
#69595=CARTESIAN_POINT ( 'NONE',  ( 4.541265875000002339, 20.49999999863440436, -1.881053915767121554 ) ) ;
#69600=EDGE_CURVE ( 'NONE', #28680, #2093, #10187, .T. ) ;
#69607=DIRECTION ( 'NONE',  ( -0.000000000000000000, -1.000000000000000000, -0.000000000000000000 ) ) ;
#69638=CARTESIAN_POINT ( 'NONE',  ( -1.656854249492381248, 11.31249999999999822, -4.000000000000001776 ) ) ;
#69641=CARTESIAN_POINT ( 'NONE',  ( -4.541265875000003227, 21.87499999863441147, 1.881053915767121110 ) ) ;
#69700=CARTESIAN_POINT ( 'NONE',  ( -4.541265875000003227, 21.87499999863441147, 1.881053915767121110 ) ) ;
#69722=CARTESIAN_POINT ( 'NONE',  ( -7.347880794884122694E-16, 18.75000000000000000, 4.000000000000001776 ) ) ;
#69733=CARTESIAN_POINT ( 'NONE',  ( -1.881053915767124440, 9.999999998634407916, 4.541265875000001451 ) ) ;
#69754=DIRECTION ( 'NONE',  ( -1.000000000000000000, 0.000000000000000000, 0.000000000000000000 ) ) ;
#69777=CARTESIAN_POINT ( 'NONE',  ( 2.449293598294707893E-16, 13.25000000000000000, -4.000000000000001776 ) ) ;
#69779=CARTESIAN_POINT ( 'NONE',  ( -4.541265875000003227, 12.87499999863440969, 1.881053915767121110 ) ) ;
#69788=CARTESIAN_POINT ( 'NONE',  ( 4.000000000000001776, 6.812499997268813168, -1.656854249492381248 ) ) ;
#69847=ORIENTED_EDGE ( 'NONE', *, *, #9397, .F. ) ;
#69855=AXIS2_PLACEMENT_3D ( 'NONE', #19528, #36896, #70854 ) ;
#69864=CARTESIAN_POINT ( 'NONE',  ( -4.541265875000002339, 17.93749999863440792, -5.561446717895856393E-16 ) ) ;
#69868=CARTESIAN_POINT ( 'NONE',  ( 4.541265875000002339, 0.4999999986344068614, -1.881053915767121554 ) ) ;
#69874=CARTESIAN_POINT ( 'NONE',  ( -2.828427124746192067, 0.6250000000000002220, 2.828427124746190735 ) ) ;
#69875=CARTESIAN_POINT ( 'NONE',  ( -2.828427124746192067, 14.37499999726881406, 2.828427124746190735 ) ) ;
#69883=CARTESIAN_POINT ( 'NONE',  ( 3.211159895383560947, 16.18749999863440436, 3.211159895383562723 ) ) ;
#69908=DIRECTION ( 'NONE',  ( 0.000000000000000000, -0.000000000000000000, 1.000000000000000000 ) ) ;
#69914=CARTESIAN_POINT ( 'NONE',  ( 1.881053915767122664, 4.124999998634407028, 4.541265875000001451 ) ) ;
#69929=CARTESIAN_POINT ( 'NONE',  ( 3.211159895383561835, 17.56249999863440792, -3.211159895383561835 ) ) ;
#69932=CARTESIAN_POINT ( 'NONE',  ( 4.000000000000000888, 7.687499997268812280, 1.656854249492384135 ) ) ;
#69956=CARTESIAN_POINT ( 'NONE',  ( 3.211159895383560947, 3.312499998634407028, 3.211159895383562723 ) ) ;
#69970=CARTESIAN_POINT ( 'NONE',  ( 1.656854249492381248, 9.187500000000000000, -4.000000000000001776 ) ) ;
#69971=CARTESIAN_POINT ( 'NONE',  ( 4.541265875000001451, 22.37499999863441147, 1.881053915767124440 ) ) ;
#69985=DIRECTION ( 'NONE',  ( -0.000000000000000000, -1.000000000000000000, -0.000000000000000000 ) ) ;
#70016=CARTESIAN_POINT ( 'NONE',  ( -1.656854249492383468, 11.68750000000000000, 4.000000000000000888 ) ) ;
#70018=VECTOR ( 'NONE', #12125, 1000.000000000000000 ) ;
#70020=CARTESIAN_POINT ( 'NONE',  ( -4.541265875000003227, 20.87499999863441147, 1.881053915767121110 ) ) ;
#70045=CARTESIAN_POINT ( 'NONE',  ( 2.828427124746191623, 9.874999997268814056, -2.828427124746191623 ) ) ;
#70064=EDGE_CURVE ( 'NONE', #23983, #29151, #2024, .T. ) ;
#70083=CARTESIAN_POINT ( 'NONE',  ( -4.261174619373528039, 22.00000000000000000, -1.025908319483143094 ) ) ;
#70113=CARTESIAN_POINT ( 'NONE',  ( 3.211159895383560947, 11.18749999863440792, 3.211159895383562723 ) ) ;
#70156=CARTESIAN_POINT ( 'NONE',  ( 4.000000000000001776, 11.06250000000000000, -1.656854249492381248 ) ) ;
#70158=CARTESIAN_POINT ( 'NONE',  ( -3.211159895383562723, 11.93749999863440614, 3.211159895383561391 ) ) ;
#70180=CARTESIAN_POINT ( 'NONE',  ( -2.828427124746192067, 0.6250000000000002220, 2.828427124746190735 ) ) ;
#70207=CARTESIAN_POINT ( 'NONE',  ( 4.898587196589415787E-16, 0.000000000000000000, 4.000000000000001776 ) ) ;
#70232=( BOUNDED_CURVE ( )  B_SPLINE_CURVE ( 2, ( #7038, #48488, #47745, #1754, #42086, #2850, #24735, #42822, #58727 ),
 .UNSPECIFIED., .F., .F. ) 
 B_SPLINE_CURVE_WITH_KNOTS ( ( 3, 2, 2, 2, 3 ),
 ( 0.4204545454545454697, 0.4261363636363636465, 0.4318181818181818232, 0.4375000000000000000, 0.4431818181818181768 ),
 .UNSPECIFIED. ) 
 CURVE ( )  GEOMETRIC_REPRESENTATION_ITEM ( )  RATIONAL_B_SPLINE_CURVE ( ( 1.000000000000000000, 0.9238795325112867385, 1.000000000000000000, 0.9238795325112867385, 1.000000000000000000, 0.9238795325112867385, 1.000000000000000000, 0.9238795325112867385, 1.000000000000000000 ) ) 
 REPRESENTATION_ITEM ( '' )  );
#70238=CARTESIAN_POINT ( 'NONE',  ( 4.541265875000002339, 16.43749999863440436, 0.000000000000000000 ) ) ;
#70242=CARTESIAN_POINT ( 'NONE',  ( 3.211159895383561835, 1.562499998634406806, -3.211159895383561835 ) ) ;
#70248=CARTESIAN_POINT ( 'NONE',  ( 2.828427124746191623, 15.87499999726881406, -2.828427124746191623 ) ) ;
#70251=AXIS2_PLACEMENT_3D ( 'NONE', #67992, #69486, #63818 ) ;
#70254=CARTESIAN_POINT ( 'NONE',  ( 2.780723358947928197E-16, 14.56249999863440792, -4.541265875000002339 ) ) ;
#70255=CARTESIAN_POINT ( 'NONE',  ( 4.000000000000001776, 12.00000000000000000, 0.000000000000000000 ) ) ;
#70274=CARTESIAN_POINT ( 'NONE',  ( 4.000000000000000888, 7.937500000000000000, 1.656854249492384135 ) ) ;
#70276=DIRECTION ( 'NONE',  ( 0.000000000000000000, 1.000000000000000000, 0.000000000000000000 ) ) ;
#70281=CARTESIAN_POINT ( 'NONE',  ( -3.211159895383562723, 2.937499998634407028, 3.211159895383561391 ) ) ;
#70284=CARTESIAN_POINT ( 'NONE',  ( 2.449293598294707893E-16, 5.250000000000000000, -4.000000000000001776 ) ) ;
#70297=CARTESIAN_POINT ( 'NONE',  ( 1.881053915767121776, 15.62499999863440614, -4.541265875000002339 ) ) ;
#70324=CARTESIAN_POINT ( 'NONE',  ( 4.541265875000002339, 4.437499998634407028, 0.000000000000000000 ) ) ;
#70333=ADVANCED_FACE ( 'NONE', ( #55256 ), #50320, .T. ) ;
#70339=CARTESIAN_POINT ( 'NONE',  ( 4.000000000000001776, 2.812499997268813612, -1.656854249492381248 ) ) ;
#70344=CARTESIAN_POINT ( 'NONE',  ( 4.541265875000002339, 2.374999998634407028, -1.881053915767121554 ) ) ;
#70378=EDGE_CURVE ( 'NONE', #25107, #30314, #9745, .T. ) ;
#70385=CARTESIAN_POINT ( 'NONE',  ( 4.541265875000002339, 2.499999998634407028, -1.881053915767121554 ) ) ;
#70388=CARTESIAN_POINT ( 'NONE',  ( -4.000000000000002665, 1.562500000000000666, 1.656854249492380582 ) ) ;
#70395=ORIENTED_EDGE ( 'NONE', *, *, #45966, .T. ) ;
#70443=CARTESIAN_POINT ( 'NONE',  ( -1.721590048263790695, 22.00000000000001776, -3.746118333428731351 ) ) ;
#70473=CARTESIAN_POINT ( 'NONE',  ( -4.541265875000003227, 15.87499999863440436, 1.881053915767121110 ) ) ;
#70477=ADVANCED_FACE ( 'NONE', ( #6904 ), #16714, .T. ) ;
#70486=CARTESIAN_POINT ( 'NONE',  ( -2.828427124746190735, 13.12499999726881406, -2.828427124746191623 ) ) ;
#70512=CARTESIAN_POINT ( 'NONE',  ( -7.347880794884122694E-16, 12.75000000000000178, 4.000000000000001776 ) ) ;
#70515=CARTESIAN_POINT ( 'NONE',  ( 3.211159895383561835, 16.43749999863440436, -3.211159895383561835 ) ) ;
#70533=ORIENTED_EDGE ( 'NONE', *, *, #17046, .F. ) ;
#70583=CARTESIAN_POINT ( 'NONE',  ( 2.449293598294707893E-16, 15.99999999726881406, -4.000000000000001776 ) ) ;
#70591=CARTESIAN_POINT ( 'NONE',  ( 0.000000000000000000, 1.806524977843537691E-16, -4.000000000000000000 ) ) ;
#70594=CARTESIAN_POINT ( 'NONE',  ( 4.541265875000002339, 18.43749999863440792, 0.000000000000000000 ) ) ;
#70604=CARTESIAN_POINT ( 'NONE',  ( 2.828427124746190291, 12.62499999726881406, 2.828427124746192067 ) ) ;
#70607=DIRECTION ( 'NONE',  ( 0.000000000000000000, 0.000000000000000000, -1.000000000000000000 ) ) ;
#70611=CARTESIAN_POINT ( 'NONE',  ( 1.881053915767121776, 12.49999999863440969, -4.541265875000002339 ) ) ;
#70639=CARTESIAN_POINT ( 'NONE',  ( 3.211159895383560947, 1.187499998634406806, 3.211159895383562723 ) ) ;
#70642=CARTESIAN_POINT ( 'NONE',  ( 4.000000000000001776, 5.000000000000000000, 0.000000000000000000 ) ) ;
#70643=ORIENTED_EDGE ( 'NONE', *, *, #72082, .T. ) ;
#70658=CARTESIAN_POINT ( 'NONE',  ( 4.541265875000002339, 15.49999999863440792, -1.881053915767121554 ) ) ;
#70682=CARTESIAN_POINT ( 'NONE',  ( -1.881053915767121776, 5.749999998634407028, -4.541265875000002339 ) ) ;
#70691=CARTESIAN_POINT ( 'NONE',  ( 4.000000000000001776, 1.812499997268813390, -1.656854249492381248 ) ) ;
#70698=CARTESIAN_POINT ( 'NONE',  ( -1.881053915767121554, 0.6249999986344065839, -4.541265875000002339 ) ) ;
#70727=DIRECTION ( 'NONE',  ( -0.000000000000000000, -1.000000000000000000, -0.000000000000000000 ) ) ;
#70743=CARTESIAN_POINT ( 'NONE',  ( -4.541265875000003227, 3.999999998634406140, 1.881053915767121110 ) ) ;
#70755=CARTESIAN_POINT ( 'NONE',  ( -8.000000000000003553, 22.99999999999999645, -1.000000000000000000 ) ) ;
#70781=CARTESIAN_POINT ( 'NONE',  ( 2.808409778661586920, 22.00000000000003553, 3.186686813332832990 ) ) ;
#70788=CARTESIAN_POINT ( 'NONE',  ( 3.211159895383561835, 11.56249999863440614, -3.211159895383561835 ) ) ;
#70796=CARTESIAN_POINT ( 'NONE',  ( 2.449293598294707893E-16, 12.99999999726881406, -4.000000000000001776 ) ) ;
#70815=ORIENTED_EDGE ( 'NONE', *, *, #37547, .T. ) ;
#70816=DIRECTION ( 'NONE',  ( -0.000000000000000000, -1.000000000000000000, -0.000000000000000000 ) ) ;
#70824=CARTESIAN_POINT ( 'NONE',  ( 2.449293598294707893E-16, 19.25000000000000000, -4.000000000000001776 ) ) ;
#70830=DIRECTION ( 'NONE',  ( -0.000000000000000000, -1.000000000000000000, -0.000000000000000000 ) ) ;
#70835=CARTESIAN_POINT ( 'NONE',  ( -4.541265875000002339, 12.81249999863440792, -5.561446717895856393E-16 ) ) ;
#70854=DIRECTION ( 'NONE',  ( 0.000000000000000000, 0.000000000000000000, -1.000000000000000000 ) ) ;
#70880=CARTESIAN_POINT ( 'NONE',  ( -4.000000000000002665, 10.56250000000000000, 1.656854249492380804 ) ) ;
#70882=CARTESIAN_POINT ( 'NONE',  ( 2.780723358947928197E-16, 17.56249999863440792, -4.541265875000002339 ) ) ;
#70907=DIRECTION ( 'NONE',  ( -0.000000000000000000, -1.000000000000000000, -0.000000000000000000 ) ) ;
#70917=CARTESIAN_POINT ( 'NONE',  ( -2.828427124746192067, 12.62500000000000000, 2.828427124746190735 ) ) ;
#70955=CARTESIAN_POINT ( 'NONE',  ( -3.211159895383561391, 16.81249999863440436, -3.211159895383561835 ) ) ;
#70959=CARTESIAN_POINT ( 'NONE',  ( -4.541265875000003227, 1.999999998634407250, 1.881053915767121110 ) ) ;
#70968=CARTESIAN_POINT ( 'NONE',  ( 1.656854249492381248, 13.93749999726881228, -4.000000000000001776 ) ) ;
#70969=CARTESIAN_POINT ( 'NONE',  ( -3.211159895383562723, 2.937499998634407028, 3.211159895383561391 ) ) ;
#70976=CARTESIAN_POINT ( 'NONE',  ( 4.541265875000002339, 14.31249999863440792, 0.000000000000000000 ) ) ;
#71002=CARTESIAN_POINT ( 'NONE',  ( -4.541265875000003227, 3.874999998634407028, 1.881053915767121110 ) ) ;
#71004=CARTESIAN_POINT ( 'NONE',  ( -4.000000000000001776, 14.24999999726881406, -4.898587196589415787E-16 ) ) ;
#71020=CARTESIAN_POINT ( 'NONE',  ( -8.342170076843785083E-16, 17.18749999863440792, 4.541265875000002339 ) ) ;
#71040=CARTESIAN_POINT ( 'NONE',  ( -1.881053915767124440, 4.124999998634407028, 4.541265875000001451 ) ) ;
#71051=CARTESIAN_POINT ( 'NONE',  ( 2.828427124746190291, 1.624999997268813390, 2.828427124746192067 ) ) ;
#71058=CARTESIAN_POINT ( 'NONE',  ( 3.211159895383561835, 1.437499998634406806, -3.211159895383561835 ) ) ;
#71079=CARTESIAN_POINT ( 'NONE',  ( -4.000000000000002665, 17.31249999726881938, 1.656854249492380582 ) ) ;
#71081=DIRECTION ( 'NONE',  ( 1.000000000000000000, 0.000000000000000000, 0.000000000000000000 ) ) ;
#71101=CARTESIAN_POINT ( 'NONE',  ( 3.211159895383560947, 3.312499998634407028, 3.211159895383562723 ) ) ;
#71111=ORIENTED_EDGE ( 'NONE', *, *, #25130, .F. ) ;
#71131=CARTESIAN_POINT ( 'NONE',  ( 2.828427124746191623, 20.87499999726881583, -2.828427124746191623 ) ) ;
#71146=CARTESIAN_POINT ( 'NONE',  ( -4.541265875000003227, 12.99999999863440969, 1.881053915767121110 ) ) ;
#71161=CARTESIAN_POINT ( 'NONE',  ( -4.423890159799090505, 21.99999999999997868, -0.1625330420329095804 ) ) ;
#71176=CYLINDRICAL_SURFACE ( 'NONE', #13101, 4.000000000000001776 ) ;
#71191=CARTESIAN_POINT ( 'NONE',  ( -3.211159895383561391, 13.68749999863440614, -3.211159895383561835 ) ) ;
#71239=CARTESIAN_POINT ( 'NONE',  ( -4.000000000000001776, 17.43750000000000000, -1.656854249492381470 ) ) ;
#71240=CARTESIAN_POINT ( 'NONE',  ( -4.541265875000003227, 14.87499999863440969, 1.881053915767121110 ) ) ;
#71247=CARTESIAN_POINT ( 'NONE',  ( 0.000000000000000000, 0.000000000000000000, 0.000000000000000000 ) ) ;
#71249=EDGE_LOOP ( 'NONE', ( #57497, #39800, #73295, #56728 ) ) ;
#71320=CARTESIAN_POINT ( 'NONE',  ( 4.541265875000001451, 15.37499999863440969, 1.881053915767124440 ) ) ;
#71324=CARTESIAN_POINT ( 'NONE',  ( 4.541265875000002339, 2.499999998634407028, -1.881053915767121554 ) ) ;
#71330=CARTESIAN_POINT ( 'NONE',  ( 4.000000000000001776, 4.062500000000000000, -1.656854249492381248 ) ) ;
#71331=CARTESIAN_POINT ( 'NONE',  ( 4.000000000000001776, 13.74999999726881583, 0.000000000000000000 ) ) ;
#71332=CARTESIAN_POINT ( 'NONE',  ( -4.541265875000002339, 5.749999998634407028, -1.881053915767121998 ) ) ;
#71337=CARTESIAN_POINT ( 'NONE',  ( -3.211159895383561391, 13.68749999863440614, -3.211159895383561835 ) ) ;
#71364=CARTESIAN_POINT ( 'NONE',  ( 2.780723358947928197E-16, 1.562499998634406584, -4.541265875000002339 ) ) ;
#71366=CARTESIAN_POINT ( 'NONE',  ( 4.000000000000000888, 4.937500000000000888, 1.656854249492384135 ) ) ;
#71378=EDGE_CURVE ( 'NONE', #11773, #9987, #35543, .T. ) ;
#71382=CARTESIAN_POINT ( 'NONE',  ( 4.541265875000001451, 17.37499999863440436, 1.881053915767124440 ) ) ;
#71408=CARTESIAN_POINT ( 'NONE',  ( -1.881053915767121776, 6.749999998634407916, -4.541265875000002339 ) ) ;
#71418=CARTESIAN_POINT ( 'NONE',  ( 4.000000000000001776, 9.062500000000000000, -1.656854249492381248 ) ) ;
#71419=CARTESIAN_POINT ( 'NONE',  ( -7.347880794884122694E-16, 3.499999997268812724, 4.000000000000001776 ) ) ;
#71423=CARTESIAN_POINT ( 'NONE',  ( 4.541265875000002339, 3.312499998634407028, 0.000000000000000000 ) ) ;
#71443=DIRECTION ( 'NONE',  ( 0.000000000000000000, 0.000000000000000000, -1.000000000000000000 ) ) ;
#71446=LINE ( 'NONE', #13725, #10204 ) ;
#71468=CARTESIAN_POINT ( 'NONE',  ( -4.541265875000002339, 4.937499998634407916, -5.561446717895856393E-16 ) ) ;
#71490=DIRECTION ( 'NONE',  ( -0.000000000000000000, -1.000000000000000000, -0.000000000000000000 ) ) ;
#71504=CARTESIAN_POINT ( 'NONE',  ( 2.549518376916382945, 21.99999999999999645, 3.425189025651766972 ) ) ;
#71514=CARTESIAN_POINT ( 'NONE',  ( -1.881053915767124440, 13.12499999863440969, 4.541265875000001451 ) ) ;
#71527=CARTESIAN_POINT ( 'NONE',  ( -3.185990892481874948, 21.99999999999999289, -2.809123505085484584 ) ) ;
#71543=CARTESIAN_POINT ( 'NONE',  ( -7.347880794884122694E-16, 15.49999999726881406, 4.000000000000001776 ) ) ;
#71560=CARTESIAN_POINT ( 'NONE',  ( 2.780723358947928197E-16, 13.56249999863440614, -4.541265875000002339 ) ) ;
#71568=VECTOR ( 'NONE', #47266, 1000.000000000000000 ) ;
#71580=CYLINDRICAL_SURFACE ( 'NONE', #69855, 4.000000000000001776 ) ;
#71606=CARTESIAN_POINT ( 'NONE',  ( -4.000000000000002665, 16.56250000000000000, 1.656854249492380804 ) ) ;
#71607=CARTESIAN_POINT ( 'NONE',  ( -3.211159895383562723, 15.93749999863440436, 3.211159895383561391 ) ) ;
#71632=CARTESIAN_POINT ( 'NONE',  ( 2.828427124746191623, 14.12500000000000000, -2.828427124746191623 ) ) ;
#71645=CARTESIAN_POINT ( 'NONE',  ( 2.449293598294707893E-16, 16.25000000000000000, -4.000000000000001776 ) ) ;
#71689=CARTESIAN_POINT ( 'NONE',  ( -3.211159895383561391, 19.81249999863440436, -3.211159895383561835 ) ) ;
#71692=CARTESIAN_POINT ( 'NONE',  ( -3.211159895383561391, 2.812499998634407028, -3.211159895383561835 ) ) ;
#71700=CARTESIAN_POINT ( 'NONE',  ( -1.656854249492383691, 5.687500000000000000, 4.000000000000000888 ) ) ;
#71701=CARTESIAN_POINT ( 'NONE',  ( 2.449293598294707893E-16, 17.99999999726881583, -4.000000000000001776 ) ) ;
#71702=CARTESIAN_POINT ( 'NONE',  ( 1.881053915767121998, 3.499999998634407028, -4.541265875000002339 ) ) ;
#71709=CARTESIAN_POINT ( 'NONE',  ( -1.881053915767121554, 17.62499999863440436, -4.541265875000002339 ) ) ;
#71714=ORIENTED_EDGE ( 'NONE', *, *, #24789, .F. ) ;
#71724=( BOUNDED_CURVE ( )  B_SPLINE_CURVE ( 2, ( #63836, #121, #23100, #47582, #46483, #12153, #52157, #58935, #24205, #53266, #69131, #64583, #12879, #1592, #58201, #35915, #24577, #11786, #17438, #6135, #63458, #34823, #492, #23472, #69503, #31351, #8339, #42666, #43793, #30979, #30614, #19653, #60393, #66809, #13976, #9096, #37018, #72078, #43409, #25676, #7977, #15111, #70969, #54381, #32110, #49066, #54753, #26046, #2690, #48696, #65311, #71702, #20020, #47953, #53637, #13612, #43030, #37774, #60770, #49448, #66052, #20395, #20774, #36651, #14360, #60020, #8719, #54000, #72466, #1947, #37392, #19283, #24936, #31731, #59661, #3063, #66423, #14735, #55128, #3431, #65677, #26422, #59298, #42294, #2311, #7607, #25308, #71332, #48325, #22254, #61521, #10958, #21523, #45282, #56987, #33993, #16217, #73580, #5300, #21149, #28302, #9473, #50940, #50196, #44171, #56242, #21888, #26811, #32490, #67185, #33242, #16589, #39628, #51311, #27552, #72842, #74322, #62255, #49825, #55501, #10582, #9843, #22628, #3813, #4557, #15482, #38518, #44917, #32869, #50564, #67924, #4935, #45648, #62627, #44545, #38143, #55874, #4190, #33613, #68663, #27179, #73215, #39257, #68292, #67555, #61143, #15851, #38886, #61890, #10213, #56620, #27932, #73951, #27, #58838, #34730, #29789, #53171, #41110, #46021, #11327, #57735, #24111, #40000, #69042, #17345, #40367, #18096, #52431, #46756, #46393, #18465, #35095, #17717, #47491, #63742, #58105, #7149, #58471, #29422, #57360, #34359, #30154, #6040, #52064, #63366, #70158, #6416, #41475, #63003, #768, #12424, #64491, #69411, #40732, #12060, #23014, #1509, #11691, #47125, #23754, #69779, #6781, #29045, #64117, #35458, #401, #24489, #23380, #5671, #52799, #1133, #16974, #12791, #35823, #28668, #51682, #54659, #36925, #19196, #30889, #7518, #65587, #43316, #60296, #65959, #37300, #13886, #59933, #20298, #8245, #31258, #13154, #71240, #14637, #19560, #48232, #71985, #54287, #36192, #25216, #42574, #66333, #2598, #8626, #2967, #25588, #42198, #53907, #48604, #71607, #65213, #2220, #19928, #25952, #31638, #42938, #48971, #70515, #14263, #37680, #41841, #1857, #60679, #8999, #32014, #55033, #3340, #30524, #26330, #18834, #53541, #59208, #64850, #24843, #47861, #70882, #13518, #36556, #59569, #7884, #4843, #44822, #61802, #56900, #33901, #72752, #67464, #22168, #33158, #66713, #15015, #56152, #5212, #61428, #4468, #33526, #21056, #45194, #32774, #56526, #32393, #27457, #21429, #15760, #68204, #50472, #15388, #20679, #62167, #9755, #38424, #55782, #16501, #4098, #27840, #72368, #3717, #26716, #49736, #73486, #55408, #50847, #21792, #38051, #43698, #27091, #49351, #10120, #73861, #73121, #50107, #44452, #61051, #9373, #39541, #38799, #67834, #44079, #62537, #16126, #39164, #10491, #67091, #10864, #69700, #12711, #51595, #318 ),
 .UNSPECIFIED., .F., .F. ) 
 B_SPLINE_CURVE_WITH_KNOTS ( ( 3, 2, 2, 2, 2, 2, 2, 2, 2, 2, 2, 2, 2, 2, 2, 2, 2, 2, 2, 2, 2, 2, 2, 2, 2, 2, 2, 2, 2, 2, 2, 2, 2, 2, 2, 2, 2, 2, 2, 2, 2, 2, 2, 2, 2, 2, 2, 2, 2, 2, 2, 2, 2, 2, 2, 2, 2, 2, 2, 2, 2, 2, 2, 2, 2, 2, 2, 2, 2, 2, 2, 2, 2, 2, 2, 2, 2, 2, 2, 2, 2, 2, 2, 2, 2, 2, 2, 2, 2, 2, 2, 2, 2, 2, 2, 2, 2, 2, 2, 2, 2, 2, 2, 2, 2, 2, 2, 2, 2, 2, 2, 2, 2, 2, 2, 2, 2, 2, 2, 2, 2, 2, 2, 2, 2, 2, 2, 2, 2, 2, 2, 2, 2, 2, 2, 2, 2, 2, 2, 2, 2, 2, 2, 2, 2, 2, 2, 2, 2, 2, 2, 2, 2, 2, 2, 2, 2, 2, 2, 2, 2, 2, 2, 2, 2, 2, 2, 2, 2, 2, 2, 2, 2, 2, 3 ),
 ( 0.000000000000000000, 0.005681818181818181976, 0.01136363636363636395, 0.01704545454545454419, 0.02272727272727272790, 0.02840909090909090814, 0.03409090909090908839, 0.03977272727272727210, 0.04545454545454545581, 0.05113636363636363952, 0.05681818181818181629, 0.06250000000000000000, 0.06818181818181817677, 0.07386363636363636742, 0.07954545454545454419, 0.08522727272727272096, 0.09090909090909091161, 0.09659090909090908839, 0.1022727272727272790, 0.1079545454545454558, 0.1136363636363636326, 0.1193181818181818232, 0.1250000000000000000, 0.1306818181818181768, 0.1363636363636363535, 0.1420454545454545581, 0.1477272727272727348, 0.1534090909090909116, 0.1590909090909090884, 0.1647727272727272652, 0.1704545454545454419, 0.1761363636363636465, 0.1818181818181818232, 0.1875000000000000000, 0.1931818181818181768, 0.1988636363636363535, 0.2045454545454545581, 0.2102272727272727348, 0.2159090909090909116, 0.2215909090909090884, 0.2272727272727272652, 0.2329545454545454419, 0.2386363636363636465, 0.2443181818181818232, 0.2500000000000000000, 0.2556818181818181768, 0.2613636363636363535, 0.2670454545454545303, 0.2727272727272727071, 0.2784090909090908839, 0.2840909090909091161, 0.2897727272727272929, 0.2954545454545454697, 0.3011363636363636465, 0.3068181818181818232, 0.3125000000000000000, 0.3181818181818181768, 0.3238636363636363535, 0.3295454545454545303, 0.3352272727272727071, 0.3409090909090908839, 0.3465909090909091161, 0.3522727272727272929, 0.3579545454545454697, 0.3636363636363636465, 0.3693181818181818232, 0.3750000000000000000, 0.3806818181818181768, 0.3863636363636363535, 0.3920454545454545303, 0.3977272727272727071, 0.4034090909090908839, 0.4090909090909091161, 0.4147727272727272929, 0.4204545454545454697, 0.4261363636363636465, 0.4318181818181818232, 0.4375000000000000000, 0.4431818181818181768, 0.4488636363636363535, 0.4545454545454545303, 0.4602272727272727071, 0.4659090909090908839, 0.4715909090909091161, 0.4772727272727272929, 0.4829545454545454697, 0.4886363636363636465, 0.4943181818181818232, 0.5000000000000000000, 0.5056818181818182323, 0.5113636363636363535, 0.5170454545454545858, 0.5227272727272727071, 0.5284090909090909394, 0.5340909090909090606, 0.5397727272727272929, 0.5454545454545454142, 0.5511363636363636465, 0.5568181818181817677, 0.5625000000000000000, 0.5681818181818182323, 0.5738636363636363535, 0.5795454545454545858, 0.5852272727272727071, 0.5909090909090909394, 0.5965909090909090606, 0.6022727272727272929, 0.6079545454545454142, 0.6136363636363636465, 0.6193181818181817677, 0.6250000000000000000, 0.6306818181818182323, 0.6363636363636363535, 0.6420454545454545858, 0.6477272727272727071, 0.6534090909090909394, 0.6590909090909090606, 0.6647727272727272929, 0.6704545454545454142, 0.6761363636363636465, 0.6818181818181817677, 0.6875000000000000000, 0.6931818181818182323, 0.6988636363636363535, 0.7045454545454545858, 0.7102272727272727071, 0.7159090909090909394, 0.7215909090909090606, 0.7272727272727272929, 0.7329545454545454142, 0.7386363636363636465, 0.7443181818181817677, 0.7500000000000000000, 0.7556818181818182323, 0.7613636363636363535, 0.7670454545454545858, 0.7727272727272727071, 0.7784090909090909394, 0.7840909090909090606, 0.7897727272727272929, 0.7954545454545454142, 0.8011363636363636465, 0.8068181818181817677, 0.8125000000000000000, 0.8181818181818182323, 0.8238636363636363535, 0.8295454545454545858, 0.8352272727272727071, 0.8409090909090909394, 0.8465909090909090606, 0.8522727272727272929, 0.8579545454545454142, 0.8636363636363636465, 0.8693181818181817677, 0.8750000000000000000, 0.8806818181818182323, 0.8863636363636363535, 0.8920454545454545858, 0.8977272727272727071, 0.9034090909090910504, 0.9090909090909090606, 0.9147727272727272929, 0.9204545454545454142, 0.9261363636363636465, 0.9318181818181817677, 0.9375000000000000000, 0.9431818181818182323, 0.9488636363636363535, 0.9545454545454545858, 0.9602272727272727071, 0.9659090909090909394, 0.9715909090909090606, 0.9772727272727272929, 0.9829545454545454142, 0.9857954546051644895 ),
 .UNSPECIFIED. ) 
 CURVE ( )  GEOMETRIC_REPRESENTATION_ITEM ( )  RATIONAL_B_SPLINE_CURVE ( ( 1.000000000000000000, 0.9238795325112867385, 1.000000000000000000, 0.9238795325112867385, 1.000000000000000000, 0.9238795325112867385, 1.000000000000000000, 0.9238795325112867385, 1.000000000000000000, 0.9238795325112867385, 1.000000000000000000, 0.9238795325112867385, 1.000000000000000000, 0.9238795325112867385, 1.000000000000000000, 0.9238795325112867385, 1.000000000000000000, 0.9238795325112867385, 1.000000000000000000, 0.9238795325112867385, 1.000000000000000000, 0.9238795325112867385, 1.000000000000000000, 0.9238795325112867385, 1.000000000000000000, 0.9238795325112867385, 1.000000000000000000, 0.9238795325112867385, 1.000000000000000000, 0.9238795325112867385, 1.000000000000000000, 0.9238795325112867385, 1.000000000000000000, 0.9238795325112867385, 1.000000000000000000, 0.9238795325112867385, 1.000000000000000000, 0.9238795325112867385, 1.000000000000000000, 0.9238795325112867385, 1.000000000000000000, 0.9238795325112867385, 1.000000000000000000, 0.9238795325112867385, 1.000000000000000000, 0.9238795325112867385, 1.000000000000000000, 0.9238795325112867385, 1.000000000000000000, 0.9238795325112867385, 1.000000000000000000, 0.9238795325112867385, 1.000000000000000000, 0.9238795325112867385, 1.000000000000000000, 0.9238795325112867385, 1.000000000000000000, 0.9238795325112867385, 1.000000000000000000, 0.9238795325112867385, 1.000000000000000000, 0.9238795325112867385, 1.000000000000000000, 0.9238795325112867385, 1.000000000000000000, 0.9238795325112867385, 1.000000000000000000, 0.9238795325112867385, 1.000000000000000000, 0.9238795325112867385, 1.000000000000000000, 0.9238795325112867385, 1.000000000000000000, 0.9238795325112867385, 1.000000000000000000, 0.9238795325112867385, 1.000000000000000000, 0.9238795325112867385, 1.000000000000000000, 0.9238795325112867385, 1.000000000000000000, 0.9238795325112867385, 1.000000000000000000, 0.9238795325112867385, 1.000000000000000000, 0.9238795325112867385, 1.000000000000000000, 0.9238795325112867385, 1.000000000000000000, 0.9238795325112867385, 1.000000000000000000, 0.9238795325112867385, 1.000000000000000000, 0.9238795325112867385, 1.000000000000000000, 0.9238795325112867385, 1.000000000000000000, 0.9238795325112867385, 1.000000000000000000, 0.9238795325112867385, 1.000000000000000000, 0.9238795325112867385, 1.000000000000000000, 0.9238795325112867385, 1.000000000000000000, 0.9238795325112867385, 1.000000000000000000, 0.9238795325112867385, 1.000000000000000000, 0.9238795325112867385, 1.000000000000000000, 0.9238795325112867385, 1.000000000000000000, 0.9238795325112867385, 1.000000000000000000, 0.9238795325112867385, 1.000000000000000000, 0.9238795325112867385, 1.000000000000000000, 0.9238795325112867385, 1.000000000000000000, 0.9238795325112867385, 1.000000000000000000, 0.9238795325112867385, 1.000000000000000000, 0.9238795325112867385, 1.000000000000000000, 0.9238795325112867385, 1.000000000000000000, 0.9238795325112867385, 1.000000000000000000, 0.9238795325112867385, 1.000000000000000000, 0.9238795325112867385, 1.000000000000000000, 0.9238795325112867385, 1.000000000000000000, 0.9238795325112867385, 1.000000000000000000, 0.9238795325112867385, 1.000000000000000000, 0.9238795325112867385, 1.000000000000000000, 0.9238795325112867385, 1.000000000000000000, 0.9238795325112867385, 1.000000000000000000, 0.9238795325112867385, 1.000000000000000000, 0.9238795325112867385, 1.000000000000000000, 0.9238795325112867385, 1.000000000000000000, 0.9238795325112867385, 1.000000000000000000, 0.9238795325112867385, 1.000000000000000000, 0.9238795325112867385, 1.000000000000000000, 0.9238795325112867385, 1.000000000000000000, 0.9238795325112867385, 1.000000000000000000, 0.9238795325112867385, 1.000000000000000000, 0.9238795325112867385, 1.000000000000000000, 0.9238795325112867385, 1.000000000000000000, 0.9238795325112867385, 1.000000000000000000, 0.9238795325112867385, 1.000000000000000000, 0.9238795325112867385, 1.000000000000000000, 0.9238795325112867385, 1.000000000000000000, 0.9238795325112867385, 1.000000000000000000, 0.9238795325112867385, 1.000000000000000000, 0.9238795325112867385, 1.000000000000000000, 0.9238795325112867385, 1.000000000000000000, 0.9238795325112867385, 1.000000000000000000, 0.9238795325112867385, 1.000000000000000000, 0.9238795325112867385, 1.000000000000000000, 0.9238795325112867385, 1.000000000000000000, 0.9238795325112867385, 1.000000000000000000, 0.9238795325112867385, 1.000000000000000000, 0.9238795325112867385, 1.000000000000000000, 0.9238795325112867385, 1.000000000000000000, 0.9238795325112867385, 1.000000000000000000, 0.9238795325112867385, 1.000000000000000000, 0.9238795325112867385, 1.000000000000000000, 0.9238795325112867385, 1.000000000000000000, 0.9238795325112867385, 1.000000000000000000, 0.9238795325112867385, 1.000000000000000000, 0.9238795325112867385, 1.000000000000000000, 0.9238795325112867385, 1.000000000000000000, 0.9238795325112867385, 1.000000000000000000, 0.9238795325112867385, 1.000000000000000000, 0.9238795325112867385, 1.000000000000000000, 0.9238795325112867385, 1.000000000000000000, 0.9238795325112867385, 1.000000000000000000, 0.9238795325112867385, 1.000000000000000000, 0.9238795325112867385, 1.000000000000000000, 0.9238795325112867385, 1.000000000000000000, 0.9238795325112867385, 1.000000000000000000, 0.9238795325112867385, 1.000000000000000000, 0.9238795325112867385, 1.000000000000000000, 0.9238795325112867385, 1.000000000000000000, 0.9238795325112867385, 1.000000000000000000, 0.9238795325112867385, 1.000000000000000000, 0.9238795325112867385, 1.000000000000000000, 0.9238795325112867385, 1.000000000000000000, 0.9238795325112867385, 1.000000000000000000, 0.9238795325112867385, 1.000000000000000000, 0.9238795325112867385, 1.000000000000000000, 0.9238795325112867385, 1.000000000000000000, 0.9238795325112867385, 1.000000000000000000, 0.9238795325112867385, 1.000000000000000000, 0.9238795325112867385, 1.000000000000000000, 0.9238795325112867385, 1.000000000000000000, 0.9238795325112867385, 1.000000000000000000, 0.9238795325112867385, 1.000000000000000000, 0.9238795325112867385, 1.000000000000000000, 0.9238795325112867385, 1.000000000000000000, 0.9238795325112867385, 1.000000000000000000, 0.9238795325112867385, 1.000000000000000000, 0.9238795325112867385, 1.000000000000000000, 0.9238795325112867385, 1.000000000000000000, 0.9238795325112867385, 1.000000000000000000, 0.9238795325112867385, 1.000000000000000000, 0.9238795325112867385, 1.000000000000000000, 0.9238795325112867385, 1.000000000000000000, 0.9238795325112867385, 1.000000000000000000, 0.9238795325112867385, 1.000000000000000000, 0.9238795325112867385, 1.000000000000000000, 0.9238795325112867385, 1.000000000000000000, 0.9238795325112867385, 1.000000000000000000, 0.9238795325112867385, 1.000000000000000000, 0.9238795325112867385, 1.000000000000000000, 0.9238795325112867385, 1.000000000000000000, 0.9238795325112867385, 1.000000000000000000, 0.9238795325112867385, 1.000000000000000000, 0.9238795325112867385, 1.000000000000000000, 0.9238795325112867385, 1.000000000000000000, 0.9238795325112867385, 1.000000000000000000, 0.9238795325112867385, 1.000000000000000000, 0.9238795325112867385, 1.000000000000000000, 0.9238795325112867385, 1.000000000000000000, 0.9238795325112867385, 1.000000000000000000, 0.9238795325112867385, 1.000000000000000000, 0.9238795325112867385, 1.000000000000000000, 0.9238795325112867385, 1.000000000000000000, 0.9238795325112867385, 1.000000000000000000, 0.9238795325112867385, 1.000000000000000000, 0.9238795325112867385, 1.000000000000000000, 0.9238795325112867385, 1.000000000000000000, 0.9238795325112867385, 1.000000000000000000, 0.9238795325112867385, 1.000000000000000000, 0.9238795325112867385, 1.000000000000000000, 0.9238795325112867385, 1.000000000000000000, 0.9238795325112867385, 1.000000000000000000, 0.9619397654556969268, 0.9619397662556434803 ) ) 
 REPRESENTATION_ITEM ( '' )  );
#71738=CARTESIAN_POINT ( 'NONE',  ( 4.541265875000001451, 8.249999998634406140, 1.881053915767124440 ) ) ;
#71758=CARTESIAN_POINT ( 'NONE',  ( 3.211159895383560947, 21.31249999863440792, 3.211159895383562723 ) ) ;
#71782=CARTESIAN_POINT ( 'NONE',  ( 4.541265875000002339, 10.49999999863440969, -1.881053915767121776 ) ) ;
#71792=CARTESIAN_POINT ( 'NONE',  ( 4.000000000000001776, 5.812499997268812280, -1.656854249492381248 ) ) ;
#71798=CARTESIAN_POINT ( 'NONE',  ( 4.541265875000001451, 7.249999998634408804, 1.881053915767124440 ) ) ;
#71805=CARTESIAN_POINT ( 'NONE',  ( -4.000000000000002665, 21.56250000000000355, 1.656854249492380582 ) ) ;
#71823=FACE_OUTER_BOUND ( 'NONE', #6043, .T. ) ;
#71842=CARTESIAN_POINT ( 'NONE',  ( -3.211159895383561391, 5.812499998634407028, -3.211159895383561835 ) ) ;
#71890=CARTESIAN_POINT ( 'NONE',  ( -1.881053915767121554, 11.74999999863440792, -4.541265875000002339 ) ) ;
#71891=EDGE_LOOP ( 'NONE', ( #16402, #44350, #41279, #18254 ) ) ;
#71908=CARTESIAN_POINT ( 'NONE',  ( -7.347880794884122694E-16, 15.49999999726881406, 4.000000000000001776 ) ) ;
#71920=DIRECTION ( 'NONE',  ( 0.000000000000000000, 0.000000000000000000, -1.000000000000000000 ) ) ;
#71935=CARTESIAN_POINT ( 'NONE',  ( 2.780723358947928197E-16, 15.56249999863440614, -4.541265875000002339 ) ) ;
#71940=ORIENTED_EDGE ( 'NONE', *, *, #69028, .F. ) ;
#71953=( BOUNDED_CURVE ( )  B_SPLINE_CURVE ( 2, ( #74134, #34165, #17530, #51492, #63932, #33798, #22435, #45831, #579 ),
 .UNSPECIFIED., .F., .F. ) 
 B_SPLINE_CURVE_WITH_KNOTS ( ( 3, 2, 2, 2, 3 ),
 ( 0.6931818181818182323, 0.6988636363636363535, 0.7045454545454545858, 0.7102272727272727071, 0.7159090909090909394 ),
 .UNSPECIFIED. ) 
 CURVE ( )  GEOMETRIC_REPRESENTATION_ITEM ( )  RATIONAL_B_SPLINE_CURVE ( ( 1.000000000000000000, 0.9238795325112867385, 1.000000000000000000, 0.9238795325112867385, 1.000000000000000000, 0.9238795325112867385, 1.000000000000000000, 0.9238795325112867385, 1.000000000000000000 ) ) 
 REPRESENTATION_ITEM ( '' )  );
#71964=CARTESIAN_POINT ( 'NONE',  ( 2.449293598294707893E-16, 3.999999997268813168, -4.000000000000001776 ) ) ;
#71965=CARTESIAN_POINT ( 'NONE',  ( -7.347880794884122694E-16, 13.49999999726881406, 4.000000000000001776 ) ) ;
#71977=ORIENTED_EDGE ( 'NONE', *, *, #32388, .T. ) ;
#71984=CARTESIAN_POINT ( 'NONE',  ( -1.656854249492383691, 15.68750000000000000, 4.000000000000000888 ) ) ;
#71985=CARTESIAN_POINT ( 'NONE',  ( 1.881053915767122664, 15.12499999863440792, 4.541265875000001451 ) ) ;
#72016=CARTESIAN_POINT ( 'NONE',  ( 2.449293598294707893E-16, 5.999999997268813168, -4.000000000000001776 ) ) ;
#72021=CARTESIAN_POINT ( 'NONE',  ( -7.347880794884122694E-16, 12.75000000000000178, 4.000000000000001776 ) ) ;
#72025=CARTESIAN_POINT ( 'NONE',  ( -1.656854249492383468, 6.687500000000000888, 4.000000000000000888 ) ) ;
#72037=CARTESIAN_POINT ( 'NONE',  ( -7.347880794884122694E-16, 10.49999999726881406, 4.000000000000001776 ) ) ;
#72041=ORIENTED_EDGE ( 'NONE', *, *, #45533, .T. ) ;
#72049=CARTESIAN_POINT ( 'NONE',  ( 4.000000000000002665, 22.00000000000000000, 0.000000000000000000 ) ) ;
#72063=CARTESIAN_POINT ( 'NONE',  ( -4.541265875000002339, 18.93749999863440436, -5.561446717895856393E-16 ) ) ;
#72066=CARTESIAN_POINT ( 'NONE',  ( 3.211159895383560947, 3.312499998634407028, 3.211159895383562723 ) ) ;
#72067=EDGE_CURVE ( 'NONE', #48083, #57615, #49222, .T. ) ;
#72075=CARTESIAN_POINT ( 'NONE',  ( -1.656854249492383691, 2.687500000000000888, 4.000000000000000888 ) ) ;
#72077=CARTESIAN_POINT ( 'NONE',  ( -1.656854249492381248, 18.06249999726882294, -4.000000000000001776 ) ) ;
#72078=CARTESIAN_POINT ( 'NONE',  ( -1.881053915767121776, 2.624999998634406584, -4.541265875000002339 ) ) ;
#72082=EDGE_CURVE ( 'NONE', #51031, #16346, #19900, .T. ) ;
#72087=CARTESIAN_POINT ( 'NONE',  ( -8.342170076843785083E-16, 18.06249999863440792, 4.541265875000002339 ) ) ;
#72108=CARTESIAN_POINT ( 'NONE',  ( -4.000000000000001776, 5.500000000000000000, -4.898587196589415787E-16 ) ) ;
#72117=CARTESIAN_POINT ( 'NONE',  ( 4.541265875000002339, 4.374999998634407028, -1.881053915767121554 ) ) ;
#72135=CARTESIAN_POINT ( 'NONE',  ( 1.881053915767121776, 18.62499999863440792, -4.541265875000002339 ) ) ;
#72158=CARTESIAN_POINT ( 'NONE',  ( -4.541265875000003227, 9.999999998634407916, 1.881053915767121110 ) ) ;
#72159=ORIENTED_EDGE ( 'NONE', *, *, #4626, .T. ) ;
#72168=CARTESIAN_POINT ( 'NONE',  ( -1.656854249492383691, 7.437499997268812280, 4.000000000000000888 ) ) ;
#72174=CARTESIAN_POINT ( 'NONE',  ( 1.881053915767121776, 6.499999998634407028, -4.541265875000002339 ) ) ;
#72182=CARTESIAN_POINT ( 'NONE',  ( -7.347880794884122694E-16, 9.750000000000000000, 4.000000000000001776 ) ) ;
#72200=CARTESIAN_POINT ( 'NONE',  ( 0.000000000000000000, 15.99999999999998579, 1.000000000000000000 ) ) ;
#72210=CARTESIAN_POINT ( 'NONE',  ( 2.449293598294707893E-16, 6.999999997268813168, -4.000000000000001776 ) ) ;
#72220=CARTESIAN_POINT ( 'NONE',  ( -8.342170076843785083E-16, 10.18749999863440614, 4.541265875000002339 ) ) ;
#72270=CARTESIAN_POINT ( 'NONE',  ( -3.211159895383561391, 17.81249999863440792, -3.211159895383561835 ) ) ;
#72276=ORIENTED_EDGE ( 'NONE', *, *, #9936, .F. ) ;
#72280=CARTESIAN_POINT ( 'NONE',  ( 2.449293598294707893E-16, 20.25000000000000000, -4.000000000000001776 ) ) ;
#72306=ORIENTED_EDGE ( 'NONE', *, *, #17146, .F. ) ;
#72316=CARTESIAN_POINT ( 'NONE',  ( -4.541265875000002339, 16.74999999863440792, -1.881053915767121998 ) ) ;
#72321=ORIENTED_EDGE ( 'NONE', *, *, #12451, .F. ) ;
#72337=CARTESIAN_POINT ( 'NONE',  ( 2.449293598294707893E-16, 15.25000000000000000, -4.000000000000001776 ) ) ;
#72349=CYLINDRICAL_SURFACE ( 'NONE', #31628, 4.000000000000001776 ) ;
#72367=CARTESIAN_POINT ( 'NONE',  ( -1.656854249492381248, 14.31250000000000000, -4.000000000000001776 ) ) ;
#72368=CARTESIAN_POINT ( 'NONE',  ( -8.342170076843785083E-16, 20.06249999863440436, 4.541265875000002339 ) ) ;
#72395=EDGE_CURVE ( 'NONE', #5243, #25993, #59313, .T. ) ;
#72445=DIRECTION ( 'NONE',  ( -0.000000000000000000, -1.000000000000000000, -0.000000000000000000 ) ) ;
#72454=CARTESIAN_POINT ( 'NONE',  ( -4.541265875000003227, 21.96751355773092129, 0.9033139658336462041 ) ) ;
#72457=VECTOR ( 'NONE', #4305, 1000.000000000000000 ) ;
#72458=CARTESIAN_POINT ( 'NONE',  ( 4.541265875000001451, 3.374999998634406584, 1.881053915767124440 ) ) ;
#72464=CARTESIAN_POINT ( 'NONE',  ( 1.656854249492381248, 5.187500000000001776, -4.000000000000001776 ) ) ;
#72465=CARTESIAN_POINT ( 'NONE',  ( 2.828427124746191623, 16.87499999726881583, -2.828427124746191623 ) ) ;
#72466=CARTESIAN_POINT ( 'NONE',  ( 2.780723358947928197E-16, 4.562499998634407028, -4.541265875000002339 ) ) ;
#72473=CARTESIAN_POINT ( 'NONE',  ( -4.541265875000002339, 17.81249999863440792, -5.561446717895856393E-16 ) ) ;
#72484=CARTESIAN_POINT ( 'NONE',  ( -2.828427124746192067, 21.37499999726881583, 2.828427124746190735 ) ) ;
#72504=CARTESIAN_POINT ( 'NONE',  ( 3.211159895383561835, 6.437499998634407028, -3.211159895383561835 ) ) ;
#72523=CARTESIAN_POINT ( 'NONE',  ( -1.881053915767121554, 21.74999999863440436, -4.541265875000002339 ) ) ;
#72548=CARTESIAN_POINT ( 'NONE',  ( -1.881053915767121776, 9.749999998634404363, -4.541265875000002339 ) ) ;
#72559=CARTESIAN_POINT ( 'NONE',  ( 2.828427124746190291, 4.624999997268813168, 2.828427124746192067 ) ) ;
#72566=CARTESIAN_POINT ( 'NONE',  ( -3.211159895383562723, 5.937499998634407028, 3.211159895383561391 ) ) ;
#72573=CYLINDRICAL_SURFACE ( 'NONE', #49644, 4.000000000000001776 ) ;
#72608=CARTESIAN_POINT ( 'NONE',  ( 4.541265875000002339, 9.499999998634406140, -1.881053915767121554 ) ) ;
#72612=CARTESIAN_POINT ( 'NONE',  ( 4.000000000000001776, 1.000000000000000222, 0.000000000000000000 ) ) ;
#72655=CARTESIAN_POINT ( 'NONE',  ( 3.211159895383561835, 16.56249999863440436, -3.211159895383561835 ) ) ;
#72665=CIRCLE ( 'NONE', #70251, 10.00000000000001243 ) ;
#72700=CARTESIAN_POINT ( 'NONE',  ( 4.541265875000002339, 19.37499999863440792, -1.881053915767121554 ) ) ;
#72733=CARTESIAN_POINT ( 'NONE',  ( 2.449293598294707893E-16, 19.25000000000000000, -4.000000000000001776 ) ) ;
#72750=CARTESIAN_POINT ( 'NONE',  ( -1.656854249492383691, 14.68750000000000000, 4.000000000000000888 ) ) ;
#72752=CARTESIAN_POINT ( 'NONE',  ( 3.211159895383560947, 18.18749999863440792, 3.211159895383562723 ) ) ;
#72801=LINE ( 'NONE', #19611, #53933 ) ;
#72829=CARTESIAN_POINT ( 'NONE',  ( 1.881053915767122664, 21.24999999863440792, 4.541265875000001451 ) ) ;
#72833=CARTESIAN_POINT ( 'NONE',  ( -4.541265875000003227, 3.999999998634406140, 1.881053915767121110 ) ) ;
#72840=CARTESIAN_POINT ( 'NONE',  ( 4.000000000000001776, 6.000000000000000000, 0.000000000000000000 ) ) ;
#72841=CARTESIAN_POINT ( 'NONE',  ( -2.828427124746190735, 19.12499999726881228, -2.828427124746191623 ) ) ;
#72842=CARTESIAN_POINT ( 'NONE',  ( 1.881053915767121998, 7.499999998634407916, -4.541265875000002339 ) ) ;
#72849=CARTESIAN_POINT ( 'NONE',  ( -8.342170076843785083E-16, 19.06249999863440436, 4.541265875000002339 ) ) ;
#72867=( BOUNDED_CURVE ( )  B_SPLINE_CURVE ( 2, ( #64124, #31267, #42206, #53549, #19203, #69788, #25225, #18104, #12431 ),
 .UNSPECIFIED., .F., .F. ) 
 B_SPLINE_CURVE_WITH_KNOTS ( ( 3, 2, 2, 2, 3 ),
 ( 0.2613636363636363535, 0.2670454545454545303, 0.2727272727272727071, 0.2784090909090908839, 0.2840909090909091161 ),
 .UNSPECIFIED. ) 
 CURVE ( )  GEOMETRIC_REPRESENTATION_ITEM ( )  RATIONAL_B_SPLINE_CURVE ( ( 1.000000000000000000, 0.9238795325112867385, 1.000000000000000000, 0.9238795325112867385, 1.000000000000000000, 0.9238795325112867385, 1.000000000000000000, 0.9238795325112867385, 1.000000000000000000 ) ) 
 REPRESENTATION_ITEM ( '' )  );
#72880=CARTESIAN_POINT ( 'NONE',  ( 1.881053915767121776, 7.499999998634408804, -4.541265875000002339 ) ) ;
#72896=CARTESIAN_POINT ( 'NONE',  ( 2.780723358947928197E-16, 20.68749999863440436, -4.541265875000002339 ) ) ;
#72918=CARTESIAN_POINT ( 'NONE',  ( 1.881053915767122664, 9.249999998634407916, 4.541265875000001451 ) ) ;
#72927=CARTESIAN_POINT ( 'NONE',  ( 1.656854249492381248, 4.937499997268813168, -4.000000000000001776 ) ) ;
#72931=ADVANCED_FACE ( 'NONE', ( #10186 ), #56215, .T. ) ;
#72936=CARTESIAN_POINT ( 'NONE',  ( -3.211159895383562723, 4.937499998634407028, 3.211159895383561391 ) ) ;
#72950=EDGE_CURVE ( 'NONE', #31861, #40603, #73851, .T. ) ;
#72961=( BOUNDED_CURVE ( )  B_SPLINE_CURVE ( 2, ( #43356, #54328, #36964, #59970, #25627, #54700, #19972, #72025, #8666 ),
 .UNSPECIFIED., .F., .F. ) 
 B_SPLINE_CURVE_WITH_KNOTS ( ( 3, 2, 2, 2, 3 ),
 ( 0.2840909090909091161, 0.2897727272727272929, 0.2954545454545454697, 0.3011363636363636465, 0.3068181818181818232 ),
 .UNSPECIFIED. ) 
 CURVE ( )  GEOMETRIC_REPRESENTATION_ITEM ( )  RATIONAL_B_SPLINE_CURVE ( ( 1.000000000000000000, 0.9238795325112867385, 1.000000000000000000, 0.9238795325112867385, 1.000000000000000000, 0.9238795325112867385, 1.000000000000000000, 0.9238795325112867385, 1.000000000000000000 ) ) 
 REPRESENTATION_ITEM ( '' )  );
#72974=CARTESIAN_POINT ( 'NONE',  ( 2.449293598294707893E-16, 10.25000000000000000, -4.000000000000001776 ) ) ;
#72980=CARTESIAN_POINT ( 'NONE',  ( 4.541265875000002339, 7.499999998634408804, -1.881053915767121554 ) ) ;
#73023=CARTESIAN_POINT ( 'NONE',  ( 4.541265875000001451, 17.37499999863440436, 1.881053915767124440 ) ) ;
#73036=CARTESIAN_POINT ( 'NONE',  ( -0.3527280876246363106, 21.99999999999999289, -4.023046032806171901 ) ) ;
#73060=CARTESIAN_POINT ( 'NONE',  ( 2.828427124746191623, 2.125000000000000000, -2.828427124746191623 ) ) ;
#73067=CARTESIAN_POINT ( 'NONE',  ( 3.211159895383561835, 16.43749999863440436, -3.211159895383561835 ) ) ;
#73099=CARTESIAN_POINT ( 'NONE',  ( -4.000000000000001776, 1.249999997268813168, -4.898587196589415787E-16 ) ) ;
#73114=ORIENTED_EDGE ( 'NONE', *, *, #64002, .F. ) ;
#73119=ORIENTED_EDGE ( 'NONE', *, *, #9666, .F. ) ;
#73120=CARTESIAN_POINT ( 'NONE',  ( -1.656854249492383691, 21.68750000000000000, 4.000000000000000888 ) ) ;
#73121=CARTESIAN_POINT ( 'NONE',  ( -3.211159895383562723, 20.93749999863440436, 3.211159895383561391 ) ) ;
#73198=EDGE_CURVE ( 'NONE', #56214, #45255, #41172, .T. ) ;
#73199=AXIS2_PLACEMENT_3D ( 'NONE', #74078, #44671, #17098 ) ;
#73205=CARTESIAN_POINT ( 'NONE',  ( 4.541265875000002339, 19.43749999863440436, 0.000000000000000000 ) ) ;
#73208=CARTESIAN_POINT ( 'NONE',  ( -1.881053915767124440, 6.124999998634407916, 4.541265875000001451 ) ) ;
#73213=CARTESIAN_POINT ( 'NONE',  ( 2.828427124746190291, 6.875000000000000000, 2.828427124746192067 ) ) ;
#73214=CARTESIAN_POINT ( 'NONE',  ( 4.000000000000001776, 19.74999999726881228, 0.000000000000000000 ) ) ;
#73215=CARTESIAN_POINT ( 'NONE',  ( 1.881053915767122664, 9.124999998634407916, 4.541265875000001451 ) ) ;
#73222=CARTESIAN_POINT ( 'NONE',  ( 2.780723358947928197E-16, 19.56249999863440436, -4.541265875000002339 ) ) ;
#73253=CARTESIAN_POINT ( 'NONE',  ( -3.211159895383561391, 6.687499998634407028, -3.211159895383561835 ) ) ;
#73263=FACE_OUTER_BOUND ( 'NONE', #41855, .T. ) ;
#73268=EDGE_CURVE ( 'NONE', #13147, #25107, #51296, .T. ) ;
#73271=CARTESIAN_POINT ( 'NONE',  ( 1.881053915767121776, 19.62499999863441147, -4.541265875000002339 ) ) ;
#73294=CARTESIAN_POINT ( 'NONE',  ( 1.881053915767121998, 8.624999998634407916, -4.541265875000002339 ) ) ;
#73295=ORIENTED_EDGE ( 'NONE', *, *, #37944, .F. ) ;
#73305=CARTESIAN_POINT ( 'NONE',  ( 1.656854249492381914, 7.562499997268812280, 4.000000000000000888 ) ) ;
#73310=CARTESIAN_POINT ( 'NONE',  ( 4.000000000000001776, 12.74999999726881406, 0.000000000000000000 ) ) ;
#73312=CARTESIAN_POINT ( 'NONE',  ( 4.541265875000001451, 6.249999998634407916, 1.881053915767124440 ) ) ;
#73341=DIRECTION ( 'NONE',  ( 0.000000000000000000, 0.000000000000000000, -1.000000000000000000 ) ) ;
#73353=CARTESIAN_POINT ( 'NONE',  ( -4.541265875000002339, 6.874999998634407916, -1.881053915767121998 ) ) ;
#73356=CARTESIAN_POINT ( 'NONE',  ( 1.656854249492379472, 1.187500000000000444, -4.000000000000002665 ) ) ;
#73357=ORIENTED_EDGE ( 'NONE', *, *, #23534, .F. ) ;
#73383=CARTESIAN_POINT ( 'NONE',  ( 2.449293598294707893E-16, 7.250000000000000000, -4.000000000000001776 ) ) ;
#73394=CARTESIAN_POINT ( 'NONE',  ( -4.541265875000002339, 16.87499999863440436, -1.881053915767121998 ) ) ;
#73418=CARTESIAN_POINT ( 'NONE',  ( -1.737867177246331662, 21.99999999999999645, 4.195582608135537406 ) ) ;
#73435=CARTESIAN_POINT ( 'NONE',  ( -3.211159895383562723, 18.93749999863440436, 3.211159895383561391 ) ) ;
#73484=ORIENTED_EDGE ( 'NONE', *, *, #37944, .T. ) ;
#73485=CARTESIAN_POINT ( 'NONE',  ( 4.000000000000000888, 19.93750000000000000, 1.656854249492384135 ) ) ;
#73486=CARTESIAN_POINT ( 'NONE',  ( 4.541265875000002339, 20.31249999863440436, 0.000000000000000000 ) ) ;
#73520=CARTESIAN_POINT ( 'NONE',  ( 2.828427124746191623, 16.87499999726881583, -2.828427124746191623 ) ) ;
#73551=DIRECTION ( 'NONE',  ( -0.000000000000000000, -1.000000000000000000, -0.000000000000000000 ) ) ;
#73571=CARTESIAN_POINT ( 'NONE',  ( -1.881053915767121554, 9.749999998634406140, -4.541265875000002339 ) ) ;
#73578=CARTESIAN_POINT ( 'NONE',  ( -2.828427124746192067, 9.625000000000000000, 2.828427124746190735 ) ) ;
#73579=CARTESIAN_POINT ( 'NONE',  ( -1.656854249492381248, 22.06249999726881583, -4.000000000000001776 ) ) ;
#73580=CARTESIAN_POINT ( 'NONE',  ( 4.541265875000002339, 6.374999998634408804, -1.881053915767121776 ) ) ;
#73597=CARTESIAN_POINT ( 'NONE',  ( -1.656854249492405895, 21.06249999726881938, -3.999999999999976463 ) ) ;
#73603=EDGE_CURVE ( 'NONE', #42656, #56422, #38305, .T. ) ;
#73659=CARTESIAN_POINT ( 'NONE',  ( 3.211159895383561835, 13.56249999863440614, -3.211159895383561835 ) ) ;
#73670=CARTESIAN_POINT ( 'NONE',  ( 1.656854249492381248, 9.937499997268814056, -4.000000000000001776 ) ) ;
#73677=CARTESIAN_POINT ( 'NONE',  ( 4.541265875000002339, 9.374999998634404363, -1.881053915767121554 ) ) ;
#73708=CARTESIAN_POINT ( 'NONE',  ( -7.347880794884122694E-16, 7.499999997268813168, 4.000000000000001776 ) ) ;
#73719=CARTESIAN_POINT ( 'NONE',  ( -1.881053915767124440, 8.124999998634407916, 4.541265875000001451 ) ) ;
#73735=CARTESIAN_POINT ( 'NONE',  ( -7.347880794884122694E-16, 2.750000000000000000, 4.000000000000001776 ) ) ;
#73748=CARTESIAN_POINT ( 'NONE',  ( -1.656854249492381248, 4.312500000000000888, -4.000000000000001776 ) ) ;
#73761=CARTESIAN_POINT ( 'NONE',  ( -4.541265875000002339, 14.87499999863441147, -1.881053915767121998 ) ) ;
#73762=EDGE_LOOP ( 'NONE', ( #37496, #36491 ) ) ;
#73786=CARTESIAN_POINT ( 'NONE',  ( -4.195582579073398932, 22.00000000000000355, 1.737867247408543925 ) ) ;
#73800=EDGE_CURVE ( 'NONE', #2093, #55673, #20567, .T. ) ;
#73806=CARTESIAN_POINT ( 'NONE',  ( 3.211159895383561835, 18.43749999863440436, -3.211159895383561835 ) ) ;
#73818=ORIENTED_EDGE ( 'NONE', *, *, #48153, .F. ) ;
#73828=CARTESIAN_POINT ( 'NONE',  ( 4.000000000000001776, 15.00000000000000000, 0.000000000000000000 ) ) ;
#73851=( BOUNDED_CURVE ( )  B_SPLINE_CURVE ( 2, ( #45625, #12407, #53522, #46371, #47100, #23730, #18072, #12770, #6397 ),
 .UNSPECIFIED., .F., .F. ) 
 B_SPLINE_CURVE_WITH_KNOTS ( ( 3, 2, 2, 2, 3 ),
 ( 0.1704545454545454697, 0.1761363636363636742, 0.1818181818181818232, 0.1875000000000000000, 0.1931818181818181768 ),
 .UNSPECIFIED. ) 
 CURVE ( )  GEOMETRIC_REPRESENTATION_ITEM ( )  RATIONAL_B_SPLINE_CURVE ( ( 0.9999999999999996669, 0.9238795325112870716, 1.000000000000000000, 0.9238795325112867385, 1.000000000000000000, 0.9238795325112867385, 1.000000000000000000, 0.9238795325112867385, 1.000000000000000000 ) ) 
 REPRESENTATION_ITEM ( '' )  );
#73860=CARTESIAN_POINT ( 'NONE',  ( -4.000000000000001776, 20.50000000000000000, -4.898587196589415787E-16 ) ) ;
#73861=CARTESIAN_POINT ( 'NONE',  ( -4.541265875000003227, 20.87499999863440792, 1.881053915767121110 ) ) ;
#73874=EDGE_CURVE ( 'NONE', #12049, #48083, #58542, .T. ) ;
#73912=CARTESIAN_POINT ( 'NONE',  ( -1.224646799147353454E-16, 25.94987437106619765, -1.000000000000000000 ) ) ;
#73929=CARTESIAN_POINT ( 'NONE',  ( 4.000000000000001776, 18.81249999726881228, -1.656854249492381248 ) ) ;
#73945=CARTESIAN_POINT ( 'NONE',  ( -3.211159895383561391, 7.812499998634407028, -3.211159895383561835 ) ) ;
#73949=CARTESIAN_POINT ( 'NONE',  ( -4.000000000000001776, 6.500000000000000888, -4.898587196589415787E-16 ) ) ;
#73950=CARTESIAN_POINT ( 'NONE',  ( 4.000000000000000888, 22.68749999726881228, 1.656854249492384135 ) ) ;
#73951=CARTESIAN_POINT ( 'NONE',  ( -4.541265875000002339, 9.812499998634406140, -5.561446717895856393E-16 ) ) ;
#73977=EDGE_CURVE ( 'NONE', #40603, #23575, #7449, .T. ) ;
#74018=CARTESIAN_POINT ( 'NONE',  ( 2.449293598294707893E-16, 14.99999999726881406, -4.000000000000001776 ) ) ;
#74027=CARTESIAN_POINT ( 'NONE',  ( 4.541265875000002339, 11.43749999863440614, 0.000000000000000000 ) ) ;
#74040=CARTESIAN_POINT ( 'NONE',  ( -1.656854249492383691, 8.437499997268814056, 4.000000000000000888 ) ) ;
#74047=CARTESIAN_POINT ( 'NONE',  ( -1.881053915767124440, 10.99999999863440969, 4.541265875000001451 ) ) ;
#74078=CARTESIAN_POINT ( 'NONE',  ( -8.000000000000003553, 22.99999999999999645, 1.000000000000000000 ) ) ;
#74093=CARTESIAN_POINT ( 'NONE',  ( 1.881053915767121776, 11.62499999863440969, -4.541265875000002339 ) ) ;
#74121=CARTESIAN_POINT ( 'NONE',  ( -4.000000000000001776, 4.500000000000000888, -4.898587196589415787E-16 ) ) ;
#74134=CARTESIAN_POINT ( 'NONE',  ( 2.449293598294707893E-16, 15.25000000000000000, -4.000000000000001776 ) ) ;
#74135=CARTESIAN_POINT ( 'NONE',  ( 1.881053915767121776, 21.62499999863441502, -4.541265875000002339 ) ) ;
#74176=CARTESIAN_POINT ( 'NONE',  ( -4.541265875000002339, 1.874999998634406806, -1.881053915767121998 ) ) ;
#74214=CARTESIAN_POINT ( 'NONE',  ( 4.000000000000001776, 0.8124999972688135008, -1.656854249492381248 ) ) ;
#74233=CARTESIAN_POINT ( 'NONE',  ( -1.656854249492381248, 19.31250000000000000, -4.000000000000001776 ) ) ;
#74236=CARTESIAN_POINT ( 'NONE',  ( 2.449293598294707893E-16, 4.999999997268813168, -4.000000000000001776 ) ) ;
#74314=CARTESIAN_POINT ( 'NONE',  ( -4.541265875000002339, 7.937499998634407028, -5.561446717895856393E-16 ) ) ;
#74320=CARTESIAN_POINT ( 'NONE',  ( -2.828427124746190735, 6.375000000000000888, -2.828427124746191623 ) ) ;
#74322=CARTESIAN_POINT ( 'NONE',  ( 2.780723358947928197E-16, 7.562499998634407028, -4.541265875000002339 ) ) ;
#74329=CARTESIAN_POINT ( 'NONE',  ( -7.347880794884122694E-16, 10.75000000000000000, 4.000000000000001776 ) ) ;
#74392=( BOUNDED_CURVE ( )  B_SPLINE_CURVE ( 2, ( #60865, #26148, #4283, #3918, #66151, #9187, #49549, #61988, #32208 ),
 .UNSPECIFIED., .F., .F. ) 
 B_SPLINE_CURVE_WITH_KNOTS ( ( 3, 2, 2, 2, 3 ),
 ( 0.6022727272727272929, 0.6079545454545454142, 0.6136363636363636465, 0.6193181818181817677, 0.6250000000000000000 ),
 .UNSPECIFIED. ) 
 CURVE ( )  GEOMETRIC_REPRESENTATION_ITEM ( )  RATIONAL_B_SPLINE_CURVE ( ( 1.000000000000000000, 0.9238795325112867385, 1.000000000000000000, 0.9238795325112867385, 1.000000000000000000, 0.9238795325112867385, 1.000000000000000000, 0.9238795325112867385, 1.000000000000000000 ) ) 
 REPRESENTATION_ITEM ( '' )  );
#74400=CARTESIAN_POINT ( 'NONE',  ( -4.541265875000002339, 12.87499999863440969, -1.881053915767121998 ) ) ;
#74412=CARTESIAN_POINT ( 'NONE',  ( -4.000000000000001776, 10.24999999726881406, -4.898587196589415787E-16 ) ) ;
#74413=CARTESIAN_POINT ( 'NONE',  ( 4.000000000000001776, 18.00000000000000355, 0.000000000000000000 ) ) ;
#74419=CARTESIAN_POINT ( 'NONE',  ( -4.541265875000002339, 9.749999998634406140, -1.881053915767121998 ) ) ;
#74422=CARTESIAN_POINT ( 'NONE',  ( 2.449293598294707893E-16, 17.99999999726881583, -4.000000000000001776 ) ) ;
#74461=CARTESIAN_POINT ( 'NONE',  ( -4.541265875000002339, 10.93749999863440792, -5.561446717895856393E-16 ) ) ;
#74482=STYLED_ITEM('',(#74706),#41611);
#74505=CARTESIAN_POINT ( 'NONE',  ( -4.541265875000003227, 21.99999999863440792, 1.881053915767121110 ) ) ;
#74547=EDGE_CURVE ( 'NONE', #28042, #11511, #18025, .T. ) ;
#74553=CARTESIAN_POINT ( 'NONE',  ( -4.541265875000002339, 21.74999999863440436, -1.881053915767121998 ) ) ;
#74561=CARTESIAN_POINT ( 'NONE',  ( -4.000000000000001776, 19.24999999726881228, -4.898587196589415787E-16 ) ) ;
#74610=CARTESIAN_POINT ( 'NONE',  ( -2.828427124746190735, 19.37500000000000000, -2.828427124746191623 ) ) ;
#74611=CARTESIAN_POINT ( 'NONE',  ( 4.000000000000000888, 2.687499997268813612, 1.656854249492384135 ) ) ;
#74630=CARTESIAN_POINT ( 'NONE',  ( 4.000000000000000888, 20.93750000000000000, 1.656854249492384135 ) ) ;
#74647=CARTESIAN_POINT ( 'NONE',  ( 2.828427124746190291, 17.62499999726881583, 2.828427124746192067 ) ) ;
#74648=CARTESIAN_POINT ( 'NONE',  ( 1.656854249492369036, 10.18750000000000000, -4.000000000000014211 ) ) ;
#74649=CARTESIAN_POINT ( 'NONE',  ( 1.881053915767121776, 10.49999999863440792, -4.541265875000002339 ) ) ;
#74700=COLOUR_RGB('Black',0.12,0.14,0.17);
#74701=FILL_AREA_STYLE_COLOUR('',#74700);
#74702=FILL_AREA_STYLE('',(#74701));
#74703=SURFACE_STYLE_FILL_AREA(#74702);
#74704=SURFACE_SIDE_STYLE('',(#74703));
#74705=SURFACE_STYLE_USAGE(.BOTH.,#74704);
#74706=PRESENTATION_STYLE_ASSIGNMENT((#74705));
ENDSEC;
END-ISO-10303-21;
